ISO-10303-21;
HEADER;
FILE_DESCRIPTION (('STEP AP214'),
    '1' );
FILE_NAME ('Pusher Pull Spring.step',
    '2026-10-06T10:23:46',
    ( '' ),
    ( '' ),
    'SwSTEP 2.0',
    'SolidWorks 2020',
    '' );
FILE_SCHEMA (( 'AUTOMOTIVE_DESIGN' ));
ENDSEC;

DATA;
#5=CARTESIAN_POINT ( 'NONE',  ( 39.02088643472237806, -8.703840866421918676, 73.73360434286902887 ) ) ;
#7=CARTESIAN_POINT ( 'NONE',  ( 38.82593461698262871, -16.91368208888610170, 69.62690120949091011 ) ) ;
#9=CARTESIAN_POINT ( 'NONE',  ( 37.25202387243752611, -25.21368208888610241, 70.00779233799262613 ) ) ;
#12=CARTESIAN_POINT ( 'NONE',  ( 36.80608444377002542, -2.303840866421914768, 72.40698646996135324 ) ) ;
#15=CARTESIAN_POINT ( 'NONE',  ( 39.82603832034400426, -20.31368208888610738, 72.40698646996133903 ) ) ;
#18=CARTESIAN_POINT ( 'NONE',  ( 36.68196826583682935, -18.00384086642191406, 70.79240656858107172 ) ) ;
#21=CARTESIAN_POINT ( 'NONE',  ( 36.64852494920107517, -13.41368208888610525, 70.89533451361947414 ) ) ;
#23=CARTESIAN_POINT ( 'NONE',  ( 39.12911128074873801, -24.11368208888611164, 73.69843995877326392 ) ) ;
#28=CARTESIAN_POINT ( 'NONE',  ( 38.26194895904384197, -26.60384086642191193, 72.51602215082114355 ) ) ;
#36=CARTESIAN_POINT ( 'NONE',  ( 36.29569395875881099, -26.30384086642192187, 72.77780686321126780 ) ) ;
#38=CARTESIAN_POINT ( 'NONE',  ( 36.89935272106204422, -5.213682088886100630, 69.52238214136768590 ) ) ;
#44=CARTESIAN_POINT ( 'NONE',  ( 38.37017380507020192, 1.986317911113890444, 73.11602215082119471 ) ) ;
#45=CARTESIAN_POINT ( 'NONE',  ( 36.80608444377002542, -24.30384086642191832, 72.40698646996131060 ) ) ;
#54=CARTESIAN_POINT ( 'NONE',  ( 39.51027997493896748, -3.103840866421909706, 71.43714994484034264 ) ) ;
#61=CARTESIAN_POINT ( 'NONE',  ( 39.31564783533280405, -12.31368208888610027, 72.03616607671141026 ) ) ;
#62=CARTESIAN_POINT ( 'NONE',  ( 39.51027997493896748, -10.51368208888610134, 71.32335560751961623 ) ) ;
#70=CARTESIAN_POINT ( 'NONE',  ( 39.29254315202757653, -18.80384086642191477, 72.81632618279321889 ) ) ;
#75=CARTESIAN_POINT ( 'NONE',  ( 38.37017380507020192, -18.01368208888610312, 72.51602215082118619 ) ) ;
#79=CARTESIAN_POINT ( 'NONE',  ( 37.33957961208646736, -13.81368208888610916, 72.81632618279321889 ) ) ;
#82=CARTESIAN_POINT ( 'NONE',  ( 39.82603832034400426, -28.31368208888610027, 72.40698646996131060 ) ) ;
#83=CARTESIAN_POINT ( 'NONE',  ( 40.08931077638955998, -29.10876147764802369, 70.44264307849509521 ) ) ;
#91=CARTESIAN_POINT ( 'NONE',  ( 39.73277004305197124, -5.403840866421909972, 69.52238214136768590 ) ) ;
#96=CARTESIAN_POINT ( 'NONE',  ( 39.95015449827720744, -8.613682088886104538, 70.79240656858107172 ) ) ;
#99=CARTESIAN_POINT ( 'NONE',  ( 40.33642880535524000, -12.31368208888611093, 72.77780686321126780 ) ) ;
#112=CARTESIAN_POINT ( 'NONE',  ( 37.69225076346193504, -15.80384086642191299, 70.42958956619168021 ) ) ;
#113=CARTESIAN_POINT ( 'NONE',  ( 39.37952058850012804, -22.61368208888610454, 70.97781676520601479 ) ) ;
#121=CARTESIAN_POINT ( 'NONE',  ( 38.26194895904384197, -22.60384086642191903, 73.71602215082113219 ) ) ;
#124=CARTESIAN_POINT ( 'NONE',  ( 37.12184278917507640, -23.51368208888609956, 71.43714994484032843 ) ) ;
#125=CARTESIAN_POINT ( 'NONE',  ( 37.61123632939165873, -5.913682088886105248, 73.73360434286902887 ) ) ;
#129=CARTESIAN_POINT ( 'NONE',  ( 37.25260217561390874, -0.003840866421911393481, 70.97781676520604321 ) ) ;
#135=CARTESIAN_POINT ( 'NONE',  ( 36.89935272106205133, -6.403840866421917077, 73.23812341099225875 ) ) ;
#139=CARTESIAN_POINT ( 'NONE',  ( 39.95015449827720744, -12.61368208888610454, 70.79240656858105751 ) ) ;
#142=CARTESIAN_POINT ( 'NONE',  ( 36.87297107704153376, -25.71368208888610596, 72.49904802271738902 ) ) ;
#146=CARTESIAN_POINT ( 'NONE',  ( 36.87297107704151244, -1.903840866421906641, 70.26145752964255564 ) ) ;
#148=CARTESIAN_POINT ( 'NONE',  ( 36.80608444377001121, -19.31368208888609672, 70.35351908239857721 ) ) ;
#151=CARTESIAN_POINT ( 'NONE',  ( 39.38009889167648936, -17.40384086642190908, 70.00779233799262613 ) ) ;
#153=CARTESIAN_POINT ( 'NONE',  ( 36.64852494920107517, -11.41368208888610525, 70.89533451361947414 ) ) ;
#155=CARTESIAN_POINT ( 'NONE',  ( 37.50301148336529167, -19.11368208888609388, 69.06206559358665231 ) ) ;
#160=CARTESIAN_POINT ( 'NONE',  ( 38.73920764526923932, -19.50384086642191406, 70.26206559358661252 ) ) ;
#163=CARTESIAN_POINT ( 'NONE',  ( 39.59824383043523000, -28.76838690529542220, 70.55371702292011094 ) ) ;
#166=CARTESIAN_POINT ( 'NONE',  ( 40.26954217208372455, -20.90384086642191974, 72.86986841596734621 ) ) ;
#167=CARTESIAN_POINT ( 'NONE',  ( 36.07789103942398867, 0.5863179111138955291, 70.70992431699450265 ) ) ;
#174=CARTESIAN_POINT ( 'NONE',  ( 36.68196826583682935, -24.00384086642191050, 70.79240656858105751 ) ) ;
#181=CARTESIAN_POINT ( 'NONE',  ( 39.41296390513587511, -9.203840866421909794, 71.08074471024443142 ) ) ;
#188=CARTESIAN_POINT ( 'NONE',  ( 39.31564783533280405, -6.313682088886101162, 72.03616607671141026 ) ) ;
#189=CARTESIAN_POINT ( 'NONE',  ( 39.02742774030102879, -4.213682088886099741, 72.26730301774236409 ) ) ;
#196=CARTESIAN_POINT ( 'NONE',  ( 38.93415946300896024, -17.50384086642190695, 69.66206559358661821 ) ) ;
#206=CARTESIAN_POINT ( 'NONE',  ( 39.82603832034401847, -12.31368208888610738, 72.40698646996131060 ) ) ;
#220=CARTESIAN_POINT ( 'NONE',  ( 36.11133435605973574, -6.003840866421917610, 70.60699637195612866 ) ) ;
#223=CARTESIAN_POINT ( 'NONE',  ( 37.80618814713140097, -9.913682088886107024, 73.13360434286904876 ) ) ;
#226=CARTESIAN_POINT ( 'NONE',  ( 36.29569395875879678, -15.31368208888610205, 69.98269868914867686 ) ) ;
#234=CARTESIAN_POINT ( 'NONE',  ( 38.93987200065208754, -24.81368208888610738, 70.42958956619166599 ) ) ;
#240=CARTESIAN_POINT ( 'NONE',  ( 37.61123632939164452, -25.70384086642191690, 69.02690120949091579 ) ) ;
#241=CARTESIAN_POINT ( 'NONE',  ( 37.33957961208646736, -27.81368208888611093, 72.81632618279320468 ) ) ;
#249=CARTESIAN_POINT ( 'NONE',  ( 40.77203464402485622, -1.103840866421915035, 71.43714994484034264 ) ) ;
#255=CARTESIAN_POINT ( 'NONE',  ( 39.95015449827720744, -4.613682088886104538, 70.79240656858107172 ) ) ;
#256=CARTESIAN_POINT ( 'NONE',  ( 39.29254315202756231, -24.81368208888610383, 69.94417936956671156 ) ) ;
#259=CARTESIAN_POINT ( 'NONE',  ( 39.98359781491296161, -3.203840866421912903, 70.89533451361947414 ) ) ;
#263=CARTESIAN_POINT ( 'NONE',  ( 37.21915885897815457, -26.20384086642190979, 71.67976084211551324 ) ) ;
#264=CARTESIAN_POINT ( 'NONE',  ( 36.64852494920107517, -9.413682088886107024, 70.89533451361948835 ) ) ;
#267=CARTESIAN_POINT ( 'NONE',  ( 36.64852494920107517, -10.20384086642191157, 71.86517103874049894 ) ) ;
#271=CARTESIAN_POINT ( 'NONE',  ( 36.64852494920107517, -9.413682088886107024, 70.89533451361948835 ) ) ;
#273=CARTESIAN_POINT ( 'NONE',  ( 38.37017380507020192, -18.01368208888610667, 73.71602215082113219 ) ) ;
#277=CARTESIAN_POINT ( 'NONE',  ( 38.63098279924290068, -16.70384086642190624, 72.53360434286904024 ) ) ;
#282=CARTESIAN_POINT ( 'NONE',  ( 37.61123632939164452, -19.70384086642190979, 69.02690120949091579 ) ) ;
#286=CARTESIAN_POINT ( 'NONE',  ( 39.82603832034400426, -26.31368208888611093, 72.40698646996131060 ) ) ;
#296=CARTESIAN_POINT ( 'NONE',  ( 39.29254315202757653, -20.80384086642191832, 72.81632618279321889 ) ) ;
#301=CARTESIAN_POINT ( 'NONE',  ( 38.26194895904384197, -0.6038408664219111488, 72.51602215082118619 ) ) ;
#311=CARTESIAN_POINT ( 'NONE',  ( 37.38336156205274818, -5.713682088886101518, 72.12822762946751709 ) ) ;
#313=CARTESIAN_POINT ( 'NONE',  ( 39.02742774030102879, -6.213682088886101518, 72.26730301774236409 ) ) ;
#320=CARTESIAN_POINT ( 'NONE',  ( 37.33957961208645315, -9.803840866421907663, 69.94417936956673998 ) ) ;
#327=CARTESIAN_POINT ( 'NONE',  ( 37.69796330110504101, -7.113682088886101873, 69.66206559358664663 ) ) ;
#341=CARTESIAN_POINT ( 'NONE',  ( 35.86008812008917346, -6.103840866421916367, 71.32335560751961623 ) ) ;
#344=CARTESIAN_POINT ( 'NONE',  ( 39.98359781491296161, -6.413682088886103472, 71.86517103874048473 ) ) ;
#349=CARTESIAN_POINT ( 'NONE',  ( 39.12911128074873801, -16.11368208888610809, 73.69843995877327814 ) ) ;
#358=CARTESIAN_POINT ( 'NONE',  ( 38.37017380507020192, -22.01368208888610312, 72.51602215082118619 ) ) ;
#365=CARTESIAN_POINT ( 'NONE',  ( 40.52078840805429394, -21.00384086642191761, 72.15350918040381600 ) ) ;
#367=CARTESIAN_POINT ( 'NONE',  ( 39.29254315202756231, -28.81368208888610383, 69.94417936956671156 ) ) ;
#376=CARTESIAN_POINT ( 'NONE',  ( 35.86008812008917346, -4.103840866421913702, 71.32335560751961623 ) ) ;
#380=CARTESIAN_POINT ( 'NONE',  ( 37.33957961208646736, -7.813682088886109156, 72.81632618279323310 ) ) ;
#389=CARTESIAN_POINT ( 'NONE',  ( 39.02742774030101458, -23.40384086642191264, 70.49320253461759478 ) ) ;
#390=CARTESIAN_POINT ( 'NONE',  ( 39.82603832034400426, -10.31368208888610383, 72.40698646996135324 ) ) ;
#393=CARTESIAN_POINT ( 'NONE',  ( 38.93415946300896024, -9.503840866421908729, 69.66206559358663242 ) ) ;
#397=CARTESIAN_POINT ( 'NONE',  ( 38.26194895904383486, -9.013682088886101340, 69.64448340153879258 ) ) ;
#399=CARTESIAN_POINT ( 'NONE',  ( 36.11133435605973574, -13.61368208888610454, 72.15350918040385864 ) ) ;
#403=CARTESIAN_POINT ( 'NONE',  ( 37.12184278917507640, -16.10384086642191193, 71.32335560751961623 ) ) ;
#410=CARTESIAN_POINT ( 'NONE',  ( 36.89935272106205133, -24.40384086642191974, 73.23812341099225875 ) ) ;
#413=CARTESIAN_POINT ( 'NONE',  ( 39.75915168707250302, -26.71368208888609530, 70.26145752964249880 ) ) ;
#418=CARTESIAN_POINT ( 'NONE',  ( 38.93415946300897446, -23.50384086642190340, 69.66206559358663242 ) ) ;
#429=CARTESIAN_POINT ( 'NONE',  ( 39.75915168707251723, -28.90384086642191619, 72.49904802271737481 ) ) ;
#438=UNCERTAINTY_MEASURE_WITH_UNIT (LENGTH_MEASURE( 1.000000000000000082E-05 ), #6854, 'distance_accuracy_value', 'NONE');
#439=CARTESIAN_POINT ( 'NONE',  ( 37.89291511884476904, -5.113682088886100985, 70.26206559358664094 ) ) ;
#440=CARTESIAN_POINT ( 'NONE',  ( 37.38336156205274818, -1.713682088886100852, 72.12822762946751709 ) ) ;
#448=CARTESIAN_POINT ( 'NONE',  ( 39.38009889167648936, -11.40384086642190908, 70.00779233799264034 ) ) ;
#457=CARTESIAN_POINT ( 'NONE',  ( 40.14115730948191185, -6.513682088886103116, 71.32335560751961623 ) ) ;
#470=CARTESIAN_POINT ( 'NONE',  ( 39.73277004305197124, -3.403840866421911748, 69.52238214136768590 ) ) ;
#474=CARTESIAN_POINT ( 'NONE',  ( 37.25202387243752611, -7.213682088886102406, 70.00779233799264034 ) ) ;
#476=CARTESIAN_POINT ( 'NONE',  ( 39.64521430340304420, -14.81368208888610205, 69.45876917294175712 ) ) ;
#488=CARTESIAN_POINT ( 'NONE',  ( 39.41296390513587511, -24.41368208888610525, 71.67976084211548482 ) ) ;
#495=CARTESIAN_POINT ( 'NONE',  ( 36.89935272106205133, -22.40384086642191974, 73.23812341099225875 ) ) ;
#496=CARTESIAN_POINT ( 'NONE',  ( 38.26194895904383486, -27.01368208888610312, 69.64448340153876416 ) ) ;
#505=CARTESIAN_POINT ( 'NONE',  ( 38.26194895904384197, -2.603840866421920364, 73.71602215082116061 ) ) ;
#510=CARTESIAN_POINT ( 'NONE',  ( 39.38009889167650357, -8.213682088886105959, 72.75271321436733274 ) ) ;
#520=CARTESIAN_POINT ( 'NONE',  ( 39.41296390513587511, -23.20384086642191335, 71.08074471024441721 ) ) ;
#521=CARTESIAN_POINT ( 'NONE',  ( 36.64852494920107517, -13.41368208888610525, 70.89533451361947414 ) ) ;
#524=CARTESIAN_POINT ( 'NONE',  ( 36.68196826583682935, -14.00384086642191228, 70.79240656858107172 ) ) ;
#527=CARTESIAN_POINT ( 'NONE',  ( 37.25202387243752611, -11.21368208888610241, 70.00779233799262613 ) ) ;
#529=CARTESIAN_POINT ( 'NONE',  ( 40.26954217208371034, -18.71368208888610241, 69.89063713639258424 ) ) ;
#533=CARTESIAN_POINT ( 'NONE',  ( 38.26194895904384197, -16.60384086642191193, 72.51602215082118619 ) ) ;
#539=CARTESIAN_POINT ( 'NONE',  ( 36.11133435605973574, -26.00384086642192116, 70.60699637195608602 ) ) ;
#542=CARTESIAN_POINT ( 'NONE',  ( 38.82593461698262871, -24.91368208888610170, 69.62690120949091011 ) ) ;
#550=CARTESIAN_POINT ( 'NONE',  ( 36.87297107704151244, -11.90384086642190908, 70.26145752964255564 ) ) ;
#557=CARTESIAN_POINT ( 'NONE',  ( 38.63098279924290068, -0.7038408664219106825, 72.53360434286905445 ) ) ;
#566=CARTESIAN_POINT ( 'NONE',  ( 37.60469502381300089, -7.213682088886102406, 70.49320253461759478 ) ) ;
#567=CARTESIAN_POINT ( 'NONE',  ( 39.24876120206128860, -4.713682088886099741, 70.63227792289247020 ) ) ;
#573=CARTESIAN_POINT ( 'NONE',  ( 37.25202387243754032, -12.40384086642191619, 72.75271321436731853 ) ) ;
#587=CARTESIAN_POINT ( 'NONE',  ( 37.25202387243752611, -7.213682088886102406, 70.00779233799264034 ) ) ;
#589=CARTESIAN_POINT ( 'NONE',  ( 39.93978280207628018, -29.10876147765328525, 71.30174507665321926 ) ) ;
#591=CARTESIAN_POINT ( 'NONE',  ( 37.25202387243752611, -27.21368208888610241, 70.00779233799262613 ) ) ;
#602=CARTESIAN_POINT ( 'NONE',  ( 36.98690846071097127, -1.803840866421911215, 69.45876917294177133 ) ) ;
#603=CARTESIAN_POINT ( 'NONE',  ( 38.37017380507020192, -26.01368208888610312, 72.51602215082114355 ) ) ;
#607=CARTESIAN_POINT ( 'NONE',  ( 37.25202387243752611, -9.213682088886100630, 70.00779233799264034 ) ) ;
#608=CARTESIAN_POINT ( 'NONE',  ( 38.26194895904384907, -28.60384086642191548, 73.11602215082115208 ) ) ;
#610=CARTESIAN_POINT ( 'NONE',  ( 40.33642880535524000, -10.31368208888610738, 72.77780686321128201 ) ) ;
#622=CARTESIAN_POINT ( 'NONE',  ( 36.29569395875881099, -22.30384086642192187, 72.77780686321128201 ) ) ;
#624=CARTESIAN_POINT ( 'NONE',  ( 38.82593461698262871, -28.91368208888610525, 69.62690120949091011 ) ) ;
#632=CARTESIAN_POINT ( 'NONE',  ( 39.73277004305197124, -3.403840866421911748, 69.52238214136768590 ) ) ;
#635=CARTESIAN_POINT ( 'NONE',  ( 40.14115730948191185, -10.51368208888609956, 71.32335560751961623 ) ) ;
#637=CARTESIAN_POINT ( 'NONE',  ( 37.25202387243752611, -19.21368208888610241, 70.00779233799262613 ) ) ;
#640=CARTESIAN_POINT ( 'NONE',  ( 37.25260217561390874, -24.00384086642191761, 70.97781676520601479 ) ) ;
#641=CARTESIAN_POINT ( 'NONE',  ( 39.75915168707250302, -10.71368208888609885, 70.26145752964252722 ) ) ;
#647=CARTESIAN_POINT ( 'NONE',  ( 39.98359781491296161, -9.203840866421911571, 70.89533451361947414 ) ) ;
#651=CARTESIAN_POINT ( 'NONE',  ( 36.68196826583682935, -3.613682088886103205, 71.96809898377890136 ) ) ;
#653=CARTESIAN_POINT ( 'NONE',  ( 40.55423172469004811, -16.41368208888610525, 72.05058123536544201 ) ) ;
#657=CARTESIAN_POINT ( 'NONE',  ( 38.63098279924290068, -18.70384086642191335, 72.53360434286904024 ) ) ;
#662=CARTESIAN_POINT ( 'NONE',  ( 39.73277004305197124, -21.40384086642191619, 69.52238214136768590 ) ) ;
#664=CARTESIAN_POINT ( 'NONE',  ( 38.37017380507020192, -26.01368208888611022, 73.11602215082115208 ) ) ;
#671=CARTESIAN_POINT ( 'NONE',  ( 37.25202387243754032, -16.40384086642191619, 72.75271321436731853 ) ) ;
#677=CARTESIAN_POINT ( 'NONE',  ( 39.95015449827720744, -29.00384086642191406, 71.96809898377885872 ) ) ;
#680=CARTESIAN_POINT ( 'NONE',  ( 38.93415946300897446, -24.11368208888610454, 73.09843995877328382 ) ) ;
#686=CARTESIAN_POINT ( 'NONE',  ( 37.25260217561390874, -5.613682088886101873, 71.78268878715394408 ) ) ;
#687=CARTESIAN_POINT ( 'NONE',  ( 37.38336156205274818, -3.713682088886102406, 72.12822762946751709 ) ) ;
#694=CARTESIAN_POINT ( 'NONE',  ( 36.80608444377001831, -12.30384086642191299, 72.40698646996135324 ) ) ;
#705=CARTESIAN_POINT ( 'NONE',  ( 37.25202387243752611, -5.213682088886100630, 70.00779233799264034 ) ) ;
#720=CARTESIAN_POINT ( 'NONE',  ( 40.52078840805428683, -26.61368208888610809, 70.60699637195608602 ) ) ;
#722=CARTESIAN_POINT ( 'NONE',  ( 38.26194895904383486, -25.01368208888610312, 70.24448340153875847 ) ) ;
#726=CARTESIAN_POINT ( 'NONE',  ( 39.95015449827720744, -4.613682088886104538, 70.79240656858107172 ) ) ;
#727=CARTESIAN_POINT ( 'NONE',  ( 39.38009889167648936, -27.40384086642190908, 70.00779233799262613 ) ) ;
#730=CARTESIAN_POINT ( 'NONE',  ( 37.50301148336529167, -7.113682088886103649, 69.06206559358666652 ) ) ;
#747=CARTESIAN_POINT ( 'NONE',  ( 39.12911128074872380, -15.50384086642191228, 69.06206559358665231 ) ) ;
#751=CARTESIAN_POINT ( 'NONE',  ( 39.82603832034400426, -28.31368208888610027, 72.40698646996131060 ) ) ;
#759=CARTESIAN_POINT ( 'NONE',  ( 36.89935272106204422, -27.21368208888609885, 69.52238214136765748 ) ) ;
#762=CARTESIAN_POINT ( 'NONE',  ( 38.26194895904383486, -3.013682088886100008, 69.64448340153879258 ) ) ;
#764=CARTESIAN_POINT ( 'NONE',  ( 37.80618814713140097, -21.91368208888611235, 73.13360434286903455 ) ) ;
#770=CARTESIAN_POINT ( 'NONE',  ( 37.12184278917507640, -26.10384086642191193, 71.32335560751960202 ) ) ;
#771=CARTESIAN_POINT ( 'NONE',  ( 36.49096545463212493, -13.51368208888610489, 71.43714994484034264 ) ) ;
#775=CARTESIAN_POINT ( 'NONE',  ( 39.82603832034400426, -5.303840866421906775, 70.35351908239857721 ) ) ;
#777=CARTESIAN_POINT ( 'NONE',  ( 37.33957961208646736, -3.813682088886109156, 72.81632618279323310 ) ) ;
#779=CARTESIAN_POINT ( 'NONE',  ( 40.77203464402485622, -18.51368208888610312, 71.32335560751960202 ) ) ;
#783=CARTESIAN_POINT ( 'NONE',  ( 39.41296390513587511, -11.20384086642191335, 71.08074471024443142 ) ) ;
#790=CARTESIAN_POINT ( 'NONE',  ( 39.73277004305197124, -19.40384086642191264, 69.52238214136768590 ) ) ;
#793=CARTESIAN_POINT ( 'NONE',  ( 37.33957961208646736, -27.81368208888611093, 72.81632618279320468 ) ) ;
#803=CARTESIAN_POINT ( 'NONE',  ( 38.26194895904384907, -14.60384086642191548, 73.11602215082116629 ) ) ;
#808=CARTESIAN_POINT ( 'NONE',  ( 38.00113996487112189, 0.2961591335780902612, 70.22690120949094705 ) ) ;
#813=CARTESIAN_POINT ( 'NONE',  ( 39.82603832034400426, -26.31368208888611093, 72.40698646996131060 ) ) ;
#819=CARTESIAN_POINT ( 'NONE',  ( 38.26194895904384197, -28.60384086642191193, 72.51602215082114355 ) ) ;
#820=CARTESIAN_POINT ( 'NONE',  ( 38.73920764526925353, 1.886317911113897905, 72.49843995877333214 ) ) ;
#825=CARTESIAN_POINT ( 'NONE',  ( 37.33957961208645315, -13.80384086642190766, 69.94417936956672577 ) ) ;
#832=CARTESIAN_POINT ( 'NONE',  ( 36.68196826583682935, -7.613682088886103649, 71.96809898377890136 ) ) ;
#844=CARTESIAN_POINT ( 'NONE',  ( 36.07789103942398867, -27.41368208888610525, 70.70992431699450265 ) ) ;
#845=CARTESIAN_POINT ( 'NONE',  ( 39.51027997493896748, -16.51368208888610312, 71.32335560751960202 ) ) ;
#850=CARTESIAN_POINT ( 'NONE',  ( 40.14115730948191185, -4.513682088886103116, 71.32335560751961623 ) ) ;
#851=CARTESIAN_POINT ( 'NONE',  ( 39.51027997493896748, -1.103840866421911704, 71.43714994484034264 ) ) ;
#854=CARTESIAN_POINT ( 'NONE',  ( 36.98690846071097837, -5.813682088886107380, 73.30173637941818754 ) ) ;
#869=ORIENTED_EDGE ( 'NONE', *, *, #6116, .T. ) ;
#870=CARTESIAN_POINT ( 'NONE',  ( 40.26954217208372455, -18.90384086642191619, 72.86986841596734621 ) ) ;
#871=CARTESIAN_POINT ( 'NONE',  ( 39.75915168707250302, -18.71368208888610241, 70.26145752964251301 ) ) ;
#876=PLANE ( 'NONE',  #7170 ) ;
#877=CARTESIAN_POINT ( 'NONE',  ( 40.26954217208371034, -28.71368208888610241, 69.89063713639254161 ) ) ;
#884=CARTESIAN_POINT ( 'NONE',  ( 40.14115730948191185, 1.486317911113896884, 71.32335560751963044 ) ) ;
#888=CARTESIAN_POINT ( 'NONE',  ( 36.87297107704153376, -17.71368208888610951, 72.49904802271740323 ) ) ;
#894=CARTESIAN_POINT ( 'NONE',  ( 39.41296390513587511, -17.20384086642191335, 71.08074471024441721 ) ) ;
#895=CARTESIAN_POINT ( 'NONE',  ( 38.37017380507020192, -4.013682088886107557, 73.11602215082118050 ) ) ;
#902=CARTESIAN_POINT ( 'NONE',  ( 38.26194895904384907, -4.603840866421914590, 73.11602215082118050 ) ) ;
#905=CARTESIAN_POINT ( 'NONE',  ( 36.49096545463212493, -3.513682088886103116, 71.43714994484035685 ) ) ;
#907=CARTESIAN_POINT ( 'NONE',  ( 37.50301148336529167, -9.113682088886102761, 69.06206559358666652 ) ) ;
#910=CARTESIAN_POINT ( 'NONE',  ( 39.51027997493896748, -13.10384086642191015, 71.43714994484032843 ) ) ;
#917=CARTESIAN_POINT ( 'NONE',  ( 35.86008812008917346, -14.10384086642191548, 71.32335560751961623 ) ) ;
#920=CARTESIAN_POINT ( 'NONE',  ( 38.37017380507020192, -20.01368208888610667, 73.11602215082116629 ) ) ;
#929=CARTESIAN_POINT ( 'NONE',  ( 38.82593461698264292, -14.70384086642191690, 73.13360434286903455 ) ) ;
#935=CARTESIAN_POINT ( 'NONE',  ( 39.38009889167648936, -25.40384086642190908, 70.00779233799262613 ) ) ;
#939=CARTESIAN_POINT ( 'NONE',  ( 38.82593461698262871, -22.91368208888609459, 69.62690120949091011 ) ) ;
#945=CARTESIAN_POINT ( 'NONE',  ( 37.31647492878122563, 0.6863179111138985045, 70.72433947564853440 ) ) ;
#946=CARTESIAN_POINT ( 'NONE',  ( 39.31564783533279694, -29.30384086642190766, 70.72433947564850598 ) ) ;
#954=CARTESIAN_POINT ( 'NONE',  ( 39.38009889167648936, -3.403840866421908196, 70.00779233799264034 ) ) ;
#962=CARTESIAN_POINT ( 'NONE',  ( 38.26194895904383486, -1.013682088886101784, 69.64448340153879258 ) ) ;
#980=CARTESIAN_POINT ( 'NONE',  ( 37.60469502381300089, -15.21368208888610063, 70.49320253461759478 ) ) ;
#984=CARTESIAN_POINT ( 'NONE',  ( 39.29254315202756231, -2.813682088886101162, 69.94417936956673998 ) ) ;
#985=CARTESIAN_POINT ( 'NONE',  ( 39.38009889167648936, -21.40384086642190553, 70.00779233799262613 ) ) ;
#990=CARTESIAN_POINT ( 'NONE',  ( 39.64521430340304420, -10.81368208888610027, 69.45876917294177133 ) ) ;
#997=PRODUCT_DEFINITION_FORMATION_WITH_SPECIFIED_SOURCE ( 'ANY', '', #19806, .NOT_KNOWN. ) ;
#1008=CARTESIAN_POINT ( 'NONE',  ( 38.26194895904384197, -16.60384086642191548, 73.71602215082113219 ) ) ;
#1009=CARTESIAN_POINT ( 'NONE',  ( 36.87297107704152666, -21.71368208888610951, 72.49904802271740323 ) ) ;
#1015=CARTESIAN_POINT ( 'NONE',  ( 36.36258059203031934, -25.71368208888611306, 72.86986841596734621 ) ) ;
#1020=CARTESIAN_POINT ( 'NONE',  ( 39.98359781491296161, -2.413682088886103472, 71.86517103874048473 ) ) ;
#1023=CARTESIAN_POINT ( 'NONE',  ( 38.93415946300898867, -22.11368208888610454, 73.09843995877329803 ) ) ;
#1026=CARTESIAN_POINT ( 'NONE',  ( 38.37017380507018771, -17.60384086642191193, 70.24448340153875847 ) ) ;
#1027=CARTESIAN_POINT ( 'NONE',  ( 38.93415946300897446, -6.113682088886107202, 73.09843995877331224 ) ) ;
#1031=CARTESIAN_POINT ( 'NONE',  ( 36.68196826583682935, -4.003840866421911393, 70.79240656858108593 ) ) ;
#1035=CARTESIAN_POINT ( 'NONE',  ( 39.95015449827720744, -8.613682088886104538, 70.79240656858107172 ) ) ;
#1037=CARTESIAN_POINT ( 'NONE',  ( 35.86008812008917346, -9.513682088886103116, 71.43714994484035685 ) ) ;
#1041=CARTESIAN_POINT ( 'NONE',  ( 39.37952058850012804, -13.00384086642191228, 71.78268878715390144 ) ) ;
#1048=CARTESIAN_POINT ( 'NONE',  ( 36.36258059203030513, -17.90384086642190908, 69.89063713639259845 ) ) ;
#1051=CARTESIAN_POINT ( 'NONE',  ( 39.98359781491296161, -20.41368208888610525, 71.86517103874047052 ) ) ;
#1058=CARTESIAN_POINT ( 'NONE',  ( 40.14115730948191185, -15.10384086642191015, 71.43714994484031422 ) ) ;
#1061=CARTESIAN_POINT ( 'NONE',  ( 36.87297107704152666, -27.71368208888610241, 72.49904802271738902 ) ) ;
#1063=CARTESIAN_POINT ( 'NONE',  ( 39.38009889167648936, -27.40384086642190908, 70.00779233799262613 ) ) ;
#1065=CARTESIAN_POINT ( 'NONE',  ( 39.75915168707250302, -22.71368208888610241, 70.26145752964251301 ) ) ;
#1070=CARTESIAN_POINT ( 'NONE',  ( 38.26194895904383486, -1.013682088886101784, 70.24448340153877268 ) ) ;
#1073=CARTESIAN_POINT ( 'NONE',  ( 37.60469502381300089, -1.213682088886100630, 70.49320253461759478 ) ) ;
#1079=CARTESIAN_POINT ( 'NONE',  ( 37.80618814713138676, -5.703840866421908018, 69.62690120949091011 ) ) ;
#1087=CARTESIAN_POINT ( 'NONE',  ( 36.64852494920107517, -1.413682088886102806, 70.89533451361948835 ) ) ;
#1104=CARTESIAN_POINT ( 'NONE',  ( 38.26194895904383486, -17.01368208888610312, 70.24448340153875847 ) ) ;
#1109=CARTESIAN_POINT ( 'NONE',  ( 39.95015449827720744, -0.6136820888861040935, 70.79240656858107172 ) ) ;
#1110=CARTESIAN_POINT ( 'NONE',  ( 36.87297107704149823, -23.90384086642190198, 70.26145752964251301 ) ) ;
#1112=CARTESIAN_POINT ( 'NONE',  ( 39.73277004305198545, -8.213682088886105959, 73.23812341099225875 ) ) ;
#1131=CARTESIAN_POINT ( 'NONE',  ( 39.64521430340305841, -16.80384086642191832, 73.30173637941818754 ) ) ;
#1133=CARTESIAN_POINT ( 'NONE',  ( 37.33957961208646736, -21.81368208888610738, 72.81632618279321889 ) ) ;
#1141=CARTESIAN_POINT ( 'NONE',  ( 39.73277004305198545, -28.21368208888611306, 73.23812341099225875 ) ) ;
#1145=CARTESIAN_POINT ( 'NONE',  ( 39.75915168707250302, 1.286317911113898260, 70.26145752964255564 ) ) ;
#1148=CARTESIAN_POINT ( 'NONE',  ( 36.64852494920107517, -19.41368208888610525, 70.89533451361947414 ) ) ;
#1151=CARTESIAN_POINT ( 'NONE',  ( 37.60469502381300799, -20.40384086642191264, 72.26730301774234988 ) ) ;
#1152=CARTESIAN_POINT ( 'NONE',  ( 39.29254315202756231, -4.813682088886099386, 69.94417936956673998 ) ) ;
#1158=CARTESIAN_POINT ( 'NONE',  ( 40.14115730948191185, -5.103840866421909261, 71.43714994484034264 ) ) ;
#1161=CARTESIAN_POINT ( 'NONE',  ( 39.98359781491296161, -6.413682088886103472, 71.86517103874048473 ) ) ;
#1163=CARTESIAN_POINT ( 'NONE',  ( 39.02088643472237095, -6.913682088886101695, 69.02690120949094421 ) ) ;
#1166=CARTESIAN_POINT ( 'NONE',  ( 39.31564783533279694, -11.30384086642191299, 70.72433947564853440 ) ) ;
#1172=CARTESIAN_POINT ( 'NONE',  ( 39.12911128074872380, -17.50384086642191406, 69.06206559358665231 ) ) ;
#1177=CARTESIAN_POINT ( 'NONE',  ( 38.93415946300897446, -20.11368208888610809, 73.09843995877329803 ) ) ;
#1186=CARTESIAN_POINT ( 'NONE',  ( 38.82593461698264292, -6.703840866421915123, 73.13360434286904876 ) ) ;
#1190=CARTESIAN_POINT ( 'NONE',  ( 39.98359781491296161, -22.41368208888610525, 71.86517103874047052 ) ) ;
#1193=CARTESIAN_POINT ( 'NONE',  ( 36.80608444377001831, -22.30384086642191477, 72.40698646996135324 ) ) ;
#1197=CARTESIAN_POINT ( 'NONE',  ( 39.75915168707250302, -24.71368208888610241, 70.26145752964249880 ) ) ;
#1202=CARTESIAN_POINT ( 'NONE',  ( 39.41296390513587511, -0.4136820888861019174, 71.67976084211552745 ) ) ;
#1209=CARTESIAN_POINT ( 'NONE',  ( 36.64852494920107517, -2.203840866421912015, 71.86517103874049894 ) ) ;
#1220=CARTESIAN_POINT ( 'NONE',  ( 37.80618814713140097, -3.913682088886108357, 73.13360434286904876 ) ) ;
#1243=CARTESIAN_POINT ( 'NONE',  ( 39.41296390513587511, -18.41368208888610170, 71.67976084211551324 ) ) ;
#1247=CARTESIAN_POINT ( 'NONE',  ( 39.95015449827720744, -2.613682088886105870, 70.79240656858107172 ) ) ;
#1248=CARTESIAN_POINT ( 'NONE',  ( 39.75915168707251723, -20.90384086642190553, 72.49904802271738902 ) ) ;
#1252=CARTESIAN_POINT ( 'NONE',  ( 36.98690846071097837, -3.813682088886109156, 73.30173637941818754 ) ) ;
#1270=CARTESIAN_POINT ( 'NONE',  ( 35.86008812008917346, -18.10384086642191548, 71.32335560751961623 ) ) ;
#1272=CARTESIAN_POINT ( 'NONE',  ( 39.98359781491296161, -18.41368208888610880, 71.86517103874047052 ) ) ;
#1279=CARTESIAN_POINT ( 'NONE',  ( 37.61123632939164452, 0.2961591335780902612, 69.02690120949095842 ) ) ;
#1282=CARTESIAN_POINT ( 'NONE',  ( 39.82603832034400426, -2.313682088886107380, 72.40698646996135324 ) ) ;
#1284=CARTESIAN_POINT ( 'NONE',  ( 36.87297107704153376, -15.71368208888610596, 72.49904802271740323 ) ) ;
#1288=CARTESIAN_POINT ( 'NONE',  ( 37.12184278917507640, -20.10384086642191193, 71.32335560751961623 ) ) ;
#1289=CARTESIAN_POINT ( 'NONE',  ( 39.82603832034400426, -6.313682088886107380, 72.40698646996135324 ) ) ;
#1293=CARTESIAN_POINT ( 'NONE',  ( 36.87297107704149823, -7.903840866421908196, 70.26145752964255564 ) ) ;
#1295=CARTESIAN_POINT ( 'NONE',  ( 39.31564783533280405, -28.31368208888610383, 72.03616607671136762 ) ) ;
#1297=CARTESIAN_POINT ( 'NONE',  ( 37.61123632939165873, -9.913682088886107024, 73.73360434286902887 ) ) ;
#1301=CARTESIAN_POINT ( 'NONE',  ( 39.51027997493896748, -9.103840866421911926, 71.43714994484034264 ) ) ;
#1307=CARTESIAN_POINT ( 'NONE',  ( 36.89935272106205133, -14.40384086642191974, 73.23812341099225875 ) ) ;
#1310=CARTESIAN_POINT ( 'NONE',  ( 37.33957961208646736, -21.81368208888610738, 72.81632618279321889 ) ) ;
#1318=CARTESIAN_POINT ( 'NONE',  ( 37.33957961208645315, -7.803840866421909439, 69.94417936956673998 ) ) ;
#1322=CARTESIAN_POINT ( 'NONE',  ( 36.64852494920107517, -27.41368208888610525, 70.89533451361945993 ) ) ;
#1325=CARTESIAN_POINT ( 'NONE',  ( 37.80618814713138676, -21.70384086642190979, 69.62690120949091011 ) ) ;
#1328=CARTESIAN_POINT ( 'NONE',  ( 39.95015449827720744, -18.61368208888610454, 70.79240656858105751 ) ) ;
#1330=CARTESIAN_POINT ( 'NONE',  ( 39.02088643472237095, -26.91368208888610170, 69.02690120949091579 ) ) ;
#1334=CARTESIAN_POINT ( 'NONE',  ( 39.37952058850012804, 1.386317911113897683, 70.97781676520604321 ) ) ;
#1341=CARTESIAN_POINT ( 'NONE',  ( 39.38009889167648936, -7.403840866421908196, 70.00779233799264034 ) ) ;
#1349=CARTESIAN_POINT ( 'NONE',  ( 39.75915168707250302, -0.7136820888860999634, 70.26145752964255564 ) ) ;
#1369=CARTESIAN_POINT ( 'NONE',  ( 37.12184278917507640, -15.51368208888610312, 71.43714994484034264 ) ) ;
#1375=CARTESIAN_POINT ( 'NONE',  ( 36.49096545463212493, -24.10384086642190482, 71.32335560751960202 ) ) ;
#1380=CARTESIAN_POINT ( 'NONE',  ( 38.37017380507020192, -4.013682088886107557, 73.71602215082116061 ) ) ;
#1400=CARTESIAN_POINT ( 'NONE',  ( 36.98690846071097127, -11.80384086642191477, 69.45876917294175712 ) ) ;
#1403=CARTESIAN_POINT ( 'NONE',  ( 38.82593461698262871, -18.91368208888609459, 69.62690120949091011 ) ) ;
#1407=CARTESIAN_POINT ( 'NONE',  ( 40.33642880535524000, -22.31368208888610738, 72.77780686321126780 ) ) ;
#1417=CARTESIAN_POINT ( 'NONE',  ( 37.38336156205273397, -21.90384086642191619, 70.63227792289247020 ) ) ;
#1418=CARTESIAN_POINT ( 'NONE',  ( 37.80618814713140097, -7.913682088886107913, 73.13360434286904876 ) ) ;
#1425=CARTESIAN_POINT ( 'NONE',  ( 39.12911128074872380, -29.50384086642191050, 69.06206559358663810 ) ) ;
#1427=CARTESIAN_POINT ( 'NONE',  ( 39.82603832034400426, -0.3136820888861094336, 72.40698646996135324 ) ) ;
#1428=CARTESIAN_POINT ( 'NONE',  ( 39.73277004305198545, -6.213682088886108623, 73.23812341099225875 ) ) ;
#1432=CARTESIAN_POINT ( 'NONE',  ( 38.63098279924290068, -4.703840866421909794, 72.53360434286905445 ) ) ;
#1437=CARTESIAN_POINT ( 'NONE',  ( 38.37017380507018771, -7.603840866421910150, 69.04448340153881247 ) ) ;
#1440=CARTESIAN_POINT ( 'NONE',  ( 36.64852494920107517, -23.41368208888610525, 70.89533451361945993 ) ) ;
#1446=CARTESIAN_POINT ( 'NONE',  ( 36.87297107704151244, -9.903840866421905531, 70.26145752964255564 ) ) ;
#1450=CARTESIAN_POINT ( 'NONE',  ( 39.38009889167650357, -22.21368208888610951, 72.75271321436731853 ) ) ;
#1454=CARTESIAN_POINT ( 'NONE',  ( 39.38009889167648936, -21.40384086642190553, 70.00779233799262613 ) ) ;
#1456=CARTESIAN_POINT ( 'NONE',  ( 36.68196826583682935, -15.61368208888610454, 71.96809898377888715 ) ) ;
#1458=CARTESIAN_POINT ( 'NONE',  ( 36.11133435605973574, -0.003840866421914862494, 70.60699637195612866 ) ) ;
#1462=CARTESIAN_POINT ( 'NONE',  ( 39.51027997493896748, -25.10384086642191193, 71.43714994484031422 ) ) ;
#1470=CARTESIAN_POINT ( 'NONE',  ( 36.87297107704149823, -1.903840866421906419, 70.26145752964255564 ) ) ;
#1475=CARTESIAN_POINT ( 'NONE',  ( 38.26194895904383486, -3.013682088886100008, 69.64448340153879258 ) ) ;
#1476=CARTESIAN_POINT ( 'NONE',  ( 38.37017380507018771, -27.60384086642191193, 69.64448340153876416 ) ) ;
#1481=CARTESIAN_POINT ( 'NONE',  ( 37.21915885897815457, -15.41368208888610347, 71.08074471024443142 ) ) ;
#1488=CARTESIAN_POINT ( 'NONE',  ( 37.25260217561390874, -11.61368208888610098, 71.78268878715392987 ) ) ;
#1494=CARTESIAN_POINT ( 'NONE',  ( 37.25202387243754032, -22.40384086642191619, 72.75271321436731853 ) ) ;
#1512=CARTESIAN_POINT ( 'NONE',  ( 36.98690846071097127, -13.80384086642191122, 69.45876917294175712 ) ) ;
#1515=CARTESIAN_POINT ( 'NONE',  ( 39.82603832034400426, -12.31368208888610560, 72.40698646996133903 ) ) ;
#1519=CARTESIAN_POINT ( 'NONE',  ( 37.50301148336529167, -23.11368208888610454, 69.06206559358663810 ) ) ;
#1529=CARTESIAN_POINT ( 'NONE',  ( 38.93987200065210175, -10.80384086642191299, 72.33091598616827866 ) ) ;
#1530=CARTESIAN_POINT ( 'NONE',  ( 39.38009889167650357, -0.2136820888861065693, 72.75271321436733274 ) ) ;
#1538=CARTESIAN_POINT ( 'NONE',  ( 36.07789103942399578, -28.20384086642191690, 72.05058123536544201 ) ) ;
#1541=CARTESIAN_POINT ( 'NONE',  ( 39.02742774030102879, -28.21368208888610596, 72.26730301774232146 ) ) ;
#1542=CARTESIAN_POINT ( 'NONE',  ( 40.33642880535524000, -2.313682088886106936, 72.77780686321128201 ) ) ;
#1545=CARTESIAN_POINT ( 'NONE',  ( 38.73920764526923932, -3.503840866421911393, 70.26206559358664094 ) ) ;
#1550=CARTESIAN_POINT ( 'NONE',  ( 38.37017380507018771, -11.60384086642191015, 69.04448340153881247 ) ) ;
#1553=CARTESIAN_POINT ( 'NONE',  ( 38.37017380507020192, -16.01368208888610667, 73.11602215082116629 ) ) ;
#1561=CARTESIAN_POINT ( 'NONE',  ( 38.82593461698264292, -10.70384086642191690, 73.13360434286904876 ) ) ;
#1564=CARTESIAN_POINT ( 'NONE',  ( 36.87297107704152666, -15.71368208888610596, 72.49904802271740323 ) ) ;
#1566=CARTESIAN_POINT ( 'NONE',  ( 39.82603832034400426, -21.30384086642191122, 70.35351908239857721 ) ) ;
#1568=CARTESIAN_POINT ( 'NONE',  ( 37.80618814713140097, -19.91368208888610170, 73.13360434286903455 ) ) ;
#1570=CARTESIAN_POINT ( 'NONE',  ( 36.11133435605973574, -23.61368208888610098, 72.15350918040381600 ) ) ;
#1574=CARTESIAN_POINT ( 'NONE',  ( 37.25260217561390874, -22.00384086642191406, 70.97781676520601479 ) ) ;
#1581=CARTESIAN_POINT ( 'NONE',  ( 38.26194895904384197, -26.60384086642191903, 73.71602215082113219 ) ) ;
#1593=CARTESIAN_POINT ( 'NONE',  ( 36.49096545463212493, -26.10384086642190837, 71.32335560751960202 ) ) ;
#1601=CARTESIAN_POINT ( 'NONE',  ( 39.31564783533279694, -7.303840866421912104, 70.72433947564853440 ) ) ;
#1609=CARTESIAN_POINT ( 'NONE',  ( 37.60469502381300089, -15.21368208888610063, 70.49320253461759478 ) ) ;
#1610=CARTESIAN_POINT ( 'NONE',  ( 37.31647492878122563, -13.31368208888610205, 70.72433947564853440 ) ) ;
#1616=CARTESIAN_POINT ( 'NONE',  ( 37.33957961208645315, -17.80384086642190766, 69.94417936956672577 ) ) ;
#1618=CARTESIAN_POINT ( 'NONE',  ( 37.69225076346193504, -15.81368208888610205, 72.33091598616826445 ) ) ;
#1634=CARTESIAN_POINT ( 'NONE',  ( 37.50301148336529877, -8.503840866421917610, 73.69843995877330656 ) ) ;
#1637=CARTESIAN_POINT ( 'NONE',  ( 37.80618814713140097, -11.91368208888611058, 73.13360434286903455 ) ) ;
#1642=CARTESIAN_POINT ( 'NONE',  ( 36.29569395875879678, -19.31368208888610027, 69.98269868914867686 ) ) ;
#1653=CARTESIAN_POINT ( 'NONE',  ( 37.69225076346193504, -11.80384086642191477, 70.42958956619168021 ) ) ;
#1654=CARTESIAN_POINT ( 'NONE',  ( 38.93415946300897446, -2.113682088886109423, 73.09843995877331224 ) ) ;
#1660=CARTESIAN_POINT ( 'NONE',  ( 38.37017380507018771, 0.3961591335780931256, 69.64448340153880679 ) ) ;
#1661=CARTESIAN_POINT ( 'NONE',  ( 39.29254315202756231, 1.186317911113898838, 69.94417936956675419 ) ) ;
#1663=CARTESIAN_POINT ( 'NONE',  ( 39.64521430340304420, -0.8136820888860993861, 69.45876917294177133 ) ) ;
#1666=CARTESIAN_POINT ( 'NONE',  ( 37.25260217561390874, -8.003840866421910505, 70.97781676520604321 ) ) ;
#1673=CARTESIAN_POINT ( 'NONE',  ( 37.50301148336529877, -8.503840866421917610, 73.69843995877330656 ) ) ;
#1679=CARTESIAN_POINT ( 'NONE',  ( 38.37017380507020192, -12.01368208888610845, 73.11602215082116629 ) ) ;
#1684=CARTESIAN_POINT ( 'NONE',  ( 37.80618814713138676, -7.703840866421908906, 69.62690120949091011 ) ) ;
#1688=CARTESIAN_POINT ( 'NONE',  ( 39.75915168707250302, -20.71368208888610596, 70.26145752964251301 ) ) ;
#1690=CARTESIAN_POINT ( 'NONE',  ( 39.75915168707251723, -16.90384086642191619, 72.49904802271738902 ) ) ;
#1694=CARTESIAN_POINT ( 'NONE',  ( 40.14115730948191185, -20.51368208888609601, 71.32335560751960202 ) ) ;
#1696=CARTESIAN_POINT ( 'NONE',  ( 39.02088643472237095, -22.91368208888609814, 69.02690120949091579 ) ) ;
#1700=CARTESIAN_POINT ( 'NONE',  ( 37.21915885897815457, -22.20384086642191335, 71.67976084211552745 ) ) ;
#1707=CARTESIAN_POINT ( 'NONE',  ( 37.33957961208645315, 0.1961591335780908663, 69.94417936956673998 ) ) ;
#1717=CARTESIAN_POINT ( 'NONE',  ( 36.80608444377002542, -28.30384086642191122, 72.40698646996131060 ) ) ;
#1723=CARTESIAN_POINT ( 'NONE',  ( 37.31647492878124694, -6.303840866421912104, 72.03616607671141026 ) ) ;
#1732=CARTESIAN_POINT ( 'NONE',  ( 38.93987200065208754, -10.81368208888610027, 70.42958956619168021 ) ) ;
#1733=CARTESIAN_POINT ( 'NONE',  ( 39.02742774030102879, -8.213682088886098853, 72.26730301774236409 ) ) ;
#1741=CARTESIAN_POINT ( 'NONE',  ( 40.14115730948191185, -19.10384086642191193, 71.43714994484030001 ) ) ;
#1745=CARTESIAN_POINT ( 'NONE',  ( 39.37952058850012804, -20.61368208888610098, 70.97781676520601479 ) ) ;
#1748=CARTESIAN_POINT ( 'NONE',  ( 36.49096545463212493, -15.51368208888610667, 71.43714994484034264 ) ) ;
#1765=CARTESIAN_POINT ( 'NONE',  ( 36.98690846071097127, -7.803840866421912104, 69.45876917294177133 ) ) ;
#1769=CARTESIAN_POINT ( 'NONE',  ( 36.80608444377001121, -13.31368208888609672, 70.35351908239857721 ) ) ;
#1777=CARTESIAN_POINT ( 'NONE',  ( 38.37017380507020192, -22.01368208888611022, 73.71602215082113219 ) ) ;
#1787=CARTESIAN_POINT ( 'NONE',  ( 37.21915885897815457, -12.20384086642191157, 71.67976084211552745 ) ) ;
#1788=CARTESIAN_POINT ( 'NONE',  ( 37.69796330110504101, 0.8863179111139003474, 69.66206559358664663 ) ) ;
#1795=CARTESIAN_POINT ( 'NONE',  ( 39.95015449827720744, -1.003840866421912281, 71.96809898377888715 ) ) ;
#1796=CARTESIAN_POINT ( 'NONE',  ( 39.38009889167650357, -0.2136820888861065693, 72.75271321436733274 ) ) ;
#1797=CARTESIAN_POINT ( 'NONE',  ( 39.12911128074873801, -4.113682088886107202, 73.69843995877330656 ) ) ;
#1800=CARTESIAN_POINT ( 'NONE',  ( 37.69225076346193504, -3.803840866421912992, 70.42958956619168021 ) ) ;
#1806=CARTESIAN_POINT ( 'NONE',  ( 37.50301148336529877, -12.50384086642191939, 73.69843995877327814 ) ) ;
#1811=CARTESIAN_POINT ( 'NONE',  ( 37.69796330110504101, -11.11368208888610276, 69.66206559358663242 ) ) ;
#1817=CARTESIAN_POINT ( 'NONE',  ( 37.33957961208645315, -3.803840866421909439, 69.94417936956673998 ) ) ;
#1821=CARTESIAN_POINT ( 'NONE',  ( 38.37017380507020192, -18.01368208888611022, 73.11602215082116629 ) ) ;
#1825=CARTESIAN_POINT ( 'NONE',  ( 39.38009889167648936, -15.40384086642190908, 70.00779233799262613 ) ) ;
#1828=CARTESIAN_POINT ( 'NONE',  ( 39.82603832034400426, -16.31368208888610738, 72.40698646996133903 ) ) ;
#1830=CARTESIAN_POINT ( 'NONE',  ( 40.33642880535524000, -22.31368208888610738, 72.77780686321126780 ) ) ;
#1834=CARTESIAN_POINT ( 'NONE',  ( 38.73920764526923932, -23.50384086642191050, 70.26206559358661252 ) ) ;
#1837=CARTESIAN_POINT ( 'NONE',  ( 39.61574158285312564, -28.86380355457609070, 70.74205085096339474 ) ) ;
#1842=CARTESIAN_POINT ( 'NONE',  ( 37.80618814713138676, 0.2961591335780937584, 69.62690120949091011 ) ) ;
#1844=CARTESIAN_POINT ( 'NONE',  ( 39.12911128074873801, -2.113682088886108534, 73.69843995877330656 ) ) ;
#1851=CARTESIAN_POINT ( 'NONE',  ( 36.68196826583682935, -20.00384086642191050, 70.79240656858107172 ) ) ;
#1858=CARTESIAN_POINT ( 'NONE',  ( 38.73920764526923932, -3.503840866421911393, 70.26206559358664094 ) ) ;
#1863=EDGE_LOOP ( 'NONE', ( #8870, #16728, #13570, #6462, #11014 ) ) ;
#1865=CARTESIAN_POINT ( 'NONE',  ( 39.02742774030102879, -12.21368208888610063, 72.26730301774234988 ) ) ;
#1866=CARTESIAN_POINT ( 'NONE',  ( 38.63098279924288647, -8.913682088886103472, 70.22690120949091863 ) ) ;
#1874=CARTESIAN_POINT ( 'NONE',  ( 36.49096545463212493, -16.10384086642191548, 71.32335560751961623 ) ) ;
#1876=CARTESIAN_POINT ( 'NONE',  ( 38.26194895904383486, -17.01368208888610312, 70.24448340153875847 ) ) ;
#1880=CARTESIAN_POINT ( 'NONE',  ( 39.38009889167650357, -12.21368208888610596, 72.75271321436731853 ) ) ;
#1892=CARTESIAN_POINT ( 'NONE',  ( 39.12911128074872380, -9.503840866421912281, 69.06206559358666652 ) ) ;
#1895=CARTESIAN_POINT ( 'NONE',  ( 36.64852494920107517, -15.41368208888610525, 70.89533451361947414 ) ) ;
#1899=CARTESIAN_POINT ( 'NONE',  ( 40.55423172469004811, -18.41368208888610525, 72.05058123536544201 ) ) ;
#1913=CARTESIAN_POINT ( 'NONE',  ( 38.93987200065210175, -12.80384086642190944, 72.33091598616826445 ) ) ;
#1914=CARTESIAN_POINT ( 'NONE',  ( 39.95015449827720744, 1.386317911113894130, 70.79240656858108593 ) ) ;
#1920=CARTESIAN_POINT ( 'NONE',  ( 38.26194895904384197, -28.60384086642191548, 73.71602215082113219 ) ) ;
#1921=CARTESIAN_POINT ( 'NONE',  ( 38.00113996487114321, -23.91368208888610170, 72.53360434286901182 ) ) ;
#1922=CARTESIAN_POINT ( 'NONE',  ( 39.73277004305198545, -4.213682088886105959, 73.23812341099225875 ) ) ;
#1927=CARTESIAN_POINT ( 'NONE',  ( 39.24876120206129571, -6.903840866421912636, 72.12822762946750288 ) ) ;
#1934=CARTESIAN_POINT ( 'NONE',  ( 40.55423172469004101, -11.20384086642191690, 70.70992431699450265 ) ) ;
#1937=CARTESIAN_POINT ( 'NONE',  ( 39.82603832034400426, -12.31368208888610560, 72.40698646996133903 ) ) ;
#1941=CARTESIAN_POINT ( 'NONE',  ( 37.69796330110505522, -0.5038408664219152788, 73.09843995877331224 ) ) ;
#1944=CARTESIAN_POINT ( 'NONE',  ( 37.69796330110504101, -21.11368208888610454, 69.66206559358661821 ) ) ;
#1949=CARTESIAN_POINT ( 'NONE',  ( 37.25202387243754032, -18.40384086642191974, 72.75271321436731853 ) ) ;
#1951=CARTESIAN_POINT ( 'NONE',  ( 37.69796330110504101, -11.11368208888610276, 69.66206559358663242 ) ) ;
#1953=CARTESIAN_POINT ( 'NONE',  ( 38.37017380507020192, -24.01368208888611022, 73.71602215082113219 ) ) ;
#1957=CARTESIAN_POINT ( 'NONE',  ( 38.37017380507018771, -25.60384086642191548, 70.24448340153875847 ) ) ;
#1963=CARTESIAN_POINT ( 'NONE',  ( 39.64521430340305841, -26.80384086642191832, 73.30173637941817333 ) ) ;
#1968=CARTESIAN_POINT ( 'NONE',  ( 36.36258059203031934, -1.713682088886108179, 72.86986841596736042 ) ) ;
#1974=CARTESIAN_POINT ( 'NONE',  ( 37.80618814713138676, -23.70384086642190979, 69.62690120949091011 ) ) ;
#1982=CARTESIAN_POINT ( 'NONE',  ( 38.37017380507018771, -3.603840866421911038, 70.24448340153877268 ) ) ;
#1990=CARTESIAN_POINT ( 'NONE',  ( 38.37017380507020192, -14.01368208888610312, 72.51602215082118619 ) ) ;
#1992=CARTESIAN_POINT ( 'NONE',  ( 37.38336156205274818, -11.71368208888610241, 72.12822762946750288 ) ) ;
#1999=CARTESIAN_POINT ( 'NONE',  ( 38.93415946300896024, -19.50384086642191050, 69.66206559358661821 ) ) ;
#2000=AXIS2_PLACEMENT_3D ( 'NONE', #9286, #12766, #22537 ) ;
#2005=CARTESIAN_POINT ( 'NONE',  ( 37.89291511884476904, -19.11368208888609388, 70.26206559358661252 ) ) ;
#2013=CARTESIAN_POINT ( 'NONE',  ( 38.26194895904383486, -15.01368208888610134, 69.64448340153877837 ) ) ;
#2017=CARTESIAN_POINT ( 'NONE',  ( 39.98359781491296161, -28.41368208888610525, 71.86517103874045631 ) ) ;
#2027=CARTESIAN_POINT ( 'NONE',  ( 39.12911128074872380, -5.503840866421911393, 69.06206559358666652 ) ) ;
#2031=CARTESIAN_POINT ( 'NONE',  ( 36.49096545463212493, -9.513682088886101340, 71.43714994484035685 ) ) ;
#2036=CARTESIAN_POINT ( 'NONE',  ( 36.29569395875879678, -13.31368208888610205, 69.98269868914867686 ) ) ;
#2047=CARTESIAN_POINT ( 'NONE',  ( 38.00113996487112189, -9.703840866421911571, 70.22690120949091863 ) ) ;
#2048=CARTESIAN_POINT ( 'NONE',  ( 37.31647492878122563, -23.31368208888610383, 70.72433947564853440 ) ) ;
#2056=CARTESIAN_POINT ( 'NONE',  ( 37.50301148336529877, -26.50384086642192116, 73.69843995877326392 ) ) ;
#2057=CARTESIAN_POINT ( 'NONE',  ( 39.41296390513587511, -24.41368208888610525, 71.67976084211548482 ) ) ;
#2058=CARTESIAN_POINT ( 'NONE',  ( 40.55423172469004811, -4.413682088886105248, 72.05058123536544201 ) ) ;
#2061=CARTESIAN_POINT ( 'NONE',  ( 39.02742774030101458, 0.5961591335780883627, 70.49320253461762320 ) ) ;
#2065=CARTESIAN_POINT ( 'NONE',  ( 37.61123632939164452, -3.703840866421909794, 69.02690120949094421 ) ) ;
#2068=CARTESIAN_POINT ( 'NONE',  ( 40.14115730948191185, -16.51368208888610667, 71.32335560751960202 ) ) ;
#2071=CARTESIAN_POINT ( 'NONE',  ( 37.25202387243752611, -27.21368208888610241, 70.00779233799262613 ) ) ;
#2074=CARTESIAN_POINT ( 'NONE',  ( 36.49096545463212493, -2.103840866421912370, 71.32335560751963044 ) ) ;
#2076=CARTESIAN_POINT ( 'NONE',  ( 37.69796330110504101, -17.11368208888610098, 69.66206559358661821 ) ) ;
#2079=CARTESIAN_POINT ( 'NONE',  ( 36.64852494920107517, -20.20384086642191335, 71.86517103874048473 ) ) ;
#2083=CARTESIAN_POINT ( 'NONE',  ( 39.38009889167650357, -14.21368208888610773, 72.75271321436731853 ) ) ;
#2085=CARTESIAN_POINT ( 'NONE',  ( 35.86008812008917346, -21.51368208888609956, 71.43714994484034264 ) ) ;
#2090=CARTESIAN_POINT ( 'NONE',  ( 37.21915885897815457, -18.20384086642190979, 71.67976084211552745 ) ) ;
#2096=CARTESIAN_POINT ( 'NONE',  ( 39.73277004305197124, -29.40384086642191264, 69.52238214136765748 ) ) ;
#2097=CARTESIAN_POINT ( 'NONE',  ( 36.11133435605973574, 0.3863179111138967392, 72.15350918040385864 ) ) ;
#2104=CARTESIAN_POINT ( 'NONE',  ( 36.87297107704151244, -19.90384086642190553, 70.26145752964255564 ) ) ;
#2112=CARTESIAN_POINT ( 'NONE',  ( 37.31647492878124694, -8.303840866421912992, 72.03616607671141026 ) ) ;
#2119=CARTESIAN_POINT ( 'NONE',  ( 38.93987200065208754, -2.813682088886101162, 70.42958956619168021 ) ) ;
#2120=CARTESIAN_POINT ( 'NONE',  ( 38.00113996487114321, -3.913682088886100807, 72.53360434286905445 ) ) ;
#2127=CARTESIAN_POINT ( 'NONE',  ( 38.93415946300896024, -15.50384086642190873, 69.66206559358661821 ) ) ;
#2133=CARTESIAN_POINT ( 'NONE',  ( 39.51027997493896748, -20.51368208888610312, 71.32335560751960202 ) ) ;
#2137=CARTESIAN_POINT ( 'NONE',  ( 37.25202387243752611, -13.21368208888610063, 70.00779233799262613 ) ) ;
#2153=CARTESIAN_POINT ( 'NONE',  ( 37.61123632939164452, -3.703840866421909794, 69.02690120949094421 ) ) ;
#2155=EDGE_CURVE ( 'NONE', #25416, #8151, #22591, .T. ) ;
#2159=CARTESIAN_POINT ( 'NONE',  ( 36.68196826583682935, -7.613682088886103649, 71.96809898377890136 ) ) ;
#2164=CARTESIAN_POINT ( 'NONE',  ( 36.89935272106204422, -15.21368208888610063, 69.52238214136768590 ) ) ;
#2175=CARTESIAN_POINT ( 'NONE',  ( 39.24876120206128860, -24.71368208888610241, 70.63227792289242757 ) ) ;
#2183=CARTESIAN_POINT ( 'NONE',  ( 40.52078840805429394, -25.00384086642191761, 72.15350918040381600 ) ) ;
#2186=CARTESIAN_POINT ( 'NONE',  ( 36.49096545463212493, -27.51368208888610312, 71.43714994484030001 ) ) ;
#2188=CARTESIAN_POINT ( 'NONE',  ( 39.31564783533279694, -1.303840866421910105, 70.72433947564853440 ) ) ;
#2195=CARTESIAN_POINT ( 'NONE',  ( 40.52078840805429394, -1.003840866421915612, 72.15350918040385864 ) ) ;
#2198=CARTESIAN_POINT ( 'NONE',  ( 39.75915168707250302, -6.713682088886099741, 70.26145752964252722 ) ) ;
#2200=CARTESIAN_POINT ( 'NONE',  ( 36.64852494920107517, -25.41368208888610525, 70.89533451361945993 ) ) ;
#2205=CARTESIAN_POINT ( 'NONE',  ( 39.95015449827720744, -5.003840866421912281, 71.96809898377888715 ) ) ;
#2208=CARTESIAN_POINT ( 'NONE',  ( 38.73920764526923932, -27.50384086642191406, 70.26206559358661252 ) ) ;
#2209=CARTESIAN_POINT ( 'NONE',  ( 36.68196826583682935, -9.613682088886104538, 71.96809898377890136 ) ) ;
#2211=CARTESIAN_POINT ( 'NONE',  ( 38.82593461698265003, -12.70384086642191512, 73.13360434286903455 ) ) ;
#2213=CARTESIAN_POINT ( 'NONE',  ( 36.49096545463212493, -9.513682088886101340, 71.43714994484035685 ) ) ;
#2215=CARTESIAN_POINT ( 'NONE',  ( 39.02088643472237095, -16.91368208888609814, 69.02690120949091579 ) ) ;
#2221=CARTESIAN_POINT ( 'NONE',  ( 38.26194895904384197, -18.60384086642190837, 72.51602215082118619 ) ) ;
#2227=CARTESIAN_POINT ( 'NONE',  ( 36.11133435605973574, -20.00384086642191406, 70.60699637195608602 ) ) ;
#2229=CARTESIAN_POINT ( 'NONE',  ( 36.64852494920107517, -25.41368208888610525, 70.89533451361945993 ) ) ;
#2237=CARTESIAN_POINT ( 'NONE',  ( 39.98359781491296161, -23.20384086642191335, 70.89533451361945993 ) ) ;
#2243=CARTESIAN_POINT ( 'NONE',  ( 38.93987200065210175, -0.8038408664219099942, 72.33091598616827866 ) ) ;
#2252=CARTESIAN_POINT ( 'NONE',  ( 37.21915885897815457, -7.413682088886101695, 71.08074471024443142 ) ) ;
#2253=CARTESIAN_POINT ( 'NONE',  ( 37.69225076346193504, -3.813682088886102051, 72.33091598616827866 ) ) ;
#2260=CARTESIAN_POINT ( 'NONE',  ( 39.29254315202757653, -8.803840866421912992, 72.81632618279323310 ) ) ;
#2266=CARTESIAN_POINT ( 'NONE',  ( 39.38009889167650357, -10.21368208888610773, 72.75271321436733274 ) ) ;
#2280=CARTESIAN_POINT ( 'NONE',  ( 36.11133435605973574, -2.003840866421913169, 70.60699637195612866 ) ) ;
#2283=CARTESIAN_POINT ( 'NONE',  ( 38.26194895904383486, -9.013682088886101340, 69.64448340153879258 ) ) ;
#2286=CARTESIAN_POINT ( 'NONE',  ( 37.50301148336529167, -15.11368208888610098, 69.06206559358665231 ) ) ;
#2288=PLANE ( 'NONE',  #19857 ) ;
#2297=CARTESIAN_POINT ( 'NONE',  ( 39.02742774030102879, -26.21368208888610241, 72.26730301774232146 ) ) ;
#2304=CARTESIAN_POINT ( 'NONE',  ( 35.86008812008917346, -22.10384086642191548, 71.32335560751961623 ) ) ;
#2306=CARTESIAN_POINT ( 'NONE',  ( 39.98359781491296161, -26.41368208888610525, 71.86517103874045631 ) ) ;
#2312=CARTESIAN_POINT ( 'NONE',  ( 36.11133435605973574, -2.003840866421913169, 70.60699637195612866 ) ) ;
#2316=CARTESIAN_POINT ( 'NONE',  ( 39.29254315202756231, -6.813682088886101162, 69.94417936956673998 ) ) ;
#2319=CARTESIAN_POINT ( 'NONE',  ( 38.37017380507020192, -24.01368208888610667, 73.11602215082115208 ) ) ;
#2324=CARTESIAN_POINT ( 'NONE',  ( 39.98359781491296161, -5.203840866421911571, 70.89533451361947414 ) ) ;
#2327=CARTESIAN_POINT ( 'NONE',  ( 39.31564783533279694, -23.30384086642191477, 70.72433947564853440 ) ) ;
#2328=CARTESIAN_POINT ( 'NONE',  ( 36.68196826583682935, -13.61368208888610454, 71.96809898377888715 ) ) ;
#2332=CARTESIAN_POINT ( 'NONE',  ( 39.29254315202757653, -10.80384086642191477, 72.81632618279323310 ) ) ;
#2336=CARTESIAN_POINT ( 'NONE',  ( 38.82593461698262871, -10.91368208888609992, 69.62690120949091011 ) ) ;
#2338=CARTESIAN_POINT ( 'NONE',  ( 37.50301148336529167, -17.11368208888609743, 69.06206559358665231 ) ) ;
#2342=CARTESIAN_POINT ( 'NONE',  ( 37.89291511884479036, -16.50384086642191050, 72.49843995877330372 ) ) ;
#2348=CARTESIAN_POINT ( 'NONE',  ( 40.52078840805429394, -25.00384086642191761, 72.15350918040381600 ) ) ;
#2350=CARTESIAN_POINT ( 'NONE',  ( 39.82603832034400426, -28.31368208888610027, 72.40698646996131060 ) ) ;
#2357=CARTESIAN_POINT ( 'NONE',  ( 38.82593461698264292, -18.70384086642191690, 73.13360434286903455 ) ) ;
#2363=CARTESIAN_POINT ( 'NONE',  ( 40.14115730948191185, -29.10384086642190482, 71.43714994484028580 ) ) ;
#2373=CARTESIAN_POINT ( 'NONE',  ( 39.02742774030102879, -6.213682088886101518, 72.26730301774236409 ) ) ;
#2376=CARTESIAN_POINT ( 'NONE',  ( 37.31647492878122563, -7.313682088886101162, 70.72433947564853440 ) ) ;
#2384=CARTESIAN_POINT ( 'NONE',  ( 36.49096545463212493, -12.10384086642191193, 71.32335560751961623 ) ) ;
#2391=CARTESIAN_POINT ( 'NONE',  ( 37.69796330110504101, -9.113682088886100985, 69.66206559358664663 ) ) ;
#2405=CARTESIAN_POINT ( 'NONE',  ( 36.11133435605973574, -4.003840866421914946, 70.60699637195612866 ) ) ;
#2410=CARTESIAN_POINT ( 'NONE',  ( 38.37017380507020192, -10.01368208888611022, 73.11602215082118050 ) ) ;
#2414=CARTESIAN_POINT ( 'NONE',  ( 39.73277004305198545, -16.21368208888610596, 73.23812341099225875 ) ) ;
#2424=CARTESIAN_POINT ( 'NONE',  ( 38.37017380507020192, -26.01368208888610312, 72.51602215082114355 ) ) ;
#2431=CARTESIAN_POINT ( 'NONE',  ( 40.33642880535521869, -21.30384086642190766, 69.98269868914866265 ) ) ;
#2433=CARTESIAN_POINT ( 'NONE',  ( 39.75915168707250302, -24.71368208888610241, 70.26145752964249880 ) ) ;
#2441=CARTESIAN_POINT ( 'NONE',  ( 36.36258059203030513, -3.903840866421911748, 69.89063713639259845 ) ) ;
#2445=CARTESIAN_POINT ( 'NONE',  ( 39.38009889167650357, -6.213682088886108623, 72.75271321436733274 ) ) ;
#2447=CARTESIAN_POINT ( 'NONE',  ( 39.98359781491296161, -28.41368208888610525, 71.86517103874045631 ) ) ;
#2451=CARTESIAN_POINT ( 'NONE',  ( 37.38336156205273397, -23.90384086642191619, 70.63227792289245599 ) ) ;
#2452=CARTESIAN_POINT ( 'NONE',  ( 36.87297107704152666, -11.71368208888611129, 72.49904802271740323 ) ) ;
#2455=CARTESIAN_POINT ( 'NONE',  ( 37.69796330110505522, -10.50384086642190873, 73.09843995877331224 ) ) ;
#2458=CARTESIAN_POINT ( 'NONE',  ( 40.14115730948191185, -10.51368208888609956, 71.32335560751961623 ) ) ;
#2461=CARTESIAN_POINT ( 'NONE',  ( 40.77203464402485622, -14.51368208888610312, 71.32335560751960202 ) ) ;
#2466=CARTESIAN_POINT ( 'NONE',  ( 39.37952058850012804, -19.00384086642191406, 71.78268878715390144 ) ) ;
#2474=CARTESIAN_POINT ( 'NONE',  ( 39.73277004305197124, -23.40384086642191264, 69.52238214136768590 ) ) ;
#2477=CARTESIAN_POINT ( 'NONE',  ( 38.37017380507020192, -28.01368208888610667, 73.11602215082115208 ) ) ;
#2484=CARTESIAN_POINT ( 'NONE',  ( 37.25202387243754032, -12.40384086642191619, 72.75271321436731853 ) ) ;
#2491=CARTESIAN_POINT ( 'NONE',  ( 38.63098279924290068, 1.296159133578087763, 72.53360434286905445 ) ) ;
#2500=CARTESIAN_POINT ( 'NONE',  ( 39.24876120206128860, -6.713682088886101518, 70.63227792289247020 ) ) ;
#2501=CARTESIAN_POINT ( 'NONE',  ( 37.60469502381300089, -7.213682088886102406, 70.49320253461759478 ) ) ;
#2508=CARTESIAN_POINT ( 'NONE',  ( 36.64852494920107517, -10.20384086642191157, 71.86517103874049894 ) ) ;
#2515=CARTESIAN_POINT ( 'NONE',  ( 37.80618814713140097, -7.913682088886108801, 73.13360434286904876 ) ) ;
#2518=CARTESIAN_POINT ( 'NONE',  ( 38.82593461698262871, -26.91368208888610170, 69.62690120949091011 ) ) ;
#2529=CARTESIAN_POINT ( 'NONE',  ( 36.89935272106205133, -4.403840866421918854, 73.23812341099225875 ) ) ;
#2530=CARTESIAN_POINT ( 'NONE',  ( 37.31647492878122563, -21.31368208888610027, 70.72433947564853440 ) ) ;
#2535=CARTESIAN_POINT ( 'NONE',  ( 38.26194895904383486, -7.013682088886100452, 69.64448340153879258 ) ) ;
#2537=CARTESIAN_POINT ( 'NONE',  ( 40.55423172469004811, -14.41368208888610347, 72.05058123536544201 ) ) ;
#2542=CARTESIAN_POINT ( 'NONE',  ( 39.64305411916487287, -29.01274100871117767, 69.84207103023153707 ) ) ;
#2550=CARTESIAN_POINT ( 'NONE',  ( 37.21915885897815457, -23.41368208888610170, 71.08074471024441721 ) ) ;
#2557=CARTESIAN_POINT ( 'NONE',  ( 39.64521430340305841, -26.80384086642191832, 73.30173637941817333 ) ) ;
#2559=CARTESIAN_POINT ( 'NONE',  ( 38.37017380507020192, -28.01368208888610667, 73.11602215082115208 ) ) ;
#2568=CARTESIAN_POINT ( 'NONE',  ( 36.36258059203030513, -1.903840866421910638, 69.89063713639259845 ) ) ;
#2570=CARTESIAN_POINT ( 'NONE',  ( 39.82603832034400426, -8.313682088886110932, 72.40698646996135324 ) ) ;
#2574=CARTESIAN_POINT ( 'NONE',  ( 36.80608444377001121, -25.31368208888610383, 70.35351908239857721 ) ) ;
#2578=CARTESIAN_POINT ( 'NONE',  ( 37.69225076346193504, -25.80384086642191477, 70.42958956619166599 ) ) ;
#2579=CARTESIAN_POINT ( 'NONE',  ( 37.25202387243752611, -11.21368208888610241, 70.00779233799262613 ) ) ;
#2583=CARTESIAN_POINT ( 'NONE',  ( 36.80608444377001831, -12.30384086642191299, 72.40698646996135324 ) ) ;
#2587=CARTESIAN_POINT ( 'NONE',  ( 36.87297107704152666, -3.713682088886109511, 72.49904802271743165 ) ) ;
#2589=CARTESIAN_POINT ( 'NONE',  ( 40.77203464402485622, -16.51368208888610667, 71.32335560751960202 ) ) ;
#2593=CARTESIAN_POINT ( 'NONE',  ( 38.93987200065210175, -20.80384086642191122, 72.33091598616826445 ) ) ;
#2598=CARTESIAN_POINT ( 'NONE',  ( 39.02088643472237806, -22.70384086642191690, 73.73360434286898624 ) ) ;
#2601=CARTESIAN_POINT ( 'NONE',  ( 39.38009889167650357, -26.21368208888610951, 72.75271321436730432 ) ) ;
#2610=CARTESIAN_POINT ( 'NONE',  ( 39.75915168707251723, -16.90384086642191619, 72.49904802271738902 ) ) ;
#2619=CARTESIAN_POINT ( 'NONE',  ( 37.12184278917507640, -2.103840866421912370, 71.32335560751961623 ) ) ;
#2624=CARTESIAN_POINT ( 'NONE',  ( 38.26194895904383486, -25.01368208888610312, 69.64448340153876416 ) ) ;
#2629=CARTESIAN_POINT ( 'NONE',  ( 37.38336156205274818, -3.713682088886102406, 72.12822762946751709 ) ) ;
#2630=CARTESIAN_POINT ( 'NONE',  ( 38.00113996487114321, -5.913682088886099919, 72.53360434286905445 ) ) ;
#2631=VERTEX_POINT ( 'NONE', #9328 ) ;
#2636=CARTESIAN_POINT ( 'NONE',  ( 38.37017380507018771, -11.60384086642190660, 69.64448340153879258 ) ) ;
#2645=CARTESIAN_POINT ( 'NONE',  ( 36.68196826583682935, -5.613682088886105426, 71.96809898377890136 ) ) ;
#2659=CARTESIAN_POINT ( 'NONE',  ( 40.33642880535524000, -28.31368208888611093, 72.77780686321125359 ) ) ;
#2660=CARTESIAN_POINT ( 'NONE',  ( 38.73920764526925353, -24.11368208888610098, 72.49843995877328950 ) ) ;
#2664=CARTESIAN_POINT ( 'NONE',  ( 38.26194895904383486, -1.013682088886101784, 69.64448340153879258 ) ) ;
#2665=CARTESIAN_POINT ( 'NONE',  ( 37.80618814713138676, -27.70384086642190269, 69.62690120949091011 ) ) ;
#2668=CARTESIAN_POINT ( 'NONE',  ( 40.77203464402485622, -10.51368208888610312, 71.32335560751961623 ) ) ;
#2673=CARTESIAN_POINT ( 'NONE',  ( 39.65227363581001185, -29.06301577344905240, 69.84007905757066226 ) ) ;
#2681=CARTESIAN_POINT ( 'NONE',  ( 40.77203464402485622, -19.10384086642191193, 71.43714994484032843 ) ) ;
#2682=CARTESIAN_POINT ( 'NONE',  ( 37.80618814713140097, -25.91368208888610880, 73.13360434286902034 ) ) ;
#2687=( NAMED_UNIT ( * ) PLANE_ANGLE_UNIT ( ) SI_UNIT ( $, .RADIAN. ) );
#2692=CARTESIAN_POINT ( 'NONE',  ( 39.73277004305198545, -26.21368208888610951, 73.23812341099225875 ) ) ;
#2695=CARTESIAN_POINT ( 'NONE',  ( 37.69796330110504101, -7.113682088886100985, 69.66206559358663242 ) ) ;
#2697=CARTESIAN_POINT ( 'NONE',  ( 38.37017380507020192, -22.01368208888611022, 73.11602215082116629 ) ) ;
#2701=CARTESIAN_POINT ( 'NONE',  ( 37.31647492878124694, -22.30384086642191122, 72.03616607671141026 ) ) ;
#2702=CARTESIAN_POINT ( 'NONE',  ( 39.29254315202756231, -12.81368208888610383, 69.94417936956672577 ) ) ;
#2706=CARTESIAN_POINT ( 'NONE',  ( 37.80618814713138676, -13.70384086642190979, 69.62690120949091011 ) ) ;
#2708=CARTESIAN_POINT ( 'NONE',  ( 36.64852494920107517, -7.413682088886104360, 70.89533451361948835 ) ) ;
#2710=CARTESIAN_POINT ( 'NONE',  ( 39.64521430340304420, -12.81368208888610383, 69.45876917294175712 ) ) ;
#2714=CARTESIAN_POINT ( 'NONE',  ( 38.37017380507018771, -9.603840866421911926, 70.24448340153877268 ) ) ;
#2719=CARTESIAN_POINT ( 'NONE',  ( 39.12911128074872380, -25.50384086642191406, 69.06206559358663810 ) ) ;
#2721=CARTESIAN_POINT ( 'NONE',  ( 36.64852494920107517, -27.41368208888610525, 70.89533451361945993 ) ) ;
#2728=CARTESIAN_POINT ( 'NONE',  ( 38.93415946300897446, -15.50384086642190695, 69.66206559358663242 ) ) ;
#2736=CARTESIAN_POINT ( 'NONE',  ( 39.31564783533279694, 0.6961591335780878964, 70.72433947564853440 ) ) ;
#2739=CARTESIAN_POINT ( 'NONE',  ( 36.64852494920107517, -23.41368208888610525, 70.89533451361945993 ) ) ;
#2744=CARTESIAN_POINT ( 'NONE',  ( 39.41296390513587511, -29.20384086642191335, 71.08074471024438878 ) ) ;
#2745=CARTESIAN_POINT ( 'NONE',  ( 38.93987200065208754, -0.8136820888860993861, 70.42958956619168021 ) ) ;
#2751=CARTESIAN_POINT ( 'NONE',  ( 39.98359781491296161, -11.20384086642191335, 70.89533451361947414 ) ) ;
#2761=CARTESIAN_POINT ( 'NONE',  ( 36.49096545463212493, -5.513682088886105781, 71.43714994484035685 ) ) ;
#2776=CARTESIAN_POINT ( 'NONE',  ( 40.33642880535524000, -26.31368208888610383, 72.77780686321125359 ) ) ;
#2779=CARTESIAN_POINT ( 'NONE',  ( 38.93987200065208754, -26.81368208888610738, 70.42958956619166599 ) ) ;
#2783=CARTESIAN_POINT ( 'NONE',  ( 36.49096545463212493, -1.513682088886105559, 71.43714994484035685 ) ) ;
#2784=CARTESIAN_POINT ( 'NONE',  ( 38.82593461698265003, -28.70384086642190624, 73.13360434286902034 ) ) ;
#2789=CARTESIAN_POINT ( 'NONE',  ( 40.33642880535524000, -6.313682088886107380, 72.77780686321128201 ) ) ;
#2808=CARTESIAN_POINT ( 'NONE',  ( 35.86008812008917346, -16.10384086642191193, 71.32335560751961623 ) ) ;
#2810=CARTESIAN_POINT ( 'NONE',  ( 38.93415946300897446, -24.11368208888610454, 73.09843995877328382 ) ) ;
#2816=CARTESIAN_POINT ( 'NONE',  ( 38.26194895904383486, -27.01368208888609956, 69.04448340153878405 ) ) ;
#2820=CARTESIAN_POINT ( 'NONE',  ( 38.93415946300897446, -4.113682088886107202, 73.09843995877331224 ) ) ;
#2822=CARTESIAN_POINT ( 'NONE',  ( 37.80618814713140097, -17.91368208888610525, 73.13360434286903455 ) ) ;
#2827=CARTESIAN_POINT ( 'NONE',  ( 38.93987200065210175, -20.80384086642191122, 72.33091598616826445 ) ) ;
#2828=CARTESIAN_POINT ( 'NONE',  ( 39.98359781491296161, -4.413682088886105248, 71.86517103874048473 ) ) ;
#2833=CARTESIAN_POINT ( 'NONE',  ( 39.82603832034400426, -3.303840866421908995, 70.35351908239857721 ) ) ;
#2835=CARTESIAN_POINT ( 'NONE',  ( 36.64852494920107517, -5.413682088886106136, 70.89533451361948835 ) ) ;
#2837=CARTESIAN_POINT ( 'NONE',  ( 36.36258059203031934, -11.71368208888610951, 72.86986841596736042 ) ) ;
#2841=CARTESIAN_POINT ( 'NONE',  ( 38.00113996487112189, -13.70384086642191157, 70.22690120949090442 ) ) ;
#2846=CARTESIAN_POINT ( 'NONE',  ( 35.86008812008917346, -16.10384086642191193, 71.32335560751961623 ) ) ;
#2850=CARTESIAN_POINT ( 'NONE',  ( 37.25202387243752611, -21.21368208888610241, 70.00779233799262613 ) ) ;
#2857=CARTESIAN_POINT ( 'NONE',  ( 36.80608444377002542, -12.30384086642191477, 72.40698646996133903 ) ) ;
#2863=CARTESIAN_POINT ( 'NONE',  ( 36.87297107704149823, -23.90384086642190198, 70.26145752964251301 ) ) ;
#2867=CARTESIAN_POINT ( 'NONE',  ( 40.14115730948191185, -24.51368208888609601, 71.32335560751958781 ) ) ;
#2873=CARTESIAN_POINT ( 'NONE',  ( 39.31564783533280405, -2.313682088886100718, 72.03616607671141026 ) ) ;
#2874=CARTESIAN_POINT ( 'NONE',  ( 37.31647492878122563, -1.313682088886099830, 70.72433947564853440 ) ) ;
#2882=CARTESIAN_POINT ( 'NONE',  ( 38.37017380507018771, -7.603840866421906597, 69.64448340153879258 ) ) ;
#2890=CARTESIAN_POINT ( 'NONE',  ( 39.38009889167650357, -2.213682088886108179, 72.75271321436733274 ) ) ;
#2904=CARTESIAN_POINT ( 'NONE',  ( 39.37952058850012804, -18.61368208888609743, 70.97781676520601479 ) ) ;
#2911=CARTESIAN_POINT ( 'NONE',  ( 38.37017380507020192, -2.013682088886109334, 73.11602215082118050 ) ) ;
#2912=CARTESIAN_POINT ( 'NONE',  ( 38.82593461698265003, -26.70384086642190624, 73.13360434286902034 ) ) ;
#2915=CARTESIAN_POINT ( 'NONE',  ( 39.12911128074873801, -10.11368208888610987, 73.69843995877330656 ) ) ;
#2934=CARTESIAN_POINT ( 'NONE',  ( 40.33642880535521869, -19.30384086642191477, 69.98269868914866265 ) ) ;
#2936=CARTESIAN_POINT ( 'NONE',  ( 36.49096545463212493, -23.51368208888609601, 71.43714994484030001 ) ) ;
#2940=PRESENTATION_STYLE_ASSIGNMENT (( #20609 ) ) ;
#2944=CARTESIAN_POINT ( 'NONE',  ( 36.07789103942398867, -27.41368208888610525, 70.70992431699450265 ) ) ;
#2949=CARTESIAN_POINT ( 'NONE',  ( 36.68196826583682935, -3.613682088886103205, 71.96809898377890136 ) ) ;
#2952=CARTESIAN_POINT ( 'NONE',  ( 36.80608444377001121, -17.31368208888610027, 70.35351908239860563 ) ) ;
#2956=CARTESIAN_POINT ( 'NONE',  ( 37.38336156205273397, -19.90384086642191264, 70.63227792289247020 ) ) ;
#2957=CARTESIAN_POINT ( 'NONE',  ( 39.82603832034400426, -4.313682088886107380, 72.40698646996135324 ) ) ;
#2962=CARTESIAN_POINT ( 'NONE',  ( 37.33957961208645315, -7.803840866421909439, 69.94417936956673998 ) ) ;
#2966=CARTESIAN_POINT ( 'NONE',  ( 39.95015449827720744, -6.613682088886106314, 70.79240656858107172 ) ) ;
#2968=CARTESIAN_POINT ( 'NONE',  ( 39.12911128074873801, -8.113682088886108090, 73.69843995877330656 ) ) ;
#2971=CARTESIAN_POINT ( 'NONE',  ( 37.89291511884479036, -10.50384086642191050, 72.49843995877331793 ) ) ;
#2977=CARTESIAN_POINT ( 'NONE',  ( 36.98690846071097127, -15.80384086642191299, 69.45876917294175712 ) ) ;
#2980=CARTESIAN_POINT ( 'NONE',  ( 37.69796330110504101, -21.11368208888610454, 69.66206559358661821 ) ) ;
#2990=CARTESIAN_POINT ( 'NONE',  ( 39.29254315202757653, -12.80384086642191299, 72.81632618279321889 ) ) ;
#2993=CARTESIAN_POINT ( 'NONE',  ( 39.98359781491296161, -24.41368208888610525, 71.86517103874045631 ) ) ;
#2996=CARTESIAN_POINT ( 'NONE',  ( 39.98359781491296161, -23.20384086642191335, 70.89533451361945993 ) ) ;
#2998=CARTESIAN_POINT ( 'NONE',  ( 36.49096545463212493, -25.51368208888609956, 71.43714994484030001 ) ) ;
#3004=CARTESIAN_POINT ( 'NONE',  ( 39.02742774030102879, 1.786317911113898704, 72.26730301774236409 ) ) ;
#3005=CARTESIAN_POINT ( 'NONE',  ( 39.37952058850012804, -29.00384086642191406, 71.78268878715390144 ) ) ;
#3013=CARTESIAN_POINT ( 'NONE',  ( 38.82593461698265003, -4.703840866421914235, 73.13360434286904876 ) ) ;
#3024=CARTESIAN_POINT ( 'NONE',  ( 36.80608444377001121, -3.313682088886101162, 70.35351908239861984 ) ) ;
#3042=CARTESIAN_POINT ( 'NONE',  ( 39.51027997493896748, -18.51368208888610312, 71.32335560751960202 ) ) ;
#3046=CARTESIAN_POINT ( 'NONE',  ( 36.64852494920107517, -3.413682088886104360, 70.89533451361948835 ) ) ;
#3047=CARTESIAN_POINT ( 'NONE',  ( 37.69796330110505522, -22.50384086642191050, 73.09843995877329803 ) ) ;
#3052=CARTESIAN_POINT ( 'NONE',  ( 40.55423172469004811, -8.413682088886105248, 72.05058123536544201 ) ) ;
#3070=CARTESIAN_POINT ( 'NONE',  ( 36.29569395875881099, -20.30384086642191122, 72.77780686321128201 ) ) ;
#3071=CARTESIAN_POINT ( 'NONE',  ( 38.37017380507020192, -24.01368208888610667, 73.11602215082115208 ) ) ;
#3079=CARTESIAN_POINT ( 'NONE',  ( 39.02088643472237095, -28.91368208888610170, 69.02690120949091579 ) ) ;
#3085=CARTESIAN_POINT ( 'NONE',  ( 38.26194895904383486, 0.9863179111138999922, 69.64448340153880679 ) ) ;
#3087=CARTESIAN_POINT ( 'NONE',  ( 36.87297107704153376, -19.71368208888610951, 72.49904802271740323 ) ) ;
#3091=CARTESIAN_POINT ( 'NONE',  ( 38.93987200065210175, -16.80384086642191477, 72.33091598616826445 ) ) ;
#3092=CARTESIAN_POINT ( 'NONE',  ( 39.95015449827720744, -4.613682088886104538, 70.79240656858107172 ) ) ;
#3095=CARTESIAN_POINT ( 'NONE',  ( 38.26194895904384907, -2.603840866421916367, 73.11602215082118050 ) ) ;
#3097=CARTESIAN_POINT ( 'NONE',  ( 38.93415946300897446, -6.113682088886107202, 73.09843995877331224 ) ) ;
#3100=CARTESIAN_POINT ( 'NONE',  ( 36.11133435605973574, -9.613682088886104538, 72.15350918040385864 ) ) ;
#3103=CARTESIAN_POINT ( 'NONE',  ( 37.12184278917507640, -14.10384086642191370, 71.32335560751961623 ) ) ;
#3110=CARTESIAN_POINT ( 'NONE',  ( 36.07789103942399578, -18.20384086642191690, 72.05058123536544201 ) ) ;
#3116=CARTESIAN_POINT ( 'NONE',  ( 39.82603832034400426, -22.31368208888610738, 72.40698646996133903 ) ) ;
#3123=CARTESIAN_POINT ( 'NONE',  ( 36.80608444377002542, -10.30384086642191299, 72.40698646996135324 ) ) ;
#3127=CARTESIAN_POINT ( 'NONE',  ( 39.95015449827720744, -22.61368208888610809, 70.79240656858105751 ) ) ;
#3129=CARTESIAN_POINT ( 'NONE',  ( 38.82593461698265003, -22.70384086642191690, 73.13360434286903455 ) ) ;
#3132=CARTESIAN_POINT ( 'NONE',  ( 39.75915168707250302, -26.71368208888609530, 70.26145752964249880 ) ) ;
#3137=CARTESIAN_POINT ( 'NONE',  ( 39.51027997493896748, -29.10384086642191193, 71.43714994484031422 ) ) ;
#3138=CARTESIAN_POINT ( 'NONE',  ( 39.41296390513587511, -0.4136820888861019174, 71.67976084211552745 ) ) ;
#3145=CARTESIAN_POINT ( 'NONE',  ( 38.37017380507018771, -3.603840866421907041, 69.64448340153879258 ) ) ;
#3151=CARTESIAN_POINT ( 'NONE',  ( 39.75915168707250302, -2.713682088886101962, 70.26145752964255564 ) ) ;
#3153=CARTESIAN_POINT ( 'NONE',  ( 39.82603832034401137, -25.30384086642190766, 70.35351908239857721 ) ) ;
#3172=CARTESIAN_POINT ( 'NONE',  ( 39.41296390513587511, -14.41368208888610347, 71.67976084211551324 ) ) ;
#3176=CARTESIAN_POINT ( 'NONE',  ( 37.69796330110504101, 0.8863179111139003474, 69.66206559358664663 ) ) ;
#3177=CARTESIAN_POINT ( 'NONE',  ( 38.37017380507018771, -25.60384086642190837, 69.64448340153876416 ) ) ;
#3179=CARTESIAN_POINT ( 'NONE',  ( 36.89935272106204422, -7.213682088886102406, 69.52238214136768590 ) ) ;
#3188=CARTESIAN_POINT ( 'NONE',  ( 38.26194895904384907, 1.396159133578083633, 73.11602215082119471 ) ) ;
#3196=CARTESIAN_POINT ( 'NONE',  ( 37.61123632939164452, -17.70384086642190979, 69.02690120949091579 ) ) ;
#3197=CARTESIAN_POINT ( 'NONE',  ( 37.25202387243752611, -19.21368208888610241, 70.00779233799262613 ) ) ;
#3206=CARTESIAN_POINT ( 'NONE',  ( 36.07789103942398867, -25.41368208888610525, 70.70992431699450265 ) ) ;
#3210=CARTESIAN_POINT ( 'NONE',  ( 38.93415946300897446, -0.1136820888861071466, 73.09843995877331224 ) ) ;
#3212=CARTESIAN_POINT ( 'NONE',  ( 36.49096545463212493, -21.51368208888610312, 71.43714994484034264 ) ) ;
#3215=CARTESIAN_POINT ( 'NONE',  ( 37.31647492878124694, -20.30384086642190766, 72.03616607671141026 ) ) ;
#3216=CARTESIAN_POINT ( 'NONE',  ( 36.64852494920107517, -7.413682088886104360, 70.89533451361948835 ) ) ;
#3222=CARTESIAN_POINT ( 'NONE',  ( 40.14115730948191185, -7.103840866421910150, 71.43714994484034264 ) ) ;
#3224=CARTESIAN_POINT ( 'NONE',  ( 37.89291511884476904, -27.11368208888610454, 70.26206559358661252 ) ) ;
#3226=CARTESIAN_POINT ( 'NONE',  ( 36.98690846071097837, -11.81368208888611093, 73.30173637941818754 ) ) ;
#3229=CARTESIAN_POINT ( 'NONE',  ( 38.73920764526923932, -13.50384086642191228, 70.26206559358661252 ) ) ;
#3235=CARTESIAN_POINT ( 'NONE',  ( 39.02088643472237806, -16.70384086642191690, 73.73360434286898624 ) ) ;
#3239=CARTESIAN_POINT ( 'NONE',  ( 39.38009889167650357, -20.21368208888610951, 72.75271321436731853 ) ) ;
#3246=CARTESIAN_POINT ( 'NONE',  ( 38.82593461698264292, -8.703840866421913347, 73.13360434286904876 ) ) ;
#3251=CARTESIAN_POINT ( 'NONE',  ( 39.98359781491296161, -26.41368208888610525, 71.86517103874045631 ) ) ;
#3256=CARTESIAN_POINT ( 'NONE',  ( 36.68196826583682935, -22.00384086642191406, 70.79240656858107172 ) ) ;
#3260=CARTESIAN_POINT ( 'NONE',  ( 37.69796330110504101, -19.11368208888610098, 69.66206559358661821 ) ) ;
#3262=CARTESIAN_POINT ( 'NONE',  ( 37.61123632939165873, -25.91368208888610880, 73.73360434286898624 ) ) ;
#3266=CARTESIAN_POINT ( 'NONE',  ( 37.89291511884476904, 0.8863179111139005695, 70.26206559358665515 ) ) ;
#3275=CARTESIAN_POINT ( 'NONE',  ( 36.49096545463212493, -6.103840866421912814, 71.32335560751963044 ) ) ;
#3283=CARTESIAN_POINT ( 'NONE',  ( 36.87297107704153376, -3.713682088886109511, 72.49904802271743165 ) ) ;
#3300=VERTEX_POINT ( 'NONE', #11222 ) ;
#3303=CARTESIAN_POINT ( 'NONE',  ( 37.25260217561390874, -19.61368208888610098, 71.78268878715392987 ) ) ;
#3308=CARTESIAN_POINT ( 'NONE',  ( 37.33957961208645315, -21.80384086642190766, 69.94417936956672577 ) ) ;
#3311=CARTESIAN_POINT ( 'NONE',  ( 36.07789103942398867, -3.413682088886104804, 70.70992431699450265 ) ) ;
#3330=CARTESIAN_POINT ( 'NONE',  ( 39.12911128074872380, -11.50384086642191050, 69.06206559358666652 ) ) ;
#3332=CARTESIAN_POINT ( 'NONE',  ( 39.98359781491296161, -24.41368208888610525, 71.86517103874045631 ) ) ;
#3337=CARTESIAN_POINT ( 'NONE',  ( 35.86008812008917346, -19.51368208888610312, 71.43714994484034264 ) ) ;
#3342=CARTESIAN_POINT ( 'NONE',  ( 39.29254315202756231, 1.186317911113898838, 69.94417936956675419 ) ) ;
#3344=CARTESIAN_POINT ( 'NONE',  ( 39.98359781491296161, -14.41368208888610525, 71.86517103874047052 ) ) ;
#3349=CARTESIAN_POINT ( 'NONE',  ( 38.73920764526923932, -21.50384086642191406, 70.26206559358661252 ) ) ;
#3350=CARTESIAN_POINT ( 'NONE',  ( 38.37017380507020192, -8.013682088886108446, 73.11602215082118050 ) ) ;
#3357=CARTESIAN_POINT ( 'NONE',  ( 37.69796330110505522, -8.503840866421915834, 73.09843995877331224 ) ) ;
#3359=CARTESIAN_POINT ( 'NONE',  ( 39.98359781491296161, -0.4136820888861053591, 71.86517103874048473 ) ) ;
#3361=CARTESIAN_POINT ( 'NONE',  ( 40.33642880535524000, -6.313682088886107380, 72.77780686321128201 ) ) ;
#3365=CARTESIAN_POINT ( 'NONE',  ( 39.02742774030101458, -7.403840866421910860, 70.49320253461759478 ) ) ;
#3371=CARTESIAN_POINT ( 'NONE',  ( 40.52078840805429394, -9.003840866421915834, 72.15350918040385864 ) ) ;
#3373=SURFACE_STYLE_FILL_AREA ( #8812 ) ;
#3374=CARTESIAN_POINT ( 'NONE',  ( 37.80618814713140097, -19.91368208888610170, 73.13360434286903455 ) ) ;
#3381=CARTESIAN_POINT ( 'NONE',  ( 40.14115730948191185, -9.103840866421911926, 71.43714994484034264 ) ) ;
#3384=CARTESIAN_POINT ( 'NONE',  ( 37.25202387243752611, -23.21368208888610241, 70.00779233799262613 ) ) ;
#3388=CARTESIAN_POINT ( 'NONE',  ( 40.14115730948191185, -27.10384086642190482, 71.43714994484028580 ) ) ;
#3391=CARTESIAN_POINT ( 'NONE',  ( 39.75915168707250302, -16.71368208888609885, 70.26145752964251301 ) ) ;
#3393=CARTESIAN_POINT ( 'NONE',  ( 36.89935272106204422, -27.21368208888609885, 69.52238214136765748 ) ) ;
#3398=CARTESIAN_POINT ( 'NONE',  ( 37.60469502381300799, -26.40384086642190908, 72.26730301774232146 ) ) ;
#3405=CARTESIAN_POINT ( 'NONE',  ( 40.14115730948191185, -7.103840866421910150, 71.43714994484034264 ) ) ;
#3415=CARTESIAN_POINT ( 'NONE',  ( 38.82593461698262871, -0.9136820888861021395, 69.62690120949091011 ) ) ;
#3417=CARTESIAN_POINT ( 'NONE',  ( 39.29254315202757653, -24.80384086642191477, 72.81632618279320468 ) ) ;
#3427=ORIENTED_EDGE ( 'NONE', *, *, #19047, .F. ) ;
#3434=CARTESIAN_POINT ( 'NONE',  ( 38.73920764526925353, -8.113682088886099208, 72.49843995877331793 ) ) ;
#3440=CARTESIAN_POINT ( 'NONE',  ( 36.68196826583682935, -26.00384086642191406, 70.79240656858105751 ) ) ;
#3460=CARTESIAN_POINT ( 'NONE',  ( 39.73277004305197124, -11.40384086642191086, 69.52238214136768590 ) ) ;
#3464=CARTESIAN_POINT ( 'NONE',  ( 38.37017380507020192, -14.01368208888610845, 73.11602215082116629 ) ) ;
#3469=CARTESIAN_POINT ( 'NONE',  ( 36.11133435605973574, -21.61368208888610454, 72.15350918040385864 ) ) ;
#3477=CARTESIAN_POINT ( 'NONE',  ( 38.73920764526923932, -13.50384086642191228, 70.26206559358661252 ) ) ;
#3478=CARTESIAN_POINT ( 'NONE',  ( 39.98359781491296161, -0.4136820888861053591, 71.86517103874048473 ) ) ;
#3485=CARTESIAN_POINT ( 'NONE',  ( 36.36258059203030513, -27.90384086642191264, 69.89063713639258424 ) ) ;
#3488=CARTESIAN_POINT ( 'NONE',  ( 38.26194895904383486, 0.9863179111138999922, 69.64448340153880679 ) ) ;
#3489=CARTESIAN_POINT ( 'NONE',  ( 40.77203464402485622, -2.513682088886103116, 71.32335560751961623 ) ) ;
#3492=CARTESIAN_POINT ( 'NONE',  ( 38.00113996487112189, -3.703840866421909794, 70.22690120949091863 ) ) ;
#3497=CARTESIAN_POINT ( 'NONE',  ( 40.52078840805429394, -7.003840866421914058, 72.15350918040385864 ) ) ;
#3500=CARTESIAN_POINT ( 'NONE',  ( 38.26194895904383486, -15.01368208888610134, 69.64448340153877837 ) ) ;
#3506=CARTESIAN_POINT ( 'NONE',  ( 37.33957961208645315, -5.803840866421907663, 69.94417936956673998 ) ) ;
#3510=CARTESIAN_POINT ( 'NONE',  ( 39.38009889167650357, -16.21368208888610596, 72.75271321436731853 ) ) ;
#3512=CARTESIAN_POINT ( 'NONE',  ( 37.69796330110505522, -16.50384086642191761, 73.09843995877329803 ) ) ;
#3514=CARTESIAN_POINT ( 'NONE',  ( 39.95015449827720744, -16.61368208888610454, 70.79240656858105751 ) ) ;
#3516=CARTESIAN_POINT ( 'NONE',  ( 37.61123632939165873, -27.91368208888610880, 73.73360434286898624 ) ) ;
#3520=CARTESIAN_POINT ( 'NONE',  ( 37.31647492878124694, -22.30384086642191122, 72.03616607671141026 ) ) ;
#3527=CARTESIAN_POINT ( 'NONE',  ( 39.02088643472237806, -26.70384086642192401, 73.73360434286898624 ) ) ;
#3536=CARTESIAN_POINT ( 'NONE',  ( 38.26194895904384907, -24.60384086642191548, 73.11602215082115208 ) ) ;
#3549=CARTESIAN_POINT ( 'NONE',  ( 37.38336156205274818, -9.713682088886098853, 72.12822762946751709 ) ) ;
#3550=CARTESIAN_POINT ( 'NONE',  ( 39.37952058850012804, -10.61368208888610276, 70.97781676520601479 ) ) ;
#3556=CARTESIAN_POINT ( 'NONE',  ( 39.95015449827720744, -17.00384086642191406, 71.96809898377887293 ) ) ;
#3559=CARTESIAN_POINT ( 'NONE',  ( 38.73920764526925353, -16.11368208888610454, 72.49843995877330372 ) ) ;
#3577=CARTESIAN_POINT ( 'NONE',  ( 37.61123632939164452, -9.703840866421911571, 69.02690120949094421 ) ) ;
#3580=CARTESIAN_POINT ( 'NONE',  ( 37.25202387243752611, -15.21368208888610063, 70.00779233799262613 ) ) ;
#3585=CARTESIAN_POINT ( 'NONE',  ( 36.98690846071097837, -19.81368208888611093, 73.30173637941818754 ) ) ;
#3597=CARTESIAN_POINT ( 'NONE',  ( 37.38336156205273397, -13.90384086642191264, 70.63227792289247020 ) ) ;
#3598=CARTESIAN_POINT ( 'NONE',  ( 38.26194895904383486, -1.013682088886101784, 69.64448340153879258 ) ) ;
#3605=CARTESIAN_POINT ( 'NONE',  ( 36.29569395875881099, -28.30384086642192187, 72.77780686321126780 ) ) ;
#3607=CARTESIAN_POINT ( 'NONE',  ( 39.37952058850012804, -28.61368208888610454, 70.97781676520600058 ) ) ;
#3608=CARTESIAN_POINT ( 'NONE',  ( 38.37017380507020192, -6.013682088886110222, 73.71602215082116061 ) ) ;
#3611=CARTESIAN_POINT ( 'NONE',  ( 39.24876120206129571, -2.903840866421911304, 72.12822762946750288 ) ) ;
#3616=CARTESIAN_POINT ( 'NONE',  ( 36.11133435605973574, -10.00384086642191761, 70.60699637195612866 ) ) ;
#3619=CARTESIAN_POINT ( 'NONE',  ( 36.49096545463212493, -15.51368208888610667, 71.43714994484034264 ) ) ;
#3626=CARTESIAN_POINT ( 'NONE',  ( 36.80608444377002542, -8.303840866421916544, 72.40698646996135324 ) ) ;
#3629=CARTESIAN_POINT ( 'NONE',  ( 37.80618814713140097, -19.91368208888610170, 73.13360434286903455 ) ) ;
#3631=CARTESIAN_POINT ( 'NONE',  ( 39.29254315202757653, -20.80384086642191832, 72.81632618279321889 ) ) ;
#3633=CARTESIAN_POINT ( 'NONE',  ( 39.98359781491296161, -18.41368208888610880, 71.86517103874047052 ) ) ;
#3635=CARTESIAN_POINT ( 'NONE',  ( 40.52078840805428683, -24.61368208888610809, 70.60699637195608602 ) ) ;
#3640=CARTESIAN_POINT ( 'NONE',  ( 38.37017380507018771, -23.60384086642191903, 70.24448340153875847 ) ) ;
#3647=CARTESIAN_POINT ( 'NONE',  ( 37.25202387243754032, -0.4038408664219159117, 72.75271321436733274 ) ) ;
#3658=CARTESIAN_POINT ( 'NONE',  ( 37.69796330110505522, -28.50384086642191761, 73.09843995877328382 ) ) ;
#3667=CARTESIAN_POINT ( 'NONE',  ( 38.93987200065210175, -4.803840866421909439, 72.33091598616827866 ) ) ;
#3676=CARTESIAN_POINT ( 'NONE',  ( 38.63098279924288647, -14.91368208888609992, 70.22690120949090442 ) ) ;
#3678=CARTESIAN_POINT ( 'NONE',  ( 39.37952058850012804, -12.61368208888609921, 70.97781676520601479 ) ) ;
#3685=CARTESIAN_POINT ( 'NONE',  ( 39.38009889167648936, -17.40384086642190908, 70.00779233799262613 ) ) ;
#3688=CARTESIAN_POINT ( 'NONE',  ( 37.12184278917507640, -21.51368208888609956, 71.43714994484034264 ) ) ;
#3704=CARTESIAN_POINT ( 'NONE',  ( 35.86008812008917346, -8.103840866421913702, 71.32335560751961623 ) ) ;
#3706=CARTESIAN_POINT ( 'NONE',  ( 36.49096545463212493, -13.51368208888610489, 71.43714994484034264 ) ) ;
#3711=CARTESIAN_POINT ( 'NONE',  ( 35.86008812008917346, -23.51368208888609956, 71.43714994484032843 ) ) ;
#3726=CARTESIAN_POINT ( 'NONE',  ( 39.24876120206129571, -12.90384086642191264, 72.12822762946747446 ) ) ;
#3727=CARTESIAN_POINT ( 'NONE',  ( 37.38336156205274818, -27.71368208888610241, 72.12822762946747446 ) ) ;
#3734=CARTESIAN_POINT ( 'NONE',  ( 39.95015449827720744, 0.9961591335780894951, 71.96809898377890136 ) ) ;
#3735=CARTESIAN_POINT ( 'NONE',  ( 39.29254315202756231, -0.8136820888860994971, 69.94417936956673998 ) ) ;
#3737=CARTESIAN_POINT ( 'NONE',  ( 40.33642880535524000, -0.3136820888861093781, 72.77780686321128201 ) ) ;
#3738=EDGE_LOOP ( 'NONE', ( #5619, #20576 ) ) ;
#3740=CARTESIAN_POINT ( 'NONE',  ( 37.31647492878124694, -4.303840866421912992, 72.03616607671141026 ) ) ;
#3745=CARTESIAN_POINT ( 'NONE',  ( 39.64521430340305841, -10.80384086642191832, 73.30173637941818754 ) ) ;
#3749=CARTESIAN_POINT ( 'NONE',  ( 36.87297107704152666, -11.71368208888611129, 72.49904802271740323 ) ) ;
#3756=CARTESIAN_POINT ( 'NONE',  ( 37.69796330110505522, -4.503840866421914946, 73.09843995877331224 ) ) ;
#3759=CARTESIAN_POINT ( 'NONE',  ( 39.29254315202756231, -16.81368208888610383, 69.94417936956672577 ) ) ;
#3762=CARTESIAN_POINT ( 'NONE',  ( 36.49096545463212493, -18.10384086642191193, 71.32335560751961623 ) ) ;
#3765=CARTESIAN_POINT ( 'NONE',  ( 38.26194895904383486, -17.01368208888610312, 69.64448340153877837 ) ) ;
#3767=CARTESIAN_POINT ( 'NONE',  ( 39.12911128074873801, -22.11368208888610809, 73.69843995877327814 ) ) ;
#3771=CARTESIAN_POINT ( 'NONE',  ( 39.31564783533279694, -27.30384086642191477, 70.72433947564850598 ) ) ;
#3778=CARTESIAN_POINT ( 'NONE',  ( 35.86008812008917346, -28.10384086642191903, 71.32335560751960202 ) ) ;
#3780=CARTESIAN_POINT ( 'NONE',  ( 36.29569395875879678, -5.313682088886097610, 69.98269868914869107 ) ) ;
#3789=CARTESIAN_POINT ( 'NONE',  ( 38.82593461698264292, -22.70384086642191690, 73.13360434286903455 ) ) ;
#3795=CARTESIAN_POINT ( 'NONE',  ( 38.00113996487112189, -3.703840866421909794, 70.22690120949091863 ) ) ;
#3803=CARTESIAN_POINT ( 'NONE',  ( 37.21915885897815457, -9.413682088886103472, 71.08074471024443142 ) ) ;
#3805=CARTESIAN_POINT ( 'NONE',  ( 37.31647492878122563, -11.31368208888609850, 70.72433947564853440 ) ) ;
#3807=ADVANCED_FACE ( 'NONE', ( #17626 ), #10461, .T. ) ;
#3814=CARTESIAN_POINT ( 'NONE',  ( 37.25202387243754032, -18.40384086642191974, 72.75271321436731853 ) ) ;
#3818=CARTESIAN_POINT ( 'NONE',  ( 37.31647492878122563, -17.31368208888610383, 70.72433947564853440 ) ) ;
#3823=CARTESIAN_POINT ( 'NONE',  ( 38.82593461698262871, -10.91368208888610170, 69.62690120949091011 ) ) ;
#3837=CARTESIAN_POINT ( 'NONE',  ( 39.12911128074872380, -13.50384086642191228, 69.06206559358665231 ) ) ;
#3841=CARTESIAN_POINT ( 'NONE',  ( 39.29254315202756231, -16.81368208888610383, 69.94417936956672577 ) ) ;
#3848=CARTESIAN_POINT ( 'NONE',  ( 40.77203464402485622, -24.51368208888610667, 71.32335560751960202 ) ) ;
#3861=CARTESIAN_POINT ( 'NONE',  ( 38.93987200065210175, -14.80384086642191122, 72.33091598616826445 ) ) ;
#3862=CARTESIAN_POINT ( 'NONE',  ( 38.37017380507020192, -0.01368208888610777940, 73.11602215082118050 ) ) ;
#3869=CARTESIAN_POINT ( 'NONE',  ( 37.50301148336529877, -28.50384086642192116, 73.69843995877326392 ) ) ;
#3870=CARTESIAN_POINT ( 'NONE',  ( 37.89291511884476904, -23.11368208888610454, 70.26206559358661252 ) ) ;
#3871=CARTESIAN_POINT ( 'NONE',  ( 38.26194895904383486, -5.013682088886101340, 69.04448340153881247 ) ) ;
#3874=CARTESIAN_POINT ( 'NONE',  ( 39.02742774030101458, -3.403840866421911748, 70.49320253461759478 ) ) ;
#3877=CARTESIAN_POINT ( 'NONE',  ( 39.02088643472237095, -2.913682088886100363, 69.02690120949094421 ) ) ;
#3882=CARTESIAN_POINT ( 'NONE',  ( 39.12911128074872380, -9.503840866421912281, 69.06206559358666652 ) ) ;
#3886=CARTESIAN_POINT ( 'NONE',  ( 37.25202387243752611, -15.21368208888610063, 70.00779233799262613 ) ) ;
#3892=CARTESIAN_POINT ( 'NONE',  ( 37.80618814713138676, -3.703840866421905798, 69.62690120949091011 ) ) ;
#3895=CARTESIAN_POINT ( 'NONE',  ( 39.29254315202756231, -20.81368208888610027, 69.94417936956672577 ) ) ;
#3898=CARTESIAN_POINT ( 'NONE',  ( 37.69796330110505522, -20.50384086642191050, 73.09843995877329803 ) ) ;
#3902=CARTESIAN_POINT ( 'NONE',  ( 38.26194895904383486, -15.01368208888610134, 69.64448340153877837 ) ) ;
#3904=CARTESIAN_POINT ( 'NONE',  ( 39.02088643472237095, -20.91368208888609814, 69.02690120949091579 ) ) ;
#3909=CARTESIAN_POINT ( 'NONE',  ( 38.73920764526923932, -21.50384086642191406, 70.26206559358661252 ) ) ;
#3913=CARTESIAN_POINT ( 'NONE',  ( 39.59324923284151510, -28.74115096347518161, 70.20355626897213597 ) ) ;
#3916=CARTESIAN_POINT ( 'NONE',  ( 36.80608444377001831, -0.3038408664219130473, 72.40698646996136745 ) ) ;
#3918=CARTESIAN_POINT ( 'NONE',  ( 40.33642880535524000, -2.313682088886106936, 72.77780686321128201 ) ) ;
#3927=CARTESIAN_POINT ( 'NONE',  ( 36.49096545463212493, -18.10384086642191193, 71.32335560751961623 ) ) ;
#3935=CARTESIAN_POINT ( 'NONE',  ( 39.37952058850012804, -7.003840866421911393, 71.78268878715392987 ) ) ;
#3941=CARTESIAN_POINT ( 'NONE',  ( 38.00113996487114321, -11.91368208888610170, 72.53360434286904024 ) ) ;
#3942=CARTESIAN_POINT ( 'NONE',  ( 38.93987200065208754, -12.81368208888610383, 70.42958956619168021 ) ) ;
#3949=CARTESIAN_POINT ( 'NONE',  ( 36.68196826583682935, -18.00384086642191406, 70.79240656858107172 ) ) ;
#3952=CARTESIAN_POINT ( 'NONE',  ( 37.25260217561390874, -17.61368208888609743, 71.78268878715392987 ) ) ;
#3956=CARTESIAN_POINT ( 'NONE',  ( 36.64852494920107517, -13.41368208888610525, 70.89533451361947414 ) ) ;
#3962=CARTESIAN_POINT ( 'NONE',  ( 39.95015449827720744, -28.61368208888610454, 70.79240656858104330 ) ) ;
#3970=CARTESIAN_POINT ( 'NONE',  ( 36.36258059203030513, -3.903840866421911748, 69.89063713639259845 ) ) ;
#3973=CARTESIAN_POINT ( 'NONE',  ( 39.75915168707250302, -16.71368208888609885, 70.26145752964251301 ) ) ;
#3977=CARTESIAN_POINT ( 'NONE',  ( 36.98690846071097837, -11.81368208888611093, 73.30173637941818754 ) ) ;
#3988=CARTESIAN_POINT ( 'NONE',  ( 38.73920764526923932, -11.50384086642191050, 70.26206559358664094 ) ) ;
#3989=CARTESIAN_POINT ( 'NONE',  ( 37.31647492878122563, -27.31368208888610027, 70.72433947564853440 ) ) ;
#3995=CARTESIAN_POINT ( 'NONE',  ( 38.37017380507018771, -29.60384086642191193, 69.04448340153878405 ) ) ;
#3997=CARTESIAN_POINT ( 'NONE',  ( 38.73920764526925353, -26.11368208888610454, 72.49843995877328950 ) ) ;
#3998=CARTESIAN_POINT ( 'NONE',  ( 38.37017380507020192, -0.01368208888610778114, 73.71602215082116061 ) ) ;
#4003=CARTESIAN_POINT ( 'NONE',  ( 38.37017380507018771, 0.3961591335780896284, 70.24448340153880110 ) ) ;
#4010=CARTESIAN_POINT ( 'NONE',  ( 40.52078840805429394, -5.003840866421915834, 72.15350918040385864 ) ) ;
#4013=CARTESIAN_POINT ( 'NONE',  ( 39.82603832034400426, -16.31368208888610738, 72.40698646996133903 ) ) ;
#4017=CARTESIAN_POINT ( 'NONE',  ( 36.64852494920107517, -4.203840866421910683, 71.86517103874049894 ) ) ;
#4019=CARTESIAN_POINT ( 'NONE',  ( 36.49096545463212493, -19.51368208888610312, 71.43714994484034264 ) ) ;
#4023=CARTESIAN_POINT ( 'NONE',  ( 40.14115730948191185, -19.10384086642191193, 71.43714994484030001 ) ) ;
#4026=CARTESIAN_POINT ( 'NONE',  ( 36.49096545463212493, -13.51368208888610489, 71.43714994484034264 ) ) ;
#4028=CARTESIAN_POINT ( 'NONE',  ( 39.73277004305198545, -22.21368208888610951, 73.23812341099225875 ) ) ;
#4032=CARTESIAN_POINT ( 'NONE',  ( 37.69225076346193504, -15.80384086642191299, 70.42958956619168021 ) ) ;
#4035=CARTESIAN_POINT ( 'NONE',  ( 39.59147561631770884, -28.73147929012166202, 70.27394150260606409 ) ) ;
#4038=CARTESIAN_POINT ( 'NONE',  ( 36.64852494920107517, -0.2038408664219101829, 71.86517103874049894 ) ) ;
#4041=CARTESIAN_POINT ( 'NONE',  ( 36.98690846071097837, -1.813682088886107602, 73.30173637941818754 ) ) ;
#4049=CARTESIAN_POINT ( 'NONE',  ( 37.33957961208645315, -19.80384086642191122, 69.94417936956672577 ) ) ;
#4059=CARTESIAN_POINT ( 'NONE',  ( 38.93987200065210175, -8.803840866421911215, 72.33091598616827866 ) ) ;
#4070=CARTESIAN_POINT ( 'NONE',  ( 39.31564783533280405, -10.31368208888610027, 72.03616607671141026 ) ) ;
#4072=CARTESIAN_POINT ( 'NONE',  ( 37.12184278917507640, -3.513682088886100452, 71.43714994484035685 ) ) ;
#4079=CARTESIAN_POINT ( 'NONE',  ( 36.80608444377001831, -18.30384086642190766, 72.40698646996135324 ) ) ;
#4084=CARTESIAN_POINT ( 'NONE',  ( 37.89291511884476904, -21.11368208888610098, 70.26206559358661252 ) ) ;
#4090=CARTESIAN_POINT ( 'NONE',  ( 37.33957961208646736, -15.81368208888610916, 72.81632618279321889 ) ) ;
#4105=CARTESIAN_POINT ( 'NONE',  ( 39.64521430340305841, -6.803840866421918321, 73.30173637941818754 ) ) ;
#4109=CARTESIAN_POINT ( 'NONE',  ( 38.26194895904383486, -11.01368208888609956, 69.64448340153879258 ) ) ;
#4115=CARTESIAN_POINT ( 'NONE',  ( 40.55423172469004811, -16.41368208888610525, 72.05058123536544201 ) ) ;
#4125=CARTESIAN_POINT ( 'NONE',  ( 38.00113996487114321, -21.91368208888610170, 72.53360434286904024 ) ) ;
#4133=CARTESIAN_POINT ( 'NONE',  ( 38.37017380507018771, -21.60384086642191548, 69.04448340153878405 ) ) ;
#4134=CARTESIAN_POINT ( 'NONE',  ( 37.60469502381300089, -23.21368208888610241, 70.49320253461758057 ) ) ;
#4135=CARTESIAN_POINT ( 'NONE',  ( 40.14115730948191185, -28.51368208888610667, 71.32335560751958781 ) ) ;
#4138=CARTESIAN_POINT ( 'NONE',  ( 37.21915885897815457, -0.2038408664219102107, 71.67976084211552745 ) ) ;
#4145=CARTESIAN_POINT ( 'NONE',  ( 40.33642880535521869, -3.303840866421912548, 69.98269868914867686 ) ) ;
#4147=CARTESIAN_POINT ( 'NONE',  ( 38.82593461698262871, -4.913682088886100807, 69.62690120949091011 ) ) ;
#4150=CARTESIAN_POINT ( 'NONE',  ( 37.69796330110504101, -27.11368208888610098, 69.66206559358661821 ) ) ;
#4154=CARTESIAN_POINT ( 'NONE',  ( 36.68196826583682935, -0.003840866421911393047, 70.79240656858108593 ) ) ;
#4156=CARTESIAN_POINT ( 'NONE',  ( 39.95015449827720744, -14.61368208888610454, 70.79240656858105751 ) ) ;
#4158=CARTESIAN_POINT ( 'NONE',  ( 36.87297107704149823, -9.903840866421901978, 70.26145752964255564 ) ) ;
#4161=CARTESIAN_POINT ( 'NONE',  ( 39.95015449827720744, -10.61368208888610631, 70.79240656858107172 ) ) ;
#4163=CARTESIAN_POINT ( 'NONE',  ( 36.11133435605973574, -21.61368208888610454, 72.15350918040385864 ) ) ;
#4168=CARTESIAN_POINT ( 'NONE',  ( 39.31564783533279694, -21.30384086642190766, 70.72433947564853440 ) ) ;
#4174=CARTESIAN_POINT ( 'NONE',  ( 38.37017380507018771, -25.60384086642191548, 69.04448340153878405 ) ) ;
#4176=CARTESIAN_POINT ( 'NONE',  ( 40.26954217208371034, 1.286317911113898260, 69.89063713639259845 ) ) ;
#4183=CARTESIAN_POINT ( 'NONE',  ( 40.14115730948191185, -19.10384086642191193, 71.43714994484031422 ) ) ;
#4189=CARTESIAN_POINT ( 'NONE',  ( 38.26194895904384197, -2.603840866421912814, 72.51602215082118619 ) ) ;
#4195=CARTESIAN_POINT ( 'NONE',  ( 39.51027997493896748, -8.513682088886101340, 71.32335560751961623 ) ) ;
#4198=CARTESIAN_POINT ( 'NONE',  ( 39.37952058850012804, -4.613682088886100985, 70.97781676520601479 ) ) ;
#4205=CARTESIAN_POINT ( 'NONE',  ( 36.49096545463212493, -10.10384086642191193, 71.32335560751963044 ) ) ;
#4214=CARTESIAN_POINT ( 'NONE',  ( 39.29254315202756231, -10.81368208888610205, 69.94417936956673998 ) ) ;
#4230=CARTESIAN_POINT ( 'NONE',  ( 37.50301148336529877, -2.503840866421917166, 73.69843995877330656 ) ) ;
#4236=CARTESIAN_POINT ( 'NONE',  ( 36.49096545463212493, -11.51368208888609956, 71.43714994484034264 ) ) ;
#4243=CARTESIAN_POINT ( 'NONE',  ( 39.02088643472237095, -12.91368208888610525, 69.02690120949091579 ) ) ;
#4254=CARTESIAN_POINT ( 'NONE',  ( 37.89291511884476904, -23.11368208888610454, 70.26206559358661252 ) ) ;
#4263=CARTESIAN_POINT ( 'NONE',  ( 37.50301148336529877, -22.50384086642191761, 73.69843995877327814 ) ) ;
#4265=CARTESIAN_POINT ( 'NONE',  ( 37.69796330110504101, -27.11368208888609388, 69.66206559358660400 ) ) ;
#4269=AXIS2_PLACEMENT_3D ( 'NONE', #21443, #19137, #9612 ) ;
#4272=CARTESIAN_POINT ( 'NONE',  ( 39.64521430340305841, -0.8038408664219169886, 73.30173637941818754 ) ) ;
#4275=CARTESIAN_POINT ( 'NONE',  ( 40.14115730948191185, -8.513682088886104893, 71.32335560751961623 ) ) ;
#4281=CARTESIAN_POINT ( 'NONE',  ( 39.38009889167648936, -1.403840866421906419, 70.00779233799264034 ) ) ;
#4284=CARTESIAN_POINT ( 'NONE',  ( 39.37952058850012804, -27.00384086642191050, 71.78268878715390144 ) ) ;
#4285=CARTESIAN_POINT ( 'NONE',  ( 38.26194895904383486, -15.01368208888610134, 69.64448340153877837 ) ) ;
#4289=CARTESIAN_POINT ( 'NONE',  ( 38.37017380507018771, -11.60384086642190660, 69.64448340153879258 ) ) ;
#4292=CARTESIAN_POINT ( 'NONE',  ( 37.33957961208646736, -9.813682088886107380, 72.81632618279323310 ) ) ;
#4294=CARTESIAN_POINT ( 'NONE',  ( 36.98690846071097837, -13.81368208888610916, 73.30173637941818754 ) ) ;
#4300=CARTESIAN_POINT ( 'NONE',  ( 38.73920764526923932, -17.50384086642191406, 70.26206559358661252 ) ) ;
#4307=CARTESIAN_POINT ( 'NONE',  ( 40.52078840805429394, -23.00384086642191761, 72.15350918040381600 ) ) ;
#4309=CARTESIAN_POINT ( 'NONE',  ( 37.80618814713140097, -27.91368208888610880, 73.13360434286902034 ) ) ;
#4315=CARTESIAN_POINT ( 'NONE',  ( 38.82593461698264292, -20.70384086642191335, 73.13360434286903455 ) ) ;
#4323=CARTESIAN_POINT ( 'NONE',  ( 39.37952058850012804, -1.003840866421912281, 71.78268878715392987 ) ) ;
#4331=CARTESIAN_POINT ( 'NONE',  ( 38.37017380507020192, -8.013682088886101340, 72.51602215082118619 ) ) ;
#4332=CARTESIAN_POINT ( 'NONE',  ( 37.21915885897815457, -25.41368208888610170, 71.08074471024441721 ) ) ;
#4333=CARTESIAN_POINT ( 'NONE',  ( 37.60469502381300089, -3.213682088886101962, 70.49320253461759478 ) ) ;
#4340=CARTESIAN_POINT ( 'NONE',  ( 37.25202387243754032, -10.40384086642191441, 72.75271321436733274 ) ) ;
#4347=CARTESIAN_POINT ( 'NONE',  ( 39.75915168707250302, -4.713682088886099741, 70.26145752964255564 ) ) ;
#4359=CARTESIAN_POINT ( 'NONE',  ( 37.50301148336529877, -6.503840866421916722, 73.69843995877330656 ) ) ;
#4363=CARTESIAN_POINT ( 'NONE',  ( 36.87297107704152666, -5.713682088886105959, 72.49904802271743165 ) ) ;
#4365=CARTESIAN_POINT ( 'NONE',  ( 35.86008812008917346, -17.51368208888610667, 71.43714994484034264 ) ) ;
#4378=CARTESIAN_POINT ( 'NONE',  ( 37.89291511884476904, -25.11368208888610454, 70.26206559358661252 ) ) ;
#4386=CARTESIAN_POINT ( 'NONE',  ( 36.07789103942399578, -26.20384086642191335, 72.05058123536544201 ) ) ;
#4389=CARTESIAN_POINT ( 'NONE',  ( 36.11133435605973574, 0.3863179111138967392, 72.15350918040385864 ) ) ;
#4396=CARTESIAN_POINT ( 'NONE',  ( 39.12911128074872380, -5.503840866421911393, 69.06206559358666652 ) ) ;
#4399=CARTESIAN_POINT ( 'NONE',  ( 37.33957961208646736, -9.813682088886107380, 72.81632618279323310 ) ) ;
#4406=CARTESIAN_POINT ( 'NONE',  ( 37.21915885897815457, -28.20384086642191335, 71.67976084211551324 ) ) ;
#4407=CARTESIAN_POINT ( 'NONE',  ( 39.98359781491296161, -12.41368208888610525, 71.86517103874047052 ) ) ;
#4410=CARTESIAN_POINT ( 'NONE',  ( 37.33957961208645315, -9.803840866421907663, 69.94417936956673998 ) ) ;
#4414=CARTESIAN_POINT ( 'NONE',  ( 37.25202387243752611, -13.21368208888610063, 70.00779233799262613 ) ) ;
#4416=CARTESIAN_POINT ( 'NONE',  ( 38.26194895904383486, -15.01368208888610134, 69.04448340153878405 ) ) ;
#4420=CARTESIAN_POINT ( 'NONE',  ( 39.41296390513587511, -19.20384086642191335, 71.08074471024441721 ) ) ;
#4425=CARTESIAN_POINT ( 'NONE',  ( 40.55423172469004101, -25.20384086642191690, 70.70992431699446001 ) ) ;
#4427=CARTESIAN_POINT ( 'NONE',  ( 38.26194895904383486, -27.01368208888610312, 69.64448340153876416 ) ) ;
#4437=CARTESIAN_POINT ( 'NONE',  ( 40.14115730948191185, -17.10384086642191193, 71.43714994484031422 ) ) ;
#4442=CARTESIAN_POINT ( 'NONE',  ( 39.24876120206129571, 1.096159133578088696, 72.12822762946751709 ) ) ;
#4451=CARTESIAN_POINT ( 'NONE',  ( 38.26194895904383486, -3.013682088886100008, 70.24448340153877268 ) ) ;
#4454=CARTESIAN_POINT ( 'NONE',  ( 38.73920764526925353, -4.113682088886099208, 72.49843995877331793 ) ) ;
#4461=CARTESIAN_POINT ( 'NONE',  ( 37.69796330110505522, -10.50384086642190873, 73.09843995877331224 ) ) ;
#4466=B_SPLINE_CURVE_WITH_KNOTS ( 'NONE', 3,
 ( #6523, #8466, #18755, #10654, #4841, #10528, #589, #18624, #16299, #20315, #12470, #24525 ),
 .UNSPECIFIED., .F., .F.,
 ( 4, 2, 2, 2, 2, 4 ),
 ( 0.002960931562157818973, 0.003008429244711963331, 0.003055926927266107256, 0.003150922292374415921, 0.003340913022591033253, 0.003720894483024222380 ),
 .UNSPECIFIED. ) ;
#4472=CARTESIAN_POINT ( 'NONE',  ( 39.98359781491296161, -10.41368208888610347, 71.86517103874048473 ) ) ;
#4486=CARTESIAN_POINT ( 'NONE',  ( 40.33642880535521869, -3.303840866421912548, 69.98269868914867686 ) ) ;
#4490=CARTESIAN_POINT ( 'NONE',  ( 36.80608444377001121, -7.313682088886100274, 70.35351908239860563 ) ) ;
#4493=CARTESIAN_POINT ( 'NONE',  ( 36.11133435605973574, -15.61368208888610454, 72.15350918040385864 ) ) ;
#4501=CARTESIAN_POINT ( 'NONE',  ( 37.89291511884476904, -27.11368208888610454, 70.26206559358661252 ) ) ;
#4508=CARTESIAN_POINT ( 'NONE',  ( 36.89935272106205133, -24.40384086642191974, 73.23812341099225875 ) ) ;
#4510=CARTESIAN_POINT ( 'NONE',  ( 40.77203464402485622, 1.486317911113896661, 71.32335560751961623 ) ) ;
#4520=CARTESIAN_POINT ( 'NONE',  ( 40.77203464402485622, -3.103840866421913258, 71.43714994484034264 ) ) ;
#4526=CARTESIAN_POINT ( 'NONE',  ( 38.82593461698262871, -8.913682088886101695, 69.62690120949091011 ) ) ;
#4528=CARTESIAN_POINT ( 'NONE',  ( 38.82593461698262871, -26.91368208888610170, 69.62690120949091011 ) ) ;
#4535=CARTESIAN_POINT ( 'NONE',  ( 37.31647492878124694, -28.30384086642191477, 72.03616607671141026 ) ) ;
#4536=CARTESIAN_POINT ( 'NONE',  ( 38.26194895904383486, -11.01368208888609956, 69.64448340153879258 ) ) ;
#4541=CARTESIAN_POINT ( 'NONE',  ( 36.87297107704149823, -13.90384086642190908, 70.26145752964252722 ) ) ;
#4544=CARTESIAN_POINT ( 'NONE',  ( 36.68196826583682935, -7.613682088886103649, 71.96809898377890136 ) ) ;
#4546=CARTESIAN_POINT ( 'NONE',  ( 37.50301148336529167, -15.11368208888610098, 69.06206559358665231 ) ) ;
#4550=CARTESIAN_POINT ( 'NONE',  ( 37.60469502381300799, -20.40384086642191264, 72.26730301774234988 ) ) ;
#4555=CARTESIAN_POINT ( 'NONE',  ( 36.98690846071097127, -21.80384086642191122, 69.45876917294175712 ) ) ;
#4560=CARTESIAN_POINT ( 'NONE',  ( 39.29254315202756231, -26.81368208888610027, 69.94417936956671156 ) ) ;
#4567=CARTESIAN_POINT ( 'NONE',  ( 37.33957961208645315, -11.80384086642190944, 69.94417936956672577 ) ) ;
#4574=CARTESIAN_POINT ( 'NONE',  ( 37.12184278917507640, -0.1038408664219107880, 71.32335560751961623 ) ) ;
#4583=CARTESIAN_POINT ( 'NONE',  ( 38.26194895904383486, -7.013682088886100452, 70.24448340153877268 ) ) ;
#4584=CARTESIAN_POINT ( 'NONE',  ( 37.25260217561390874, -1.613682088886101651, 71.78268878715394408 ) ) ;
#4590=CARTESIAN_POINT ( 'NONE',  ( 37.25202387243754032, -8.403840866421916189, 72.75271321436733274 ) ) ;
#4597=CARTESIAN_POINT ( 'NONE',  ( 36.64852494920107517, -5.413682088886106136, 70.89533451361948835 ) ) ;
#4609=CARTESIAN_POINT ( 'NONE',  ( 40.26954217208371034, -26.71368208888610596, 69.89063713639254161 ) ) ;
#4610=CARTESIAN_POINT ( 'NONE',  ( 39.24876120206128860, -20.71368208888610596, 70.63227792289245599 ) ) ;
#4615=CARTESIAN_POINT ( 'NONE',  ( 40.14115730948191185, -10.51368208888609956, 71.32335560751961623 ) ) ;
#4616=CARTESIAN_POINT ( 'NONE',  ( 36.87297107704149823, -27.90384086642190908, 70.26145752964251301 ) ) ;
#4619=CARTESIAN_POINT ( 'NONE',  ( 39.73277004305198545, -10.21368208888610773, 73.23812341099225875 ) ) ;
#4634=CARTESIAN_POINT ( 'NONE',  ( 38.26194895904384197, -14.60384086642191726, 73.71602215082113219 ) ) ;
#4635=CARTESIAN_POINT ( 'NONE',  ( 36.07789103942398867, 0.5863179111138955291, 70.70992431699450265 ) ) ;
#4645=CARTESIAN_POINT ( 'NONE',  ( 35.86008812008917346, -27.51368208888610667, 71.43714994484032843 ) ) ;
#4648=CARTESIAN_POINT ( 'NONE',  ( 39.82603832034400426, -6.313682088886107380, 72.40698646996135324 ) ) ;
#4651=CARTESIAN_POINT ( 'NONE',  ( 39.29254315202756231, -20.81368208888610027, 69.94417936956672577 ) ) ;
#4656=CARTESIAN_POINT ( 'NONE',  ( 38.26194895904384197, -22.60384086642191548, 72.51602215082118619 ) ) ;
#4657=CARTESIAN_POINT ( 'NONE',  ( 37.80618814713140097, -9.913682088886107024, 73.13360434286904876 ) ) ;
#4661=CARTESIAN_POINT ( 'NONE',  ( 39.29254315202757653, -8.803840866421912992, 72.81632618279323310 ) ) ;
#4664=CARTESIAN_POINT ( 'NONE',  ( 40.14115730948191185, -4.513682088886103116, 71.32335560751961623 ) ) ;
#4666=CARTESIAN_POINT ( 'NONE',  ( 39.02088643472237095, -12.91368208888610525, 69.02690120949091579 ) ) ;
#4670=CARTESIAN_POINT ( 'NONE',  ( 38.63098279924290068, -8.703840866421911571, 72.53360434286905445 ) ) ;
#4671=( GEOMETRIC_REPRESENTATION_CONTEXT ( 3 ) GLOBAL_UNCERTAINTY_ASSIGNED_CONTEXT ( ( #22658 ) ) GLOBAL_UNIT_ASSIGNED_CONTEXT ( ( #18674, #22910, #8895 ) ) REPRESENTATION_CONTEXT ( 'NONE', 'WORKASPACE' ) );
#4677=CARTESIAN_POINT ( 'NONE',  ( 40.55423172469004101, -23.20384086642191690, 70.70992431699450265 ) ) ;
#4680=CARTESIAN_POINT ( 'NONE',  ( 38.37017380507020192, 1.986317911113890666, 73.71602215082117482 ) ) ;
#4687=CARTESIAN_POINT ( 'NONE',  ( 39.95015449827720744, -17.00384086642191406, 71.96809898377887293 ) ) ;
#4696=CARTESIAN_POINT ( 'NONE',  ( 38.93987200065210175, 1.196159133578088118, 72.33091598616827866 ) ) ;
#4701=CARTESIAN_POINT ( 'NONE',  ( 40.14115730948191185, -26.51368208888610667, 71.32335560751958781 ) ) ;
#4706=CARTESIAN_POINT ( 'NONE',  ( 39.31564783533280405, -4.313682088886102051, 72.03616607671141026 ) ) ;
#4707=CARTESIAN_POINT ( 'NONE',  ( 38.63098279924288647, -0.9136820888861024725, 70.22690120949091863 ) ) ;
#4713=CARTESIAN_POINT ( 'NONE',  ( 36.68196826583682935, -14.00384086642191228, 70.79240656858107172 ) ) ;
#4723=CARTESIAN_POINT ( 'NONE',  ( 37.80618814713140097, -5.913682088886107024, 73.13360434286904876 ) ) ;
#4735=CARTESIAN_POINT ( 'NONE',  ( 36.29569395875881099, -0.3038408664219164890, 72.77780686321129622 ) ) ;
#4736=CARTESIAN_POINT ( 'NONE',  ( 39.51027997493896748, -22.51368208888609246, 71.32335560751960202 ) ) ;
#4740=CARTESIAN_POINT ( 'NONE',  ( 36.68196826583682935, -1.613682088886104982, 71.96809898377890136 ) ) ;
#4741=CARTESIAN_POINT ( 'NONE',  ( 39.41296390513587511, 0.7961591335780872081, 71.08074471024443142 ) ) ;
#4743=CARTESIAN_POINT ( 'NONE',  ( 36.29569395875879678, -9.313682088886098498, 69.98269868914869107 ) ) ;
#4755=CARTESIAN_POINT ( 'NONE',  ( 36.07789103942399578, -18.20384086642191690, 72.05058123536544201 ) ) ;
#4756=CARTESIAN_POINT ( 'NONE',  ( 40.14115730948191185, -20.51368208888609601, 71.32335560751960202 ) ) ;
#4763=CARTESIAN_POINT ( 'NONE',  ( 36.36258059203031934, -27.71368208888610596, 72.86986841596734621 ) ) ;
#4769=CARTESIAN_POINT ( 'NONE',  ( 38.93415946300897446, 1.886317911113891244, 73.09843995877332645 ) ) ;
#4771=CARTESIAN_POINT ( 'NONE',  ( 38.37017380507020192, -18.01368208888611022, 73.11602215082116629 ) ) ;
#4774=CARTESIAN_POINT ( 'NONE',  ( 37.12184278917507640, -16.10384086642191193, 71.32335560751961623 ) ) ;
#4775=CARTESIAN_POINT ( 'NONE',  ( 36.68196826583682935, -5.613682088886105426, 71.96809898377890136 ) ) ;
#4780=CARTESIAN_POINT ( 'NONE',  ( 38.93415946300896024, -3.503840866421906952, 69.66206559358663242 ) ) ;
#4781=CARTESIAN_POINT ( 'NONE',  ( 40.05245289102396100, -29.10876147765230115, 71.40796565871902146 ) ) ;
#4782=CARTESIAN_POINT ( 'NONE',  ( 37.33957961208646736, -7.813682088886109156, 72.81632618279323310 ) ) ;
#4784=CARTESIAN_POINT ( 'NONE',  ( 40.52078840805428683, -12.61368208888610454, 70.60699637195608602 ) ) ;
#4788=CARTESIAN_POINT ( 'NONE',  ( 37.89291511884479036, -14.50384086642191228, 72.49843995877330372 ) ) ;
#4793=CARTESIAN_POINT ( 'NONE',  ( 39.02088643472237806, -14.70384086642192045, 73.73360434286898624 ) ) ;
#4796=CARTESIAN_POINT ( 'NONE',  ( 38.26194895904383486, -19.01368208888610312, 69.64448340153877837 ) ) ;
#4802=CARTESIAN_POINT ( 'NONE',  ( 38.93415946300897446, -17.50384086642190695, 69.66206559358663242 ) ) ;
#4811=CARTESIAN_POINT ( 'NONE',  ( 36.64852494920107517, -24.20384086642190979, 71.86517103874047052 ) ) ;
#4814=CARTESIAN_POINT ( 'NONE',  ( 38.26194895904383486, -27.01368208888610312, 69.64448340153876416 ) ) ;
#4819=CARTESIAN_POINT ( 'NONE',  ( 37.12184278917507640, -28.10384086642191193, 71.32335560751960202 ) ) ;
#4820=CARTESIAN_POINT ( 'NONE',  ( 39.02742774030101458, -29.40384086642191264, 70.49320253461758057 ) ) ;
#4826=CARTESIAN_POINT ( 'NONE',  ( 39.82603832034400426, -5.303840866421906775, 70.35351908239857721 ) ) ;
#4840=CARTESIAN_POINT ( 'NONE',  ( 40.14115730948191185, 1.486317911113897106, 71.32335560751963044 ) ) ;
#4841=CARTESIAN_POINT ( 'NONE',  ( 39.98436526329850693, -29.10876147765399224, 71.36840536879221020 ) ) ;
#4855=CARTESIAN_POINT ( 'NONE',  ( 40.33642880535521869, 0.6961591335780878964, 69.98269868914869107 ) ) ;
#4857=CARTESIAN_POINT ( 'NONE',  ( 39.37952058850012804, -20.61368208888610098, 70.97781676520601479 ) ) ;
#4861=CARTESIAN_POINT ( 'NONE',  ( 39.98359781491296161, -0.4136820888861053591, 71.86517103874048473 ) ) ;
#4862=CARTESIAN_POINT ( 'NONE',  ( 39.82603832034400426, -27.30384086642191122, 70.35351908239857721 ) ) ;
#4864=CARTESIAN_POINT ( 'NONE',  ( 38.37017380507020192, -6.013682088886110222, 73.71602215082116061 ) ) ;
#4881=CARTESIAN_POINT ( 'NONE',  ( 39.73277004305197124, -19.40384086642191264, 69.52238214136768590 ) ) ;
#4884=CARTESIAN_POINT ( 'NONE',  ( 40.14115730948191185, -22.51368208888609956, 71.32335560751960202 ) ) ;
#4891=CARTESIAN_POINT ( 'NONE',  ( 40.33642880535524000, -28.31368208888611093, 72.77780686321125359 ) ) ;
#4896=CARTESIAN_POINT ( 'NONE',  ( 37.25202387243752611, -3.213682088886102406, 70.00779233799264034 ) ) ;
#4898=CARTESIAN_POINT ( 'NONE',  ( 39.75915168707250302, -20.71368208888610241, 70.26145752964252722 ) ) ;
#4904=CARTESIAN_POINT ( 'NONE',  ( 37.25260217561390874, -22.00384086642191406, 70.97781676520601479 ) ) ;
#4905=CARTESIAN_POINT ( 'NONE',  ( 36.80608444377001121, -3.313682088886100718, 70.35351908239860563 ) ) ;
#4911=CARTESIAN_POINT ( 'NONE',  ( 37.69796330110505522, -4.503840866421913169, 73.09843995877331224 ) ) ;
#4915=CARTESIAN_POINT ( 'NONE',  ( 36.87297107704152666, -7.713682088886109511, 72.49904802271743165 ) ) ;
#4917=CARTESIAN_POINT ( 'NONE',  ( 36.07789103942398867, -9.413682088886105248, 70.70992431699450265 ) ) ;
#4920=CARTESIAN_POINT ( 'NONE',  ( 39.24876120206129571, -12.90384086642191264, 72.12822762946747446 ) ) ;
#4926=CARTESIAN_POINT ( 'NONE',  ( 37.61123632939164452, -17.70384086642190979, 69.02690120949091579 ) ) ;
#4929=PRESENTATION_STYLE_ASSIGNMENT (( #16650 ) ) ;
#4930=CARTESIAN_POINT ( 'NONE',  ( 39.38009889167650357, -18.21368208888610951, 72.75271321436731853 ) ) ;
#4938=CARTESIAN_POINT ( 'NONE',  ( 39.82603832034401137, -15.30384086642190766, 70.35351908239857721 ) ) ;
#4941=CARTESIAN_POINT ( 'NONE',  ( 39.75915168707250302, -26.71368208888609530, 70.26145752964249880 ) ) ;
#4944=CARTESIAN_POINT ( 'NONE',  ( 37.33957961208645315, -25.80384086642190766, 69.94417936956671156 ) ) ;
#4945=FACE_OUTER_BOUND ( 'NONE', #14844, .T. ) ;
#4947=CARTESIAN_POINT ( 'NONE',  ( 36.49096545463212493, -27.51368208888610312, 71.43714994484030001 ) ) ;
#4953=CARTESIAN_POINT ( 'NONE',  ( 39.41296390513587511, 1.586317911113900081, 71.67976084211552745 ) ) ;
#4955=CARTESIAN_POINT ( 'NONE',  ( 37.21915885897815457, 0.5863179111138989708, 71.08074471024443142 ) ) ;
#4962=CARTESIAN_POINT ( 'NONE',  ( 39.98359781491296161, -7.203840866421913347, 70.89533451361947414 ) ) ;
#4970=CARTESIAN_POINT ( 'NONE',  ( 38.93415946300898867, 1.886317911113891022, 73.09843995877332645 ) ) ;
#4987=CARTESIAN_POINT ( 'NONE',  ( 38.00113996487114321, -15.91368208888609992, 72.53360434286904024 ) ) ;
#4991=CARTESIAN_POINT ( 'NONE',  ( 38.93415946300897446, -0.1136820888861071466, 73.09843995877331224 ) ) ;
#4992=CARTESIAN_POINT ( 'NONE',  ( 36.87297107704149823, -25.90384086642190908, 70.26145752964251301 ) ) ;
#4995=CARTESIAN_POINT ( 'NONE',  ( 40.52078840805428683, -8.613682088886102761, 70.60699637195608602 ) ) ;
#5012=CARTESIAN_POINT ( 'NONE',  ( 40.52078840805429394, -15.00384086642191583, 72.15350918040381600 ) ) ;
#5015=CARTESIAN_POINT ( 'NONE',  ( 39.95015449827720744, -18.61368208888610454, 70.79240656858105751 ) ) ;
#5022=CARTESIAN_POINT ( 'NONE',  ( 36.07789103942399578, -0.2038408664219136524, 72.05058123536544201 ) ) ;
#5027=CARTESIAN_POINT ( 'NONE',  ( 38.82593461698262871, -0.9136820888861022505, 69.62690120949091011 ) ) ;
#5030=CARTESIAN_POINT ( 'NONE',  ( 38.37017380507020192, -20.01368208888610667, 73.11602215082116629 ) ) ;
#5033=CARTESIAN_POINT ( 'NONE',  ( 39.02742774030101458, -17.40384086642191264, 70.49320253461759478 ) ) ;
#5034=CARTESIAN_POINT ( 'NONE',  ( 36.49096545463212493, -5.513682088886105781, 71.43714994484035685 ) ) ;
#5039=CARTESIAN_POINT ( 'NONE',  ( 39.75915168707251723, -4.903840866421914413, 72.49904802271740323 ) ) ;
#5042=CARTESIAN_POINT ( 'NONE',  ( 37.33957961208646736, -5.813682088886107380, 72.81632618279323310 ) ) ;
#5044=CARTESIAN_POINT ( 'NONE',  ( 36.98690846071097837, -7.813682088886109156, 73.30173637941818754 ) ) ;
#5047=CARTESIAN_POINT ( 'NONE',  ( 38.26194895904384197, -14.60384086642191193, 72.51602215082118619 ) ) ;
#5053=CARTESIAN_POINT ( 'NONE',  ( 39.73277004305197124, -13.40384086642191619, 69.52238214136768590 ) ) ;
#5058=CARTESIAN_POINT ( 'NONE',  ( 38.26194895904383486, -23.01368208888609956, 69.64448340153877837 ) ) ;
#5070=CARTESIAN_POINT ( 'NONE',  ( 36.64852494920107517, -10.20384086642191157, 71.86517103874049894 ) ) ;
#5073=CARTESIAN_POINT ( 'NONE',  ( 37.69796330110504101, -25.11368208888609388, 69.66206559358660400 ) ) ;
#5076=CARTESIAN_POINT ( 'NONE',  ( 38.26194895904384907, -24.60384086642191548, 73.11602215082115208 ) ) ;
#5080=CARTESIAN_POINT ( 'NONE',  ( 36.68196826583682935, -27.61368208888610809, 71.96809898377887293 ) ) ;
#5086=CARTESIAN_POINT ( 'NONE',  ( 38.93987200065208754, -0.8136820888860993861, 70.42958956619168021 ) ) ;
#5087=CARTESIAN_POINT ( 'NONE',  ( 38.37017380507020192, 1.986317911113897550, 72.51602215082118619 ) ) ;
#5095=CARTESIAN_POINT ( 'NONE',  ( 39.82603832034400426, -7.303840866421906775, 70.35351908239857721 ) ) ;
#5106=CARTESIAN_POINT ( 'NONE',  ( 39.82603832034401847, -2.313682088886107824, 72.40698646996133903 ) ) ;
#5124=CARTESIAN_POINT ( 'NONE',  ( 39.37952058850012804, -14.61368208888610098, 70.97781676520601479 ) ) ;
#5128=CARTESIAN_POINT ( 'NONE',  ( 36.64852494920107517, 0.5863179111138955291, 70.89533451361948835 ) ) ;
#5129=CARTESIAN_POINT ( 'NONE',  ( 36.49096545463212493, -26.10384086642190482, 71.32335560751960202 ) ) ;
#5134=CARTESIAN_POINT ( 'NONE',  ( 38.26194895904383486, -9.013682088886101340, 69.04448340153881247 ) ) ;
#5149=CARTESIAN_POINT ( 'NONE',  ( 39.12911128074872380, -17.50384086642191406, 69.06206559358665231 ) ) ;
#5150=CARTESIAN_POINT ( 'NONE',  ( 39.38009889167650357, -22.21368208888610951, 72.75271321436731853 ) ) ;
#5155=CARTESIAN_POINT ( 'NONE',  ( 36.36258059203030513, 0.09615913357808798800, 69.89063713639259845 ) ) ;
#5160=CARTESIAN_POINT ( 'NONE',  ( 36.49096545463212493, -1.513682088886105559, 71.43714994484035685 ) ) ;
#5164=CARTESIAN_POINT ( 'NONE',  ( 37.80618814713140097, -19.91368208888610525, 73.13360434286903455 ) ) ;
#5170=CARTESIAN_POINT ( 'NONE',  ( 37.31647492878124694, -18.30384086642191122, 72.03616607671141026 ) ) ;
#5171=CARTESIAN_POINT ( 'NONE',  ( 36.64852494920107517, -3.413682088886104360, 70.89533451361948835 ) ) ;
#5177=CARTESIAN_POINT ( 'NONE',  ( 38.93415946300896024, -5.503840866421906952, 69.66206559358663242 ) ) ;
#5179=CARTESIAN_POINT ( 'NONE',  ( 39.82603832034400426, -2.313682088886107380, 72.40698646996135324 ) ) ;
#5181=CARTESIAN_POINT ( 'NONE',  ( 39.73277004305198545, -10.21368208888610773, 73.23812341099225875 ) ) ;
#5184=CARTESIAN_POINT ( 'NONE',  ( 37.38336156205273397, -11.90384086642191441, 70.63227792289247020 ) ) ;
#5189=CARTESIAN_POINT ( 'NONE',  ( 40.55423172469004101, -15.20384086642191512, 70.70992431699450265 ) ) ;
#5192=CARTESIAN_POINT ( 'NONE',  ( 38.93415946300897446, -22.11368208888610454, 73.09843995877329803 ) ) ;
#5198=CARTESIAN_POINT ( 'NONE',  ( 37.33957961208645315, -9.803840866421907663, 69.94417936956673998 ) ) ;
#5201=CARTESIAN_POINT ( 'NONE',  ( 38.26194895904383486, -27.01368208888610312, 69.64448340153876416 ) ) ;
#5204=CARTESIAN_POINT ( 'NONE',  ( 37.80618814713138676, -23.70384086642190979, 69.62690120949091011 ) ) ;
#5206=CARTESIAN_POINT ( 'NONE',  ( 38.37017380507020192, -26.01368208888611022, 73.11602215082115208 ) ) ;
#5211=CARTESIAN_POINT ( 'NONE',  ( 37.12184278917507640, 0.4863179111138996036, 71.43714994484035685 ) ) ;
#5218=CARTESIAN_POINT ( 'NONE',  ( 37.25202387243754032, -2.403840866421914413, 72.75271321436733274 ) ) ;
#5226=CARTESIAN_POINT ( 'NONE',  ( 37.25202387243752611, 0.7863179111138978161, 70.00779233799264034 ) ) ;
#5227=CARTESIAN_POINT ( 'NONE',  ( 37.33957961208645315, -27.80384086642191122, 69.94417936956671156 ) ) ;
#5244=CARTESIAN_POINT ( 'NONE',  ( 39.02742774030102879, -20.21368208888610241, 72.26730301774234988 ) ) ;
#5249=CARTESIAN_POINT ( 'NONE',  ( 38.82593461698262871, 1.086317911113899637, 69.62690120949091011 ) ) ;
#5250=CARTESIAN_POINT ( 'NONE',  ( 38.26194895904384907, -20.60384086642191548, 73.11602215082116629 ) ) ;
#5252=CARTESIAN_POINT ( 'NONE',  ( 36.11133435605973574, -3.613682088886103205, 72.15350918040385864 ) ) ;
#5259=CARTESIAN_POINT ( 'NONE',  ( 39.59567279493035841, -28.75436684219576833, 70.10737821607207820 ) ) ;
#5269=CARTESIAN_POINT ( 'NONE',  ( 36.11133435605973574, -8.003840866421915834, 70.60699637195612866 ) ) ;
#5271=CARTESIAN_POINT ( 'NONE',  ( 38.93415946300897446, -18.11368208888611164, 73.09843995877329803 ) ) ;
#5277=CARTESIAN_POINT ( 'NONE',  ( 40.26954217208371034, -22.71368208888610241, 69.89063713639258424 ) ) ;
#5280=CARTESIAN_POINT ( 'NONE',  ( 39.95015449827720744, -2.613682088886105870, 70.79240656858107172 ) ) ;
#5283=CARTESIAN_POINT ( 'NONE',  ( 37.69796330110504101, -15.11368208888609921, 69.66206559358663242 ) ) ;
#5286=CARTESIAN_POINT ( 'NONE',  ( 39.37952058850012804, -21.00384086642191050, 71.78268878715390144 ) ) ;
#5287=CARTESIAN_POINT ( 'NONE',  ( 36.87297107704152666, -5.713682088886105959, 72.49904802271743165 ) ) ;
#5294=CARTESIAN_POINT ( 'NONE',  ( 37.25202387243754032, -2.403840866421914413, 72.75271321436733274 ) ) ;
#5299=CARTESIAN_POINT ( 'NONE',  ( 39.82603832034400426, 1.686317911113891732, 72.40698646996136745 ) ) ;
#5301=CARTESIAN_POINT ( 'NONE',  ( 36.07789103942398867, -7.413682088886105248, 70.70992431699450265 ) ) ;
#5305=CARTESIAN_POINT ( 'NONE',  ( 38.63098279924290068, -2.703840866421912015, 72.53360434286905445 ) ) ;
#5307=EDGE_CURVE ( 'NONE', #12953, #8151, #6205, .T. ) ;
#5312=CARTESIAN_POINT ( 'NONE',  ( 36.29569395875881099, -18.30384086642191477, 72.77780686321128201 ) ) ;
#5316=CARTESIAN_POINT ( 'NONE',  ( 36.87297107704152666, -17.71368208888610951, 72.49904802271740323 ) ) ;
#5324=CARTESIAN_POINT ( 'NONE',  ( 37.25202387243754032, -6.403840866421914413, 72.75271321436733274 ) ) ;
#5328=CARTESIAN_POINT ( 'NONE',  ( 40.14115730948191185, -26.51368208888610667, 71.32335560751958781 ) ) ;
#5330=CARTESIAN_POINT ( 'NONE',  ( 37.25202387243754032, -24.40384086642191619, 72.75271321436730432 ) ) ;
#5333=CARTESIAN_POINT ( 'NONE',  ( 37.25202387243752611, -21.21368208888610241, 70.00779233799262613 ) ) ;
#5335=CARTESIAN_POINT ( 'NONE',  ( 36.07789103942398867, -25.41368208888610525, 70.70992431699450265 ) ) ;
#5339=CARTESIAN_POINT ( 'NONE',  ( 38.00113996487114321, -1.913682088886099475, 72.53360434286905445 ) ) ;
#5348=CARTESIAN_POINT ( 'NONE',  ( 38.82593461698265003, -2.703840866421916012, 73.13360434286904876 ) ) ;
#5355=CARTESIAN_POINT ( 'NONE',  ( 38.82593461698262871, 1.086317911113899637, 69.62690120949092432 ) ) ;
#5357=CARTESIAN_POINT ( 'NONE',  ( 36.87297107704151244, -25.90384086642190908, 70.26145752964252722 ) ) ;
#5373=CARTESIAN_POINT ( 'NONE',  ( 37.38336156205274818, -17.71368208888609885, 72.12822762946750288 ) ) ;
#5378=CARTESIAN_POINT ( 'NONE',  ( 38.37017380507018771, -23.60384086642190837, 69.64448340153877837 ) ) ;
#5399=CARTESIAN_POINT ( 'NONE',  ( 36.07789103942399578, -12.20384086642191512, 72.05058123536544201 ) ) ;
#5402=CARTESIAN_POINT ( 'NONE',  ( 36.64852494920107517, -13.41368208888610525, 70.89533451361947414 ) ) ;
#5407=CARTESIAN_POINT ( 'NONE',  ( 39.73277004305198545, -18.21368208888610596, 73.23812341099225875 ) ) ;
#5416=CARTESIAN_POINT ( 'NONE',  ( 38.37017380507018771, -15.60384086642191370, 70.24448340153875847 ) ) ;
#5417=CARTESIAN_POINT ( 'NONE',  ( 37.25202387243752611, 0.7863179111138978161, 70.00779233799264034 ) ) ;
#5423=CARTESIAN_POINT ( 'NONE',  ( 40.14115730948191185, 0.8961591335780898504, 71.43714994484035685 ) ) ;
#5425=CARTESIAN_POINT ( 'NONE',  ( 38.37017380507020192, -28.01368208888610312, 72.51602215082114355 ) ) ;
#5426=CARTESIAN_POINT ( 'NONE',  ( 40.77203464402485622, -4.513682088886104893, 71.32335560751961623 ) ) ;
#5430=CARTESIAN_POINT ( 'NONE',  ( 37.31647492878124694, -6.303840866421912104, 72.03616607671141026 ) ) ;
#5436=CARTESIAN_POINT ( 'NONE',  ( 36.11133435605973574, -8.003840866421915834, 70.60699637195612866 ) ) ;
#5439=CARTESIAN_POINT ( 'NONE',  ( 39.38009889167650357, -16.21368208888610596, 72.75271321436731853 ) ) ;
#5444=CARTESIAN_POINT ( 'NONE',  ( 39.95015449827720744, -9.003840866421912281, 71.96809898377888715 ) ) ;
#5448=CARTESIAN_POINT ( 'NONE',  ( 36.80608444377001121, -17.31368208888609672, 70.35351908239857721 ) ) ;
#5451=CARTESIAN_POINT ( 'NONE',  ( 39.82603832034400426, -17.30384086642190056, 70.35351908239857721 ) ) ;
#5454=CARTESIAN_POINT ( 'NONE',  ( 36.64852494920107517, -17.41368208888610525, 70.89533451361947414 ) ) ;
#5456=CARTESIAN_POINT ( 'NONE',  ( 40.26954217208371034, -28.71368208888610241, 69.89063713639254161 ) ) ;
#5461=CARTESIAN_POINT ( 'NONE',  ( 39.51027997493896748, -23.10384086642191548, 71.43714994484032843 ) ) ;
#5468=CARTESIAN_POINT ( 'NONE',  ( 37.50301148336529877, -28.50384086642192116, 73.69843995877326392 ) ) ;
#5475=ORIENTED_EDGE ( 'NONE', *, *, #2155, .F. ) ;
#5480=CARTESIAN_POINT ( 'NONE',  ( 39.38009889167648936, -27.40384086642190908, 70.00779233799262613 ) ) ;
#5500=CARTESIAN_POINT ( 'NONE',  ( 37.12184278917507640, -9.513682088886101340, 71.43714994484035685 ) ) ;
#5501=CARTESIAN_POINT ( 'NONE',  ( 38.26194895904383486, -11.01368208888609956, 70.24448340153877268 ) ) ;
#5507=CARTESIAN_POINT ( 'NONE',  ( 40.14115730948191185, -21.10384086642191193, 71.43714994484030001 ) ) ;
#5508=STYLED_ITEM ( 'NONE', ( #2940 ), #8595 ) ;
#5511=CARTESIAN_POINT ( 'NONE',  ( 37.21915885897815457, -21.41368208888610525, 71.08074471024443142 ) ) ;
#5530=CARTESIAN_POINT ( 'NONE',  ( 39.64521430340305841, -10.80384086642191832, 73.30173637941818754 ) ) ;
#5533=CARTESIAN_POINT ( 'NONE',  ( 36.87297107704152666, -17.71368208888610951, 72.49904802271740323 ) ) ;
#5537=CARTESIAN_POINT ( 'NONE',  ( 36.36258059203031934, -21.71368208888610596, 72.86986841596736042 ) ) ;
#5545=CARTESIAN_POINT ( 'NONE',  ( 39.24876120206129571, -10.90384086642191264, 72.12822762946750288 ) ) ;
#5546=CARTESIAN_POINT ( 'NONE',  ( 37.33957961208646736, 0.1863179111138910105, 72.81632618279323310 ) ) ;
#5552=CARTESIAN_POINT ( 'NONE',  ( 39.29254315202757653, 1.196159133578084788, 72.81632618279324731 ) ) ;
#5553=CARTESIAN_POINT ( 'NONE',  ( 37.25202387243752611, 0.7863179111138978161, 70.00779233799264034 ) ) ;
#5554=CARTESIAN_POINT ( 'NONE',  ( 36.98690846071097837, -3.813682088886109156, 73.30173637941818754 ) ) ;
#5559=CARTESIAN_POINT ( 'NONE',  ( 37.21915885897815457, -4.203840866421909794, 71.67976084211552745 ) ) ;
#5565=CARTESIAN_POINT ( 'NONE',  ( 36.36258059203030513, -9.903840866421909084, 69.89063713639259845 ) ) ;
#5568=CARTESIAN_POINT ( 'NONE',  ( 37.69796330110504101, -13.11368208888609743, 69.66206559358661821 ) ) ;
#5574=CARTESIAN_POINT ( 'NONE',  ( 39.38009889167648936, -5.403840866421906419, 70.00779233799264034 ) ) ;
#5579=CARTESIAN_POINT ( 'NONE',  ( 36.64852494920107517, -15.41368208888610525, 70.89533451361947414 ) ) ;
#5581=CARTESIAN_POINT ( 'NONE',  ( 36.68196826583682935, -16.00384086642191050, 70.79240656858107172 ) ) ;
#5583=CARTESIAN_POINT ( 'NONE',  ( 36.49096545463212493, -15.51368208888610667, 71.43714994484034264 ) ) ;
#5585=CARTESIAN_POINT ( 'NONE',  ( 36.07789103942398867, -21.41368208888610880, 70.70992431699450265 ) ) ;
#5589=CARTESIAN_POINT ( 'NONE',  ( 39.51027997493896748, -27.10384086642191903, 71.43714994484031422 ) ) ;
#5595=CARTESIAN_POINT ( 'NONE',  ( 39.82603832034400426, 0.6961591335780910050, 70.35351908239860563 ) ) ;
#5604=CARTESIAN_POINT ( 'NONE',  ( 40.14115730948191185, -27.10384086642191193, 71.43714994484030001 ) ) ;
#5609=CARTESIAN_POINT ( 'NONE',  ( 39.37952058850012804, -5.003840866421912281, 71.78268878715392987 ) ) ;
#5615=CARTESIAN_POINT ( 'NONE',  ( 38.00113996487114321, -13.91368208888610347, 72.53360434286904024 ) ) ;
#5618=CARTESIAN_POINT ( 'NONE',  ( 39.31564783533280405, -10.31368208888610027, 72.03616607671141026 ) ) ;
#5619=ORIENTED_EDGE ( 'NONE', *, *, #10532, .F. ) ;
#5625=CARTESIAN_POINT ( 'NONE',  ( 36.80608444377001831, -14.30384086642191122, 72.40698646996135324 ) ) ;
#5629=CARTESIAN_POINT ( 'NONE',  ( 38.93987200065208754, -18.81368208888610027, 70.42958956619168021 ) ) ;
#5644=CARTESIAN_POINT ( 'NONE',  ( 36.29569395875881099, -10.30384086642191832, 72.77780686321129622 ) ) ;
#5646=CARTESIAN_POINT ( 'NONE',  ( 39.38009889167650357, -16.21368208888610596, 72.75271321436731853 ) ) ;
#5652=CARTESIAN_POINT ( 'NONE',  ( 40.52078840805428683, -18.61368208888610098, 70.60699637195608602 ) ) ;
#5663=CARTESIAN_POINT ( 'NONE',  ( 37.25260217561390874, -10.00384086642191406, 70.97781676520604321 ) ) ;
#5664=CARTESIAN_POINT ( 'NONE',  ( 39.51027997493896748, -28.51368208888610667, 71.32335560751960202 ) ) ;
#5672=CARTESIAN_POINT ( 'NONE',  ( 40.77203464402485622, -27.10384086642191903, 71.43714994484031422 ) ) ;
#5675=CARTESIAN_POINT ( 'NONE',  ( 37.31647492878122563, -27.31368208888610027, 70.72433947564853440 ) ) ;
#5676=CARTESIAN_POINT ( 'NONE',  ( 36.89935272106204422, -3.213682088886101962, 69.52238214136768590 ) ) ;
#5679=CARTESIAN_POINT ( 'NONE',  ( 38.73920764526923932, -7.503840866421911393, 70.26206559358664094 ) ) ;
#5685=CARTESIAN_POINT ( 'NONE',  ( 36.98690846071097127, -9.803840866421911215, 69.45876917294177133 ) ) ;
#5688=CARTESIAN_POINT ( 'NONE',  ( 39.98359781491296161, -16.41368208888610525, 71.86517103874047052 ) ) ;
#5694=CARTESIAN_POINT ( 'NONE',  ( 39.29254315202757653, -0.8038408664219134359, 72.81632618279323310 ) ) ;
#5695=PRODUCT_CONTEXT ( 'NONE', #10953, 'mechanical' ) ;
#5699=CARTESIAN_POINT ( 'NONE',  ( 39.82603832034400426, -18.31368208888610738, 72.40698646996133903 ) ) ;
#5704=CARTESIAN_POINT ( 'NONE',  ( 37.33957961208645315, -17.80384086642190766, 69.94417936956672577 ) ) ;
#5706=CARTESIAN_POINT ( 'NONE',  ( 37.33957961208646736, -19.81368208888611093, 72.81632618279321889 ) ) ;
#5708=CARTESIAN_POINT ( 'NONE',  ( 39.64521430340304420, -22.81368208888610383, 69.45876917294175712 ) ) ;
#5712=CARTESIAN_POINT ( 'NONE',  ( 39.41296390513587511, -27.20384086642191690, 71.08074471024438878 ) ) ;
#5716=CARTESIAN_POINT ( 'NONE',  ( 39.59505955540748801, -28.75102279782487358, 70.48438567037749181 ) ) ;
#5719=CARTESIAN_POINT ( 'NONE',  ( 38.37017380507018771, 0.3961591335780931256, 69.64448340153880679 ) ) ;
#5722=CARTESIAN_POINT ( 'NONE',  ( 39.73277004305198545, -4.213682088886105959, 73.23812341099225875 ) ) ;
#5729=CARTESIAN_POINT ( 'NONE',  ( 39.82603832034401137, -27.30384086642190766, 70.35351908239857721 ) ) ;
#5737=CARTESIAN_POINT ( 'NONE',  ( 37.25260217561390874, -4.003840866421911393, 70.97781676520604321 ) ) ;
#5745=CARTESIAN_POINT ( 'NONE',  ( 38.93987200065208754, -12.81368208888610383, 70.42958956619168021 ) ) ;
#5746=CARTESIAN_POINT ( 'NONE',  ( 38.73920764526925353, -12.11368208888610098, 72.49843995877330372 ) ) ;
#5754=CARTESIAN_POINT ( 'NONE',  ( 39.98359781491296161, -15.20384086642191157, 70.89533451361945993 ) ) ;
#5757=CARTESIAN_POINT ( 'NONE',  ( 37.38336156205274818, -21.71368208888610241, 72.12822762946750288 ) ) ;
#5762=CARTESIAN_POINT ( 'NONE',  ( 39.98359781491296161, -12.41368208888610525, 71.86517103874047052 ) ) ;
#5776=CARTESIAN_POINT ( 'NONE',  ( 37.61123632939164452, -7.703840866421914235, 69.02690120949094421 ) ) ;
#5781=CARTESIAN_POINT ( 'NONE',  ( 38.26194895904383486, -13.01368208888610134, 69.64448340153877837 ) ) ;
#5786=CARTESIAN_POINT ( 'NONE',  ( 36.89935272106204422, -19.21368208888609885, 69.52238214136768590 ) ) ;
#5800=CARTESIAN_POINT ( 'NONE',  ( 37.21915885897815457, -14.20384086642191335, 71.67976084211552745 ) ) ;
#5801=CARTESIAN_POINT ( 'NONE',  ( 36.49096545463212493, 0.4863179111138959954, 71.43714994484035685 ) ) ;
#5808=CARTESIAN_POINT ( 'NONE',  ( 38.26194895904384907, -0.6038408664219147015, 73.11602215082118050 ) ) ;
#5810=CARTESIAN_POINT ( 'NONE',  ( 38.63098279924288647, -24.91368208888610170, 70.22690120949089021 ) ) ;
#5811=CARTESIAN_POINT ( 'NONE',  ( 40.33642880535524000, -4.313682088886108268, 72.77780686321128201 ) ) ;
#5815=CARTESIAN_POINT ( 'NONE',  ( 39.31564783533279694, -3.303840866421912548, 70.72433947564853440 ) ) ;
#5820=CARTESIAN_POINT ( 'NONE',  ( 40.26954217208372455, -10.90384086642191974, 72.86986841596736042 ) ) ;
#5822=CARTESIAN_POINT ( 'NONE',  ( 39.38009889167650357, -14.21368208888610773, 72.75271321436731853 ) ) ;
#5827=CARTESIAN_POINT ( 'NONE',  ( 38.37017380507018771, -1.603840866421908595, 69.64448340153879258 ) ) ;
#5830=CARTESIAN_POINT ( 'NONE',  ( 37.69796330110504101, -19.11368208888610098, 69.66206559358661821 ) ) ;
#5833=CARTESIAN_POINT ( 'NONE',  ( 39.98359781491296161, -19.20384086642191335, 70.89533451361945993 ) ) ;
#5835=CARTESIAN_POINT ( 'NONE',  ( 37.25202387243752611, -19.21368208888610241, 70.00779233799262613 ) ) ;
#5837=CARTESIAN_POINT ( 'NONE',  ( 38.26194895904383486, -19.01368208888609956, 69.04448340153878405 ) ) ;
#5841=CARTESIAN_POINT ( 'NONE',  ( 38.63098279924290068, -22.70384086642191335, 72.53360434286904024 ) ) ;
#5848=CARTESIAN_POINT ( 'NONE',  ( 39.82603832034400426, -1.303840866421906997, 70.35351908239857721 ) ) ;
#5852=CARTESIAN_POINT ( 'NONE',  ( 36.36258059203031934, 0.2863179111138938193, 72.86986841596736042 ) ) ;
#5862=CARTESIAN_POINT ( 'NONE',  ( 36.68196826583682935, -22.00384086642191406, 70.79240656858107172 ) ) ;
#5869=CARTESIAN_POINT ( 'NONE',  ( 37.12184278917507640, -4.103840866421911038, 71.32335560751961623 ) ) ;
#5876=CARTESIAN_POINT ( 'NONE',  ( 38.26194895904383486, -13.01368208888610312, 70.24448340153875847 ) ) ;
#5877=CARTESIAN_POINT ( 'NONE',  ( 39.02742774030102879, -12.21368208888610063, 72.26730301774234988 ) ) ;
#5884=CARTESIAN_POINT ( 'NONE',  ( 37.25202387243754032, -20.40384086642191619, 72.75271321436731853 ) ) ;
#5889=CARTESIAN_POINT ( 'NONE',  ( 39.31564783533280405, -18.31368208888610027, 72.03616607671141026 ) ) ;
#5893=CARTESIAN_POINT ( 'NONE',  ( 38.26194895904383486, -11.01368208888609956, 69.64448340153879258 ) ) ;
#5908=CARTESIAN_POINT ( 'NONE',  ( 36.89935272106205133, -6.403840866421917077, 73.23812341099225875 ) ) ;
#5911=CARTESIAN_POINT ( 'NONE',  ( 36.80608444377001121, -15.31368208888610383, 70.35351908239857721 ) ) ;
#5917=CARTESIAN_POINT ( 'NONE',  ( 39.12911128074873801, -12.11368208888610987, 73.69843995877327814 ) ) ;
#5927=CARTESIAN_POINT ( 'NONE',  ( 39.37952058850012804, -11.00384086642191050, 71.78268878715392987 ) ) ;
#5928=CARTESIAN_POINT ( 'NONE',  ( 37.69796330110504101, -1.113682088886101207, 69.66206559358663242 ) ) ;
#5935=CARTESIAN_POINT ( 'NONE',  ( 38.82593461698265003, 1.296159133578084210, 73.13360434286906298 ) ) ;
#5936=CARTESIAN_POINT ( 'NONE',  ( 37.25260217561390874, -25.61368208888610098, 71.78268878715390144 ) ) ;
#5937=CARTESIAN_POINT ( 'NONE',  ( 40.55423172469004811, -2.413682088886103472, 72.05058123536544201 ) ) ;
#5940=CARTESIAN_POINT ( 'NONE',  ( 39.82603832034400426, -29.30384086642190766, 70.35351908239857721 ) ) ;
#5947=CARTESIAN_POINT ( 'NONE',  ( 40.77203464402485622, -9.103840866421915479, 71.43714994484034264 ) ) ;
#5953=CARTESIAN_POINT ( 'NONE',  ( 38.93415946300897446, -12.11368208888610276, 73.09843995877329803 ) ) ;
#5956=CARTESIAN_POINT ( 'NONE',  ( 39.38009889167650357, -26.21368208888610951, 72.75271321436730432 ) ) ;
#5959=CARTESIAN_POINT ( 'NONE',  ( 39.95015449827720744, 0.9961591335780894951, 71.96809898377890136 ) ) ;
#5962=CARTESIAN_POINT ( 'NONE',  ( 39.75915168707250302, -18.71368208888610241, 70.26145752964251301 ) ) ;
#5964=CARTESIAN_POINT ( 'NONE',  ( 37.25202387243754032, -16.40384086642191619, 72.75271321436731853 ) ) ;
#5967=CARTESIAN_POINT ( 'NONE',  ( 38.93415946300897446, -10.11368208888610987, 73.09843995877331224 ) ) ;
#5969=CARTESIAN_POINT ( 'NONE',  ( 36.29569395875879678, -23.31368208888610383, 69.98269868914866265 ) ) ;
#5973=CARTESIAN_POINT ( 'NONE',  ( 39.51027997493896748, -17.10384086642191193, 71.43714994484032843 ) ) ;
#5980=CARTESIAN_POINT ( 'NONE',  ( 38.26194895904384907, 1.396159133578083633, 73.11602215082119471 ) ) ;
#5982=CARTESIAN_POINT ( 'NONE',  ( 36.89935272106204422, -3.213682088886101962, 69.52238214136768590 ) ) ;
#5990=CARTESIAN_POINT ( 'NONE',  ( 39.82603832034401137, -23.30384086642190766, 70.35351908239857721 ) ) ;
#5997=CARTESIAN_POINT ( 'NONE',  ( 39.24876120206129571, -4.903840866421912636, 72.12822762946750288 ) ) ;
#6005=CARTESIAN_POINT ( 'NONE',  ( 39.51027997493896748, -10.51368208888610134, 71.32335560751961623 ) ) ;
#6006=CARTESIAN_POINT ( 'NONE',  ( 39.02742774030102879, -10.21368208888610241, 72.26730301774236409 ) ) ;
#6013=CARTESIAN_POINT ( 'NONE',  ( 36.64852494920107517, -16.20384086642190979, 71.86517103874048473 ) ) ;
#6016=CARTESIAN_POINT ( 'NONE',  ( 38.00113996487114321, -15.91368208888609992, 72.53360434286904024 ) ) ;
#6020=CARTESIAN_POINT ( 'NONE',  ( 39.82603832034401847, -14.31368208888610738, 72.40698646996131060 ) ) ;
#6025=CARTESIAN_POINT ( 'NONE',  ( 40.07112981125872864, -29.10876147765398869, 71.40768163349989095 ) ) ;
#6036=CARTESIAN_POINT ( 'NONE',  ( 38.37017380507018771, -3.603840866421911038, 69.04448340153881247 ) ) ;
#6039=CARTESIAN_POINT ( 'NONE',  ( 38.82593461698262871, -6.913682088886100807, 69.62690120949091011 ) ) ;
#6043=CARTESIAN_POINT ( 'NONE',  ( 40.52078840805428683, -16.61368208888610454, 70.60699637195608602 ) ) ;
#6054=CARTESIAN_POINT ( 'NONE',  ( 38.00113996487114321, -25.91368208888609814, 72.53360434286901182 ) ) ;
#6060=CARTESIAN_POINT ( 'NONE',  ( 36.98690846071097127, -21.80384086642191122, 69.45876917294175712 ) ) ;
#6061=CARTESIAN_POINT ( 'NONE',  ( 39.37952058850012804, -24.61368208888610454, 70.97781676520600058 ) ) ;
#6062=CARTESIAN_POINT ( 'NONE',  ( 40.14115730948191185, -24.51368208888609601, 71.32335560751958781 ) ) ;
#6065=CARTESIAN_POINT ( 'NONE',  ( 39.37952058850012804, 0.9961591335780894951, 71.78268878715394408 ) ) ;
#6073=CARTESIAN_POINT ( 'NONE',  ( 40.55423172469004101, -5.203840866421914235, 70.70992431699450265 ) ) ;
#6076=CARTESIAN_POINT ( 'NONE',  ( 37.25202387243752611, -5.213682088886100630, 70.00779233799264034 ) ) ;
#6078=CARTESIAN_POINT ( 'NONE',  ( 37.80618814713140097, -27.91368208888610880, 73.13360434286902034 ) ) ;
#6080=CARTESIAN_POINT ( 'NONE',  ( 38.37017380507018771, -3.603840866421907041, 69.64448340153879258 ) ) ;
#6084=CARTESIAN_POINT ( 'NONE',  ( 39.38009889167650357, -10.21368208888610773, 72.75271321436733274 ) ) ;
#6088=CARTESIAN_POINT ( 'NONE',  ( 36.68196826583682935, -12.00384086642191228, 70.79240656858107172 ) ) ;
#6091=CARTESIAN_POINT ( 'NONE',  ( 38.26194895904383486, -11.01368208888609956, 69.64448340153879258 ) ) ;
#6093=CARTESIAN_POINT ( 'NONE',  ( 36.89935272106204422, -19.21368208888609885, 69.52238214136768590 ) ) ;
#6096=CARTESIAN_POINT ( 'NONE',  ( 39.24876120206129571, -20.90384086642191264, 72.12822762946747446 ) ) ;
#6102=CARTESIAN_POINT ( 'NONE',  ( 40.33642880535521869, -21.30384086642190766, 69.98269868914866265 ) ) ;
#6105=CARTESIAN_POINT ( 'NONE',  ( 36.89935272106204422, 0.7863179111138978161, 69.52238214136768590 ) ) ;
#6111=CARTESIAN_POINT ( 'NONE',  ( 39.82603832034401137, -19.30384086642190411, 70.35351908239857721 ) ) ;
#6116=EDGE_CURVE ( 'NONE', #25416, #2631, #8284, .T. ) ;
#6121=CARTESIAN_POINT ( 'NONE',  ( 38.63098279924290068, -6.703840866421912459, 72.53360434286905445 ) ) ;
#6131=CARTESIAN_POINT ( 'NONE',  ( 38.63098279924288647, -6.913682088886101695, 70.22690120949091863 ) ) ;
#6132=CARTESIAN_POINT ( 'NONE',  ( 39.02742774030102879, -2.213682088886101518, 72.26730301774236409 ) ) ;
#6138=CARTESIAN_POINT ( 'NONE',  ( 39.82603832034400426, -19.30384086642190056, 70.35351908239857721 ) ) ;
#6148=CARTESIAN_POINT ( 'NONE',  ( 38.93415946300898867, -12.11368208888610631, 73.09843995877329803 ) ) ;
#6162=CARTESIAN_POINT ( 'NONE',  ( 40.26954217208372455, -6.903840866421917966, 72.86986841596736042 ) ) ;
#6165=CARTESIAN_POINT ( 'NONE',  ( 37.69796330110504101, -9.113682088886100985, 69.66206559358663242 ) ) ;
#6169=CARTESIAN_POINT ( 'NONE',  ( 38.26194895904383486, -15.01368208888610134, 69.04448340153878405 ) ) ;
#6184=CARTESIAN_POINT ( 'NONE',  ( 37.12184278917507640, -23.51368208888609956, 71.43714994484032843 ) ) ;
#6194=CARTESIAN_POINT ( 'NONE',  ( 36.07789103942399578, -22.20384086642191690, 72.05058123536544201 ) ) ;
#6195=CARTESIAN_POINT ( 'NONE',  ( 39.82603832034400426, -26.31368208888611093, 72.40698646996131060 ) ) ;
#6201=CARTESIAN_POINT ( 'NONE',  ( 40.26954217208372455, -0.9038408664219198529, 72.86986841596736042 ) ) ;
#6203=CARTESIAN_POINT ( 'NONE',  ( 39.98359781491296161, -8.413682088886105248, 71.86517103874048473 ) ) ;
#6205=CIRCLE ( 'NONE', #7438, 0.2999999999999938827 ) ;
#6206=CARTESIAN_POINT ( 'NONE',  ( 40.14115730948191185, -26.51368208888610667, 71.32335560751960202 ) ) ;
#6209=CARTESIAN_POINT ( 'NONE',  ( 38.93415946300897446, -3.503840866421906952, 69.66206559358664663 ) ) ;
#6211=CARTESIAN_POINT ( 'NONE',  ( 39.51027997493896748, -25.10384086642191193, 71.43714994484031422 ) ) ;
#6212=CARTESIAN_POINT ( 'NONE',  ( 38.26194895904383486, -9.013682088886101340, 69.64448340153879258 ) ) ;
#6215=CARTESIAN_POINT ( 'NONE',  ( 36.49096545463212493, -14.10384086642191015, 71.32335560751961623 ) ) ;
#6218=CARTESIAN_POINT ( 'NONE',  ( 39.75915168707250302, -14.71368208888610063, 70.26145752964251301 ) ) ;
#6220=CARTESIAN_POINT ( 'NONE',  ( 36.07789103942398867, -17.41368208888610525, 70.70992431699450265 ) ) ;
#6225=CARTESIAN_POINT ( 'NONE',  ( 37.25260217561390874, -20.00384086642191406, 70.97781676520601479 ) ) ;
#6230=CARTESIAN_POINT ( 'NONE',  ( 40.55423172469004101, -21.20384086642191690, 70.70992431699450265 ) ) ;
#6232=CARTESIAN_POINT ( 'NONE',  ( 38.93415946300897446, -24.11368208888610454, 73.09843995877328382 ) ) ;
#6239=CARTESIAN_POINT ( 'NONE',  ( 39.29254315202757653, -22.80384086642191477, 72.81632618279321889 ) ) ;
#6245=CARTESIAN_POINT ( 'NONE',  ( 38.26194895904384197, 1.396159133578087186, 72.51602215082118619 ) ) ;
#6253=CARTESIAN_POINT ( 'NONE',  ( 39.24876120206128860, -4.713682088886099741, 70.63227792289247020 ) ) ;
#6254=CARTESIAN_POINT ( 'NONE',  ( 39.41296390513587511, -4.413682088886102584, 71.67976084211552745 ) ) ;
#6262=CARTESIAN_POINT ( 'NONE',  ( 36.87297107704149823, -9.903840866421901978, 70.26145752964255564 ) ) ;
#6276=CARTESIAN_POINT ( 'NONE',  ( 36.87297107704153376, -7.713682088886109511, 72.49904802271743165 ) ) ;
#6291=CARTESIAN_POINT ( 'NONE',  ( 40.55423172469004101, -7.203840866421916900, 70.70992431699450265 ) ) ;
#6296=CARTESIAN_POINT ( 'NONE',  ( 38.37017380507020192, -6.013682088886109334, 73.11602215082118050 ) ) ;
#6300=CARTESIAN_POINT ( 'NONE',  ( 38.37017380507020192, -18.01368208888610667, 73.71602215082113219 ) ) ;
#6304=DIRECTION ( 'NONE',  ( 0.000000000000000000, -1.632680918566405215E-15, 1.000000000000000000 ) ) ;
#6312=CARTESIAN_POINT ( 'NONE',  ( 39.51027997493896748, -22.51368208888609246, 71.32335560751960202 ) ) ;
#6318=CARTESIAN_POINT ( 'NONE',  ( 39.64521430340305841, -20.80384086642191832, 73.30173637941818754 ) ) ;
#6321=CARTESIAN_POINT ( 'NONE',  ( 40.14115730948191185, -26.51368208888610667, 71.32335560751958781 ) ) ;
#6329=CARTESIAN_POINT ( 'NONE',  ( 39.64521430340305841, -4.803840866421917433, 73.30173637941818754 ) ) ;
#6333=CARTESIAN_POINT ( 'NONE',  ( 36.49096545463212493, -5.513682088886105781, 71.43714994484035685 ) ) ;
#6335=CARTESIAN_POINT ( 'NONE',  ( 38.37017380507020192, -28.01368208888610667, 73.11602215082115208 ) ) ;
#6342=CARTESIAN_POINT ( 'NONE',  ( 38.26194895904384197, -28.60384086642191193, 72.51602215082114355 ) ) ;
#6343=CARTESIAN_POINT ( 'NONE',  ( 36.87297107704152666, -13.71368208888610773, 72.49904802271740323 ) ) ;
#6346=CARTESIAN_POINT ( 'NONE',  ( 39.95015449827720744, -9.003840866421912281, 71.96809898377888715 ) ) ;
#6351=CARTESIAN_POINT ( 'NONE',  ( 38.82593461698262871, -12.91368208888610347, 69.62690120949091011 ) ) ;
#6353=CARTESIAN_POINT ( 'NONE',  ( 39.64521430340304420, -16.81368208888610383, 69.45876917294175712 ) ) ;
#6359=CARTESIAN_POINT ( 'NONE',  ( 37.69225076346193504, -19.80384086642191477, 70.42958956619168021 ) ) ;
#6364=CARTESIAN_POINT ( 'NONE',  ( 36.36258059203030513, -23.90384086642191619, 69.89063713639258424 ) ) ;
#6366=CARTESIAN_POINT ( 'NONE',  ( 39.12911128074873801, 1.886317911113891244, 73.69843995877330656 ) ) ;
#6373=CARTESIAN_POINT ( 'NONE',  ( 37.69796330110505522, -14.50384086642191583, 73.09843995877329803 ) ) ;
#6379=CARTESIAN_POINT ( 'NONE',  ( 38.37017380507018771, 0.3961591335780896284, 70.24448340153880110 ) ) ;
#6382=CARTESIAN_POINT ( 'NONE',  ( 39.95015449827720744, -28.61368208888610454, 70.79240656858104330 ) ) ;
#6387=CARTESIAN_POINT ( 'NONE',  ( 39.37952058850012804, -4.613682088886100985, 70.97781676520601479 ) ) ;
#6388=CARTESIAN_POINT ( 'NONE',  ( 37.25260217561390874, -7.613682088886100985, 71.78268878715394408 ) ) ;
#6395=CARTESIAN_POINT ( 'NONE',  ( 39.29254315202757653, -12.80384086642191299, 72.81632618279321889 ) ) ;
#6405=CARTESIAN_POINT ( 'NONE',  ( 39.82603832034401847, -8.313682088886109156, 72.40698646996133903 ) ) ;
#6420=CARTESIAN_POINT ( 'NONE',  ( 38.26194895904384197, -2.603840866421920364, 73.71602215082116061 ) ) ;
#6424=CARTESIAN_POINT ( 'NONE',  ( 39.29254315202756231, -6.813682088886101162, 69.94417936956673998 ) ) ;
#6427=CARTESIAN_POINT ( 'NONE',  ( 39.12911128074873801, -14.11368208888610987, 73.69843995877327814 ) ) ;
#6435=CARTESIAN_POINT ( 'NONE',  ( 39.02742774030102879, -24.21368208888609885, 72.26730301774232146 ) ) ;
#6441=CARTESIAN_POINT ( 'NONE',  ( 36.98690846071097127, -23.80384086642191477, 69.45876917294174291 ) ) ;
#6444=CARTESIAN_POINT ( 'NONE',  ( 40.26954217208371034, 1.286317911113898260, 69.89063713639259845 ) ) ;
#6451=CARTESIAN_POINT ( 'NONE',  ( 39.02088643472237806, -4.703840866421917788, 73.73360434286902887 ) ) ;
#6454=CARTESIAN_POINT ( 'NONE',  ( 39.95015449827720744, -8.613682088886104538, 70.79240656858107172 ) ) ;
#6456=CARTESIAN_POINT ( 'NONE',  ( 38.26194895904383486, -27.01368208888610312, 69.64448340153876416 ) ) ;
#6460=CARTESIAN_POINT ( 'NONE',  ( 37.89291511884479036, -28.50384086642191406, 72.49843995877328950 ) ) ;
#6461=CARTESIAN_POINT ( 'NONE',  ( 36.80608444377001121, -15.31368208888610383, 70.35351908239857721 ) ) ;
#6462=ORIENTED_EDGE ( 'NONE', *, *, #2155, .T. ) ;
#6466=CARTESIAN_POINT ( 'NONE',  ( 39.98359781491296161, -11.20384086642191335, 70.89533451361947414 ) ) ;
#6469=CARTESIAN_POINT ( 'NONE',  ( 37.80618814713140097, -3.913682088886108801, 73.13360434286904876 ) ) ;
#6471=CARTESIAN_POINT ( 'NONE',  ( 36.29569395875879678, -17.31368208888610383, 69.98269868914867686 ) ) ;
#6475=CARTESIAN_POINT ( 'NONE',  ( 37.25260217561390874, -18.00384086642191050, 70.97781676520601479 ) ) ;
#6480=CARTESIAN_POINT ( 'NONE',  ( 36.11133435605973574, -24.00384086642191761, 70.60699637195608602 ) ) ;
#6482=CARTESIAN_POINT ( 'NONE',  ( 39.98359781491296161, -24.41368208888610525, 71.86517103874045631 ) ) ;
#6492=CARTESIAN_POINT ( 'NONE',  ( 38.26194895904384907, -12.60384086642191548, 73.11602215082116629 ) ) ;
#6496=CARTESIAN_POINT ( 'NONE',  ( 37.31647492878124694, -0.3038408664219096056, 72.03616607671141026 ) ) ;
#6506=CARTESIAN_POINT ( 'NONE',  ( 38.00113996487114321, -3.913682088886100807, 72.53360434286905445 ) ) ;
#6508=CARTESIAN_POINT ( 'NONE',  ( 38.63098279924288647, -2.913682088886100363, 70.22690120949091863 ) ) ;
#6514=CARTESIAN_POINT ( 'NONE',  ( 38.26194895904384907, -8.603840866421915479, 73.11602215082118050 ) ) ;
#6522=CARTESIAN_POINT ( 'NONE',  ( 36.87297107704153376, -5.713682088886106847, 72.49904802271743165 ) ) ;
#6523=CARTESIAN_POINT ( 'NONE',  ( 40.05245289102396100, -29.10876147765230115, 71.40796565871902146 ) ) ;
#6526=CARTESIAN_POINT ( 'NONE',  ( 40.11557105022964720, -29.10876147765400646, 71.37118765889773897 ) ) ;
#6535=CARTESIAN_POINT ( 'NONE',  ( 40.52078840805429394, -1.003840866421915612, 72.15350918040385864 ) ) ;
#6537=CARTESIAN_POINT ( 'NONE',  ( 39.02742774030102879, -22.21368208888610241, 72.26730301774234988 ) ) ;
#6541=CARTESIAN_POINT ( 'NONE',  ( 36.80608444377001121, -5.313682088886100274, 70.35351908239860563 ) ) ;
#6542=CARTESIAN_POINT ( 'NONE',  ( 36.68196826583682935, -28.00384086642191050, 70.79240656858105751 ) ) ;
#6545=CARTESIAN_POINT ( 'NONE',  ( 36.07789103942398867, -11.41368208888610525, 70.70992431699450265 ) ) ;
#6561=CARTESIAN_POINT ( 'NONE',  ( 36.36258059203030513, -25.90384086642191264, 69.89063713639258424 ) ) ;
#6563=CARTESIAN_POINT ( 'NONE',  ( 36.68196826583682935, -25.61368208888610454, 71.96809898377887293 ) ) ;
#6570=CARTESIAN_POINT ( 'NONE',  ( 40.26954217208372455, -2.903840866421918410, 72.86986841596736042 ) ) ;
#6574=CARTESIAN_POINT ( 'NONE',  ( 36.80608444377001121, -7.313682088886100274, 70.35351908239860563 ) ) ;
#6577=CARTESIAN_POINT ( 'NONE',  ( 39.29254315202756231, -22.81368208888610027, 69.94417936956672577 ) ) ;
#6585=CARTESIAN_POINT ( 'NONE',  ( 39.51027997493896748, -27.10384086642191903, 71.43714994484031422 ) ) ;
#6586=CARTESIAN_POINT ( 'NONE',  ( 36.64852494920107517, -11.41368208888610525, 70.89533451361947414 ) ) ;
#6591=CARTESIAN_POINT ( 'NONE',  ( 37.69796330110505522, -12.50384086642191228, 73.09843995877329803 ) ) ;
#6593=CARTESIAN_POINT ( 'NONE',  ( 37.25202387243752611, -5.213682088886100630, 70.00779233799264034 ) ) ;
#6595=CARTESIAN_POINT ( 'NONE',  ( 39.02088643472237095, -18.91368208888609814, 69.02690120949091579 ) ) ;
#6599=CARTESIAN_POINT ( 'NONE',  ( 38.93987200065210175, -8.803840866421911215, 72.33091598616827866 ) ) ;
#6604=CARTESIAN_POINT ( 'NONE',  ( 37.61123632939164452, -23.70384086642191335, 69.02690120949091579 ) ) ;
#6607=CARTESIAN_POINT ( 'NONE',  ( 38.93415946300897446, -26.11368208888610098, 73.09843995877328382 ) ) ;
#6613=CARTESIAN_POINT ( 'NONE',  ( 37.80618814713138676, -15.70384086642190979, 69.62690120949091011 ) ) ;
#6620=CARTESIAN_POINT ( 'NONE',  ( 37.25202387243754032, -28.40384086642191619, 72.75271321436730432 ) ) ;
#6623=CARTESIAN_POINT ( 'NONE',  ( 37.33957961208646736, -27.81368208888611093, 72.81632618279320468 ) ) ;
#6629=CARTESIAN_POINT ( 'NONE',  ( 38.63098279924288647, -4.913682088886102584, 70.22690120949091863 ) ) ;
#6630=CARTESIAN_POINT ( 'NONE',  ( 38.26194895904383486, -7.013682088886100452, 70.24448340153877268 ) ) ;
#6637=CARTESIAN_POINT ( 'NONE',  ( 39.95015449827720744, -9.003840866421912281, 71.96809898377888715 ) ) ;
#6645=CARTESIAN_POINT ( 'NONE',  ( 36.80608444377001121, -5.313682088886100274, 70.35351908239861984 ) ) ;
#6658=CARTESIAN_POINT ( 'NONE',  ( 40.55423172469004811, -28.41368208888610525, 72.05058123536539938 ) ) ;
#6660=CARTESIAN_POINT ( 'NONE',  ( 39.37952058850012804, -22.61368208888610454, 70.97781676520601479 ) ) ;
#6665=CARTESIAN_POINT ( 'NONE',  ( 39.75915168707250302, -2.713682088886101962, 70.26145752964252722 ) ) ;
#6666=CARTESIAN_POINT ( 'NONE',  ( 37.38336156205273397, -1.903840866421910638, 70.63227792289248441 ) ) ;
#6668=CARTESIAN_POINT ( 'NONE',  ( 36.36258059203031934, -7.713682088886110400, 72.86986841596736042 ) ) ;
#6685=CARTESIAN_POINT ( 'NONE',  ( 37.50301148336529877, -14.50384086642191761, 73.69843995877327814 ) ) ;
#6686=CARTESIAN_POINT ( 'NONE',  ( 39.38009889167650357, -24.21368208888610596, 72.75271321436730432 ) ) ;
#6695=CARTESIAN_POINT ( 'NONE',  ( 36.29569395875879678, -27.31368208888610027, 69.98269868914866265 ) ) ;
#6699=CARTESIAN_POINT ( 'NONE',  ( 38.82593461698262871, -2.913682088886099919, 69.62690120949091011 ) ) ;
#6703=CARTESIAN_POINT ( 'NONE',  ( 36.80608444377001121, -23.31368208888610383, 70.35351908239857721 ) ) ;
#6708=CARTESIAN_POINT ( 'NONE',  ( 39.31564783533279694, -25.30384086642191477, 70.72433947564850598 ) ) ;
#6709=CARTESIAN_POINT ( 'NONE',  ( 39.75915168707250302, -8.713682088886097077, 70.26145752964252722 ) ) ;
#6713=CARTESIAN_POINT ( 'NONE',  ( 36.64852494920107517, -6.203840866421912459, 71.86517103874049894 ) ) ;
#6718=CARTESIAN_POINT ( 'NONE',  ( 37.80618814713140097, -7.913682088886107913, 73.13360434286904876 ) ) ;
#6720=CARTESIAN_POINT ( 'NONE',  ( 36.36258059203031934, -17.71368208888610596, 72.86986841596736042 ) ) ;
#6725=CARTESIAN_POINT ( 'NONE',  ( 37.38336156205273397, -13.90384086642191264, 70.63227792289247020 ) ) ;
#6733=CARTESIAN_POINT ( 'NONE',  ( 40.77203464402485622, -15.10384086642191548, 71.43714994484032843 ) ) ;
#6737=CARTESIAN_POINT ( 'NONE',  ( 36.49096545463212493, -27.51368208888610312, 71.43714994484030001 ) ) ;
#6746=CARTESIAN_POINT ( 'NONE',  ( 36.80608444377002542, -16.30384086642191477, 72.40698646996133903 ) ) ;
#6752=CARTESIAN_POINT ( 'NONE',  ( 39.02742774030101458, 0.5961591335780883627, 70.49320253461762320 ) ) ;
#6756=CARTESIAN_POINT ( 'NONE',  ( 39.95015449827720744, -24.61368208888610454, 70.79240656858104330 ) ) ;
#6761=CARTESIAN_POINT ( 'NONE',  ( 37.60469502381300089, -1.213682088886100630, 70.49320253461759478 ) ) ;
#6763=CARTESIAN_POINT ( 'NONE',  ( 38.26194895904383486, 0.9863179111139001032, 70.24448340153880110 ) ) ;
#6770=CARTESIAN_POINT ( 'NONE',  ( 39.95015449827720744, -5.003840866421912281, 71.96809898377888715 ) ) ;
#6780=CARTESIAN_POINT ( 'NONE',  ( 38.26194895904383486, -5.013682088886102228, 69.64448340153879258 ) ) ;
#6793=CARTESIAN_POINT ( 'NONE',  ( 38.37017380507020192, -26.01368208888611022, 73.71602215082113219 ) ) ;
#6795=CARTESIAN_POINT ( 'NONE',  ( 37.25260217561390874, -15.61368208888610276, 71.78268878715392987 ) ) ;
#6799=CARTESIAN_POINT ( 'NONE',  ( 36.87297107704152666, -1.713682088886108179, 72.49904802271743165 ) ) ;
#6800=CARTESIAN_POINT ( 'NONE',  ( 37.31647492878124694, -0.3038408664219096056, 72.03616607671141026 ) ) ;
#6802=CARTESIAN_POINT ( 'NONE',  ( 36.07789103942398867, -9.413682088886105248, 70.70992431699450265 ) ) ;
#6819=CARTESIAN_POINT ( 'NONE',  ( 36.36258059203030513, -17.90384086642190908, 69.89063713639259845 ) ) ;
#6820=CARTESIAN_POINT ( 'NONE',  ( 37.69796330110504101, -21.11368208888610454, 69.66206559358661821 ) ) ;
#6825=DIRECTION ( 'NONE',  ( 0.1803747433772529551, 0.9835979625596985576, 0.000000000000000000 ) ) ;
#6826=CARTESIAN_POINT ( 'NONE',  ( 36.89935272106205133, -0.4038408664219194089, 73.23812341099225875 ) ) ;
#6830=CARTESIAN_POINT ( 'NONE',  ( 39.38009889167650357, -0.2136820888861065693, 72.75271321436733274 ) ) ;
#6832=CARTESIAN_POINT ( 'NONE',  ( 37.69796330110504101, -21.11368208888610098, 69.66206559358663242 ) ) ;
#6835=CARTESIAN_POINT ( 'NONE',  ( 37.25260217561390874, -16.00384086642191050, 70.97781676520601479 ) ) ;
#6836=CARTESIAN_POINT ( 'NONE',  ( 36.49096545463212493, -3.513682088886103116, 71.43714994484035685 ) ) ;
#6839=CARTESIAN_POINT ( 'NONE',  ( 38.26194895904384907, -6.603840866421916367, 73.11602215082118050 ) ) ;
#6842=CARTESIAN_POINT ( 'NONE',  ( 39.95015449827720744, -4.613682088886104538, 70.79240656858107172 ) ) ;
#6844=CARTESIAN_POINT ( 'NONE',  ( 37.50301148336529167, -11.11368208888610276, 69.06206559358666652 ) ) ;
#6847=CARTESIAN_POINT ( 'NONE',  ( 37.12184278917507640, -12.10384086642191193, 71.32335560751961623 ) ) ;
#6852=CARTESIAN_POINT ( 'NONE',  ( 40.55423172469004101, -17.20384086642191335, 70.70992431699450265 ) ) ;
#6854=( LENGTH_UNIT ( ) NAMED_UNIT ( * ) SI_UNIT ( .MILLI., .METRE. ) );
#6855=CARTESIAN_POINT ( 'NONE',  ( 39.95015449827720744, -18.61368208888610454, 70.79240656858105751 ) ) ;
#6863=CARTESIAN_POINT ( 'NONE',  ( 36.87297107704151244, -17.90384086642190553, 70.26145752964255564 ) ) ;
#6868=CARTESIAN_POINT ( 'NONE',  ( 36.80608444377001121, -25.31368208888610383, 70.35351908239857721 ) ) ;
#6872=CARTESIAN_POINT ( 'NONE',  ( 38.82593461698265003, -24.70384086642191690, 73.13360434286902034 ) ) ;
#6876=CARTESIAN_POINT ( 'NONE',  ( 38.93415946300897446, -22.11368208888610454, 73.09843995877329803 ) ) ;
#6881=CARTESIAN_POINT ( 'NONE',  ( 39.37952058850012804, -0.6136820888861006518, 70.97781676520601479 ) ) ;
#6882=CARTESIAN_POINT ( 'NONE',  ( 39.24876120206129571, -28.90384086642191264, 72.12822762946746025 ) ) ;
#6889=CARTESIAN_POINT ( 'NONE',  ( 39.38009889167648936, -1.403840866421906419, 70.00779233799264034 ) ) ;
#6901=CARTESIAN_POINT ( 'NONE',  ( 39.95015449827720744, -0.6136820888861040935, 70.79240656858107172 ) ) ;
#6920=CARTESIAN_POINT ( 'NONE',  ( 39.24876120206128860, -18.71368208888610241, 70.63227792289245599 ) ) ;
#6925=CARTESIAN_POINT ( 'NONE',  ( 36.64852494920107517, -1.413682088886102806, 70.89533451361948835 ) ) ;
#6926=CARTESIAN_POINT ( 'NONE',  ( 36.68196826583682935, -22.00384086642191406, 70.79240656858107172 ) ) ;
#6929=CARTESIAN_POINT ( 'NONE',  ( 36.11133435605973574, -11.61368208888610454, 72.15350918040385864 ) ) ;
#6944=CARTESIAN_POINT ( 'NONE',  ( 35.86008812008917346, -14.10384086642191548, 71.32335560751961623 ) ) ;
#6946=CARTESIAN_POINT ( 'NONE',  ( 39.95015449827720744, -22.61368208888610809, 70.79240656858105751 ) ) ;
#6952=SHAPE_REPRESENTATION_RELATIONSHIP ( 'NONE' , 'NONE' ,  #24379, #8595 ) ;
#6956=CARTESIAN_POINT ( 'NONE',  ( 38.37017380507020192, -26.01368208888611022, 73.71602215082113219 ) ) ;
#6961=CARTESIAN_POINT ( 'NONE',  ( 37.25202387243752611, -1.213682088886100630, 70.00779233799264034 ) ) ;
#6963=CARTESIAN_POINT ( 'NONE',  ( 38.26194895904383486, -23.01368208888609956, 69.64448340153877837 ) ) ;
#6968=CARTESIAN_POINT ( 'NONE',  ( 38.00113996487112189, -21.70384086642190979, 70.22690120949090442 ) ) ;
#6969=CARTESIAN_POINT ( 'NONE',  ( 37.25202387243752611, -7.213682088886102406, 70.00779233799264034 ) ) ;
#6974=CARTESIAN_POINT ( 'NONE',  ( 38.37017380507018771, -5.603840866421908373, 69.64448340153879258 ) ) ;
#6976=CARTESIAN_POINT ( 'NONE',  ( 38.37017380507020192, -4.013682088886107557, 73.11602215082118050 ) ) ;
#6978=CARTESIAN_POINT ( 'NONE',  ( 38.37017380507020192, -10.01368208888611022, 73.71602215082116061 ) ) ;
#6982=CARTESIAN_POINT ( 'NONE',  ( 39.02742774030101458, -9.403840866421907307, 70.49320253461759478 ) ) ;
#6988=CARTESIAN_POINT ( 'NONE',  ( 36.98690846071097127, -13.80384086642191122, 69.45876917294175712 ) ) ;
#6990=CARTESIAN_POINT ( 'NONE',  ( 39.75915168707250302, -22.71368208888610241, 70.26145752964251301 ) ) ;
#6998=CARTESIAN_POINT ( 'NONE',  ( 38.93415946300897446, -7.503840866421907840, 69.66206559358664663 ) ) ;
#7001=CARTESIAN_POINT ( 'NONE',  ( 39.29254315202756231, -26.81368208888610027, 69.94417936956671156 ) ) ;
#7004=CARTESIAN_POINT ( 'NONE',  ( 38.37017380507018771, -25.60384086642190837, 69.64448340153876416 ) ) ;
#7005=PLANE ( 'NONE',  #13064 ) ;
#7006=CARTESIAN_POINT ( 'NONE',  ( 39.82603832034400426, -22.31368208888610738, 72.40698646996133903 ) ) ;
#7012=CARTESIAN_POINT ( 'NONE',  ( 38.93987200065210175, -28.80384086642191477, 72.33091598616823603 ) ) ;
#7013=CARTESIAN_POINT ( 'NONE',  ( 39.24876120206128860, 1.286317911113898260, 70.63227792289248441 ) ) ;
#7020=CARTESIAN_POINT ( 'NONE',  ( 36.80608444377001831, -6.303840866421912104, 72.40698646996136745 ) ) ;
#7028=CARTESIAN_POINT ( 'NONE',  ( 39.95015449827720744, -2.613682088886105870, 70.79240656858107172 ) ) ;
#7045=CARTESIAN_POINT ( 'NONE',  ( 39.24876120206128860, -16.71368208888610241, 70.63227792289245599 ) ) ;
#7049=CARTESIAN_POINT ( 'NONE',  ( 38.26194895904383486, -3.013682088886100008, 69.64448340153879258 ) ) ;
#7050=CARTESIAN_POINT ( 'NONE',  ( 39.75915168707251723, -26.90384086642191619, 72.49904802271737481 ) ) ;
#7055=CARTESIAN_POINT ( 'NONE',  ( 36.98690846071097837, -7.813682088886109156, 73.30173637941818754 ) ) ;
#7072=CARTESIAN_POINT ( 'NONE',  ( 35.86008812008917346, -20.10384086642191548, 71.32335560751961623 ) ) ;
#7073=CARTESIAN_POINT ( 'NONE',  ( 38.82593461698262871, -22.91368208888609459, 69.62690120949091011 ) ) ;
#7080=CARTESIAN_POINT ( 'NONE',  ( 36.11133435605973574, -25.61368208888610454, 72.15350918040381600 ) ) ;
#7086=CARTESIAN_POINT ( 'NONE',  ( 39.95015449827720744, -0.6136820888861040935, 70.79240656858107172 ) ) ;
#7090=CARTESIAN_POINT ( 'NONE',  ( 36.80608444377001121, -19.31368208888610027, 70.35351908239860563 ) ) ;
#7093=CARTESIAN_POINT ( 'NONE',  ( 38.63098279924290068, -16.70384086642190624, 72.53360434286904024 ) ) ;
#7094=CARTESIAN_POINT ( 'NONE',  ( 39.29254315202756231, -6.813682088886101162, 69.94417936956673998 ) ) ;
#7101=CARTESIAN_POINT ( 'NONE',  ( 38.93415946300896024, -7.503840866421907840, 69.66206559358663242 ) ) ;
#7104=CARTESIAN_POINT ( 'NONE',  ( 38.37017380507020192, -0.01368208888610777940, 73.11602215082118050 ) ) ;
#7106=CARTESIAN_POINT ( 'NONE',  ( 36.36258059203031934, -9.713682088886105959, 72.86986841596736042 ) ) ;
#7109=CARTESIAN_POINT ( 'NONE',  ( 39.02742774030101458, -13.40384086642191619, 70.49320253461759478 ) ) ;
#7115=CARTESIAN_POINT ( 'NONE',  ( 36.11133435605973574, -16.00384086642191406, 70.60699637195608602 ) ) ;
#7119=CARTESIAN_POINT ( 'NONE',  ( 36.80608444377001121, -23.31368208888610383, 70.35351908239857721 ) ) ;
#7128=CARTESIAN_POINT ( 'NONE',  ( 39.75915168707251723, -10.90384086642191441, 72.49904802271740323 ) ) ;
#7131=CARTESIAN_POINT ( 'NONE',  ( 38.37017380507020192, -22.01368208888611022, 73.11602215082116629 ) ) ;
#7136=CARTESIAN_POINT ( 'NONE',  ( 36.49096545463212493, -22.10384086642191548, 71.32335560751961623 ) ) ;
#7138=CARTESIAN_POINT ( 'NONE',  ( 39.38009889167650357, -22.21368208888610951, 72.75271321436731853 ) ) ;
#7144=CARTESIAN_POINT ( 'NONE',  ( 37.89291511884476904, -1.113682088886101207, 70.26206559358664094 ) ) ;
#7153=CARTESIAN_POINT ( 'NONE',  ( 39.95015449827720744, -3.003840866421910505, 71.96809898377888715 ) ) ;
#7161=CARTESIAN_POINT ( 'NONE',  ( 39.38009889167650357, -0.2136820888861065693, 72.75271321436733274 ) ) ;
#7170=AXIS2_PLACEMENT_3D ( 'NONE', #12639, #22541, #6825 ) ;
#7179=CARTESIAN_POINT ( 'NONE',  ( 36.64852494920107517, -0.2038408664219101829, 71.86517103874049894 ) ) ;
#7180=CARTESIAN_POINT ( 'NONE',  ( 39.02742774030102879, -18.21368208888610241, 72.26730301774234988 ) ) ;
#7185=CARTESIAN_POINT ( 'NONE',  ( 37.33957961208646736, -1.813682088886107380, 72.81632618279323310 ) ) ;
#7186=CARTESIAN_POINT ( 'NONE',  ( 38.26194895904384907, -24.60384086642191548, 73.11602215082115208 ) ) ;
#7190=CARTESIAN_POINT ( 'NONE',  ( 40.55423172469004811, -2.413682088886103472, 72.05058123536544201 ) ) ;
#7209=CARTESIAN_POINT ( 'NONE',  ( 36.98690846071097127, -17.80384086642191122, 69.45876917294175712 ) ) ;
#7212=CARTESIAN_POINT ( 'NONE',  ( 39.38009889167650357, -18.21368208888610951, 72.75271321436731853 ) ) ;
#7216=CARTESIAN_POINT ( 'NONE',  ( 37.61123632939165873, -21.91368208888611235, 73.73360434286898624 ) ) ;
#7220=CARTESIAN_POINT ( 'NONE',  ( 36.80608444377001121, 0.6863179111138983934, 70.35351908239860563 ) ) ;
#7222=CARTESIAN_POINT ( 'NONE',  ( 36.68196826583682935, -13.61368208888610454, 71.96809898377888715 ) ) ;
#7226=CARTESIAN_POINT ( 'NONE',  ( 37.21915885897815457, -20.20384086642191335, 71.67976084211552745 ) ) ;
#7227=CARTESIAN_POINT ( 'NONE',  ( 39.75915168707250302, -2.713682088886101962, 70.26145752964252722 ) ) ;
#7232=CARTESIAN_POINT ( 'NONE',  ( 36.64852494920107517, -4.203840866421910683, 71.86517103874049894 ) ) ;
#7235=CARTESIAN_POINT ( 'NONE',  ( 39.95015449827720744, -0.6136820888861040935, 70.79240656858107172 ) ) ;
#7237=CARTESIAN_POINT ( 'NONE',  ( 35.86008812008917346, -11.51368208888610134, 71.43714994484034264 ) ) ;
#7240=CARTESIAN_POINT ( 'NONE',  ( 38.26194895904384197, -4.603840866421910150, 72.51602215082118619 ) ) ;
#7245=CARTESIAN_POINT ( 'NONE',  ( 40.26954217208372455, -18.90384086642191619, 72.86986841596734621 ) ) ;
#7247=CARTESIAN_POINT ( 'NONE',  ( 39.95015449827720744, -22.61368208888610809, 70.79240656858105751 ) ) ;
#7255=CARTESIAN_POINT ( 'NONE',  ( 36.68196826583682935, -10.00384086642191406, 70.79240656858108593 ) ) ;
#7257=CARTESIAN_POINT ( 'NONE',  ( 37.80618814713140097, -27.91368208888610880, 73.13360434286902034 ) ) ;
#7259=CARTESIAN_POINT ( 'NONE',  ( 39.75915168707251723, -24.90384086642191619, 72.49904802271737481 ) ) ;
#7261=CARTESIAN_POINT ( 'NONE',  ( 39.75915168707250302, -20.71368208888610596, 70.26145752964251301 ) ) ;
#7263=CARTESIAN_POINT ( 'NONE',  ( 36.11133435605973574, -25.61368208888610454, 72.15350918040381600 ) ) ;
#7267=CARTESIAN_POINT ( 'NONE',  ( 39.31564783533280405, -0.3136820888861025503, 72.03616607671141026 ) ) ;
#7274=CARTESIAN_POINT ( 'NONE',  ( 36.80608444377001831, -4.303840866421916544, 72.40698646996136745 ) ) ;
#7286=CARTESIAN_POINT ( 'NONE',  ( 36.80608444377001121, 0.6863179111138983934, 70.35351908239861984 ) ) ;
#7288=CARTESIAN_POINT ( 'NONE',  ( 38.26194895904384907, -26.60384086642191548, 73.11602215082115208 ) ) ;
#7304=CARTESIAN_POINT ( 'NONE',  ( 37.21915885897815457, -17.41368208888610170, 71.08074471024443142 ) ) ;
#7309=CARTESIAN_POINT ( 'NONE',  ( 39.98359781491296161, -25.20384086642191335, 70.89533451361944572 ) ) ;
#7311=CARTESIAN_POINT ( 'NONE',  ( 39.02088643472237095, -0.9136820888861024725, 69.02690120949094421 ) ) ;
#7329=CARTESIAN_POINT ( 'NONE',  ( 36.98690846071097127, -9.803840866421911215, 69.45876917294177133 ) ) ;
#7331=CARTESIAN_POINT ( 'NONE',  ( 37.80618814713140097, -15.91368208888610880, 73.13360434286903455 ) ) ;
#7338=CARTESIAN_POINT ( 'NONE',  ( 36.07789103942398867, -21.41368208888610880, 70.70992431699450265 ) ) ;
#7348=CARTESIAN_POINT ( 'NONE',  ( 38.37017380507018771, -21.60384086642191548, 70.24448340153875847 ) ) ;
#7349=CARTESIAN_POINT ( 'NONE',  ( 38.26194895904383486, 0.9863179111138999922, 69.64448340153880679 ) ) ;
#7356=CARTESIAN_POINT ( 'NONE',  ( 36.87297107704149823, -1.903840866421906419, 70.26145752964255564 ) ) ;
#7358=CARTESIAN_POINT ( 'NONE',  ( 39.75915168707250302, -0.7136820888860997414, 70.26145752964252722 ) ) ;
#7359=CARTESIAN_POINT ( 'NONE',  ( 39.73277004305198545, -12.21368208888610951, 73.23812341099225875 ) ) ;
#7362=CARTESIAN_POINT ( 'NONE',  ( 37.89291511884479036, -4.503840866421912281, 72.49843995877331793 ) ) ;
#7370=CARTESIAN_POINT ( 'NONE',  ( 40.26954217208372455, -6.903840866421917966, 72.86986841596736042 ) ) ;
#7378=CARTESIAN_POINT ( 'NONE',  ( 37.25202387243752611, -19.21368208888610241, 70.00779233799262613 ) ) ;
#7385=CARTESIAN_POINT ( 'NONE',  ( 36.68196826583682935, -6.003840866421913169, 70.79240656858108593 ) ) ;
#7390=CARTESIAN_POINT ( 'NONE',  ( 37.80618814713140097, -21.91368208888610880, 73.13360434286903455 ) ) ;
#7392=CARTESIAN_POINT ( 'NONE',  ( 39.95015449827720744, -27.00384086642191050, 71.96809898377885872 ) ) ;
#7396=CARTESIAN_POINT ( 'NONE',  ( 39.75915168707250302, -18.71368208888610241, 70.26145752964251301 ) ) ;
#7398=CARTESIAN_POINT ( 'NONE',  ( 39.64521430340305841, 1.196159133578081457, 73.30173637941821596 ) ) ;
#7402=CARTESIAN_POINT ( 'NONE',  ( 37.25260217561390874, -24.00384086642191761, 70.97781676520601479 ) ) ;
#7410=CARTESIAN_POINT ( 'NONE',  ( 38.37017380507018771, -27.60384086642191548, 69.04448340153878405 ) ) ;
#7417=CARTESIAN_POINT ( 'NONE',  ( 36.49096545463212493, -3.513682088886103561, 71.43714994484035685 ) ) ;
#7418=CARTESIAN_POINT ( 'NONE',  ( 36.80608444377002542, -26.30384086642191477, 72.40698646996131060 ) ) ;
#7431=CARTESIAN_POINT ( 'NONE',  ( 39.51027997493896748, -14.51368208888610134, 71.32335560751960202 ) ) ;
#7432=CARTESIAN_POINT ( 'NONE',  ( 39.41296390513587511, -12.41368208888609992, 71.67976084211551324 ) ) ;
#7437=CARTESIAN_POINT ( 'NONE',  ( 36.80608444377001831, -26.30384086642191477, 72.40698646996133903 ) ) ;
#7438=AXIS2_PLACEMENT_3D ( 'NONE', #8508, #22028, #8255 ) ;
#7440=CARTESIAN_POINT ( 'NONE',  ( 39.31564783533280405, -20.31368208888610027, 72.03616607671141026 ) ) ;
#7456=ORIENTED_EDGE ( 'NONE', *, *, #18801, .T. ) ;
#7458=CARTESIAN_POINT ( 'NONE',  ( 36.11133435605973574, -12.00384086642191583, 70.60699637195608602 ) ) ;
#7460=CARTESIAN_POINT ( 'NONE',  ( 37.25202387243752611, -13.21368208888610063, 70.00779233799262613 ) ) ;
#7466=CARTESIAN_POINT ( 'NONE',  ( 36.36258059203031934, -23.71368208888610951, 72.86986841596734621 ) ) ;
#7474=CARTESIAN_POINT ( 'NONE',  ( 37.60469502381300799, -10.40384086642191086, 72.26730301774236409 ) ) ;
#7475=CARTESIAN_POINT ( 'NONE',  ( 39.98359781491296161, 1.586317911113896528, 71.86517103874049894 ) ) ;
#7481=CARTESIAN_POINT ( 'NONE',  ( 39.12911128074872380, -27.50384086642191406, 69.06206559358663810 ) ) ;
#7482=CARTESIAN_POINT ( 'NONE',  ( 39.95015449827720744, 1.386317911113894130, 70.79240656858108593 ) ) ;
#7483=CARTESIAN_POINT ( 'NONE',  ( 38.37017380507020192, -2.013682088886109334, 73.71602215082116061 ) ) ;
#7488=CARTESIAN_POINT ( 'NONE',  ( 37.60469502381300799, -4.403840866421911748, 72.26730301774236409 ) ) ;
#7495=CARTESIAN_POINT ( 'NONE',  ( 40.77203464402485622, -11.10384086642191193, 71.43714994484034264 ) ) ;
#7498=CARTESIAN_POINT ( 'NONE',  ( 40.14115730948191185, -14.51368208888610667, 71.32335560751960202 ) ) ;
#7503=CARTESIAN_POINT ( 'NONE',  ( 39.82603832034401137, -5.303840866421906775, 70.35351908239860563 ) ) ;
#7508=CARTESIAN_POINT ( 'NONE',  ( 39.82603832034400426, -16.31368208888610738, 72.40698646996133903 ) ) ;
#7514=CARTESIAN_POINT ( 'NONE',  ( 39.38009889167648936, -19.40384086642190908, 70.00779233799262613 ) ) ;
#7518=CARTESIAN_POINT ( 'NONE',  ( 37.80618814713140097, -15.91368208888610880, 73.13360434286903455 ) ) ;
#7520=CARTESIAN_POINT ( 'NONE',  ( 40.77203464402485622, -24.51368208888610667, 71.32335560751960202 ) ) ;
#7526=CARTESIAN_POINT ( 'NONE',  ( 39.02742774030101458, -23.40384086642191264, 70.49320253461759478 ) ) ;
#7535=CARTESIAN_POINT ( 'NONE',  ( 38.26194895904384907, -0.6038408664219147015, 73.11602215082118050 ) ) ;
#7546=CARTESIAN_POINT ( 'NONE',  ( 37.80618814713138676, -27.70384086642190624, 69.62690120949091011 ) ) ;
#7555=CARTESIAN_POINT ( 'NONE',  ( 38.37017380507018771, -5.603840866421911926, 70.24448340153877268 ) ) ;
#7563=CARTESIAN_POINT ( 'NONE',  ( 37.21915885897815457, -11.41368208888610170, 71.08074471024443142 ) ) ;
#7564=CARTESIAN_POINT ( 'NONE',  ( 39.41296390513587511, -10.41368208888610170, 71.67976084211552745 ) ) ;
#7571=CARTESIAN_POINT ( 'NONE',  ( 37.33957961208645315, -19.80384086642191122, 69.94417936956672577 ) ) ;
#7574=CARTESIAN_POINT ( 'NONE',  ( 37.12184278917507640, -15.51368208888610312, 71.43714994484034264 ) ) ;
#7593=CARTESIAN_POINT ( 'NONE',  ( 40.33642880535521869, -11.30384086642191299, 69.98269868914867686 ) ) ;
#7596=CARTESIAN_POINT ( 'NONE',  ( 37.25202387243752611, -17.21368208888610241, 70.00779233799262613 ) ) ;
#7600=CARTESIAN_POINT ( 'NONE',  ( 38.26194895904383486, -19.01368208888609956, 69.04448340153878405 ) ) ;
#7611=CARTESIAN_POINT ( 'NONE',  ( 38.00113996487112189, -11.70384086642191335, 70.22690120949091863 ) ) ;
#7612=CARTESIAN_POINT ( 'NONE',  ( 38.93987200065208754, -28.81368208888610383, 70.42958956619166599 ) ) ;
#7619=CARTESIAN_POINT ( 'NONE',  ( 39.73277004305197124, -27.40384086642191619, 69.52238214136765748 ) ) ;
#7620=CARTESIAN_POINT ( 'NONE',  ( 37.21915885897815457, -27.41368208888609814, 71.08074471024441721 ) ) ;
#7621=CARTESIAN_POINT ( 'NONE',  ( 38.26194895904383486, -3.013682088886100008, 69.04448340153881247 ) ) ;
#7624=CARTESIAN_POINT ( 'NONE',  ( 38.37017380507018771, -5.603840866421911926, 70.24448340153877268 ) ) ;
#7630=CARTESIAN_POINT ( 'NONE',  ( 36.98690846071097127, -7.803840866421912104, 69.45876917294177133 ) ) ;
#7633=CARTESIAN_POINT ( 'NONE',  ( 38.82593461698262871, -12.91368208888610347, 69.62690120949091011 ) ) ;
#7638=CARTESIAN_POINT ( 'NONE',  ( 37.25202387243754032, -4.403840866421916189, 72.75271321436733274 ) ) ;
#7642=CARTESIAN_POINT ( 'NONE',  ( 39.38009889167650357, -18.21368208888610951, 72.75271321436731853 ) ) ;
#7645=CARTESIAN_POINT ( 'NONE',  ( 39.82603832034400426, -19.30384086642190056, 70.35351908239857721 ) ) ;
#7647=CARTESIAN_POINT ( 'NONE',  ( 36.87297107704152666, -15.71368208888610596, 72.49904802271740323 ) ) ;
#7649=CARTESIAN_POINT ( 'NONE',  ( 40.77203464402485622, -20.51368208888610667, 71.32335560751960202 ) ) ;
#7653=CARTESIAN_POINT ( 'NONE',  ( 37.69225076346193504, -21.80384086642191122, 70.42958956619168021 ) ) ;
#7656=CARTESIAN_POINT ( 'NONE',  ( 39.59167754530926686, -28.73258042513078436, 70.34536827862072528 ) ) ;
#7659=CARTESIAN_POINT ( 'NONE',  ( 40.26954217208372455, -28.90384086642191619, 72.86986841596730358 ) ) ;
#7669=CARTESIAN_POINT ( 'NONE',  ( 38.93415946300897446, -27.50384086642190340, 69.66206559358661821 ) ) ;
#7677=CARTESIAN_POINT ( 'NONE',  ( 39.51027997493896748, -9.103840866421911926, 71.43714994484034264 ) ) ;
#7683=CARTESIAN_POINT ( 'NONE',  ( 39.02742774030102879, -10.21368208888610241, 72.26730301774236409 ) ) ;
#7684=CARTESIAN_POINT ( 'NONE',  ( 37.21915885897815457, -13.41368208888610170, 71.08074471024443142 ) ) ;
#7690=CARTESIAN_POINT ( 'NONE',  ( 37.80618814713138676, -15.70384086642191157, 69.62690120949091011 ) ) ;
#7694=CARTESIAN_POINT ( 'NONE',  ( 37.69225076346193504, -21.81368208888610027, 72.33091598616826445 ) ) ;
#7700=CARTESIAN_POINT ( 'NONE',  ( 38.93415946300898867, -14.11368208888610809, 73.09843995877329803 ) ) ;
#7714=CARTESIAN_POINT ( 'NONE',  ( 37.50301148336529877, -10.50384086642191761, 73.69843995877330656 ) ) ;
#7718=CARTESIAN_POINT ( 'NONE',  ( 37.33957961208646736, -17.81368208888611093, 72.81632618279321889 ) ) ;
#7722=CARTESIAN_POINT ( 'NONE',  ( 36.36258059203031934, -19.71368208888610951, 72.86986841596736042 ) ) ;
#7732=CARTESIAN_POINT ( 'NONE',  ( 39.41296390513587511, -13.20384086642191157, 71.08074471024441721 ) ) ;
#7733=CARTESIAN_POINT ( 'NONE',  ( 37.80618814713140097, 0.08631791111389161553, 73.13360434286904876 ) ) ;
#7741=CARTESIAN_POINT ( 'NONE',  ( 39.64521430340305841, -28.80384086642192187, 73.30173637941817333 ) ) ;
#7746=CARTESIAN_POINT ( 'NONE',  ( 38.00113996487114321, -25.91368208888609814, 72.53360434286901182 ) ) ;
#7747=CARTESIAN_POINT ( 'NONE',  ( 36.98690846071097837, -1.813682088886107602, 73.30173637941818754 ) ) ;
#7750=CARTESIAN_POINT ( 'NONE',  ( 38.93987200065210175, -4.803840866421909439, 72.33091598616827866 ) ) ;
#7755=CARTESIAN_POINT ( 'NONE',  ( 36.07789103942399578, -12.20384086642191512, 72.05058123536544201 ) ) ;
#7758=CARTESIAN_POINT ( 'NONE',  ( 39.29254315202756231, -14.81368208888610205, 69.94417936956672577 ) ) ;
#7763=CARTESIAN_POINT ( 'NONE',  ( 38.26194895904384907, -2.603840866421916367, 73.11602215082118050 ) ) ;
#7768=CARTESIAN_POINT ( 'NONE',  ( 38.93415946300897446, -18.11368208888611164, 73.09843995877329803 ) ) ;
#7772=CARTESIAN_POINT ( 'NONE',  ( 40.14115730948191185, -15.10384086642190837, 71.43714994484030001 ) ) ;
#7775=CARTESIAN_POINT ( 'NONE',  ( 39.82603832034400426, -20.31368208888610738, 72.40698646996133903 ) ) ;
#7777=CARTESIAN_POINT ( 'NONE',  ( 37.61123632939165873, -23.91368208888611235, 73.73360434286898624 ) ) ;
#7782=CARTESIAN_POINT ( 'NONE',  ( 37.89291511884479036, -24.50384086642190695, 72.49843995877328950 ) ) ;
#7787=CARTESIAN_POINT ( 'NONE',  ( 37.61123632939164452, -27.70384086642191690, 69.02690120949091579 ) ) ;
#7790=CARTESIAN_POINT ( 'NONE',  ( 38.37017380507020192, -0.01368208888610778114, 73.71602215082116061 ) ) ;
#7797=CARTESIAN_POINT ( 'NONE',  ( 37.25202387243754032, -18.40384086642191974, 72.75271321436731853 ) ) ;
#7805=CARTESIAN_POINT ( 'NONE',  ( 37.12184278917507640, -8.103840866421910150, 71.32335560751961623 ) ) ;
#7813=CARTESIAN_POINT ( 'NONE',  ( 37.25260217561390874, -11.61368208888610098, 71.78268878715392987 ) ) ;
#7814=CARTESIAN_POINT ( 'NONE',  ( 39.02742774030102879, -14.21368208888610241, 72.26730301774234988 ) ) ;
#7821=CARTESIAN_POINT ( 'NONE',  ( 37.33957961208645315, -15.80384086642190589, 69.94417936956672577 ) ) ;
#7825=CARTESIAN_POINT ( 'NONE',  ( 38.63098279924288647, -18.91368208888609814, 70.22690120949090442 ) ) ;
#7829=CARTESIAN_POINT ( 'NONE',  ( 40.14115730948191185, -12.51368208888610489, 71.32335560751960202 ) ) ;
#7845=CARTESIAN_POINT ( 'NONE',  ( 39.73277004305197124, -13.40384086642191619, 69.52238214136768590 ) ) ;
#7851=CARTESIAN_POINT ( 'NONE',  ( 38.26194895904383486, -17.01368208888610312, 69.64448340153877837 ) ) ;
#7857=CARTESIAN_POINT ( 'NONE',  ( 36.89935272106204422, -13.21368208888610241, 69.52238214136768590 ) ) ;
#7867=CARTESIAN_POINT ( 'NONE',  ( 39.41296390513587511, -11.20384086642191335, 71.08074471024443142 ) ) ;
#7868=CARTESIAN_POINT ( 'NONE',  ( 39.82603832034400426, 1.686317911113891732, 72.40698646996136745 ) ) ;
#7874=CARTESIAN_POINT ( 'NONE',  ( 37.33957961208645315, -1.803840866421907441, 69.94417936956673998 ) ) ;
#7875=CARTESIAN_POINT ( 'NONE',  ( 37.38336156205274818, -23.71368208888610241, 72.12822762946747446 ) ) ;
#7877=CARTESIAN_POINT ( 'NONE',  ( 37.50301148336529167, -3.113682088886100097, 69.06206559358666652 ) ) ;
#7880=CARTESIAN_POINT ( 'NONE',  ( 39.98359781491296161, -27.20384086642191335, 70.89533451361944572 ) ) ;
#7885=CARTESIAN_POINT ( 'NONE',  ( 36.29569395875881099, -10.30384086642191832, 72.77780686321129622 ) ) ;
#7888=CARTESIAN_POINT ( 'NONE',  ( 39.95015449827720744, -16.61368208888610454, 70.79240656858105751 ) ) ;
#7891=CARTESIAN_POINT ( 'NONE',  ( 37.69796330110504101, -25.11368208888609743, 69.66206559358661821 ) ) ;
#7894=CARTESIAN_POINT ( 'NONE',  ( 36.80608444377002542, -0.3038408664219130473, 72.40698646996135324 ) ) ;
#7898=CARTESIAN_POINT ( 'NONE',  ( 38.93415946300897446, -20.11368208888610809, 73.09843995877329803 ) ) ;
#7900=CARTESIAN_POINT ( 'NONE',  ( 37.25202387243754032, -20.40384086642191619, 72.75271321436731853 ) ) ;
#7903=CARTESIAN_POINT ( 'NONE',  ( 39.82603832034400426, -10.31368208888610383, 72.40698646996135324 ) ) ;
#7905=CARTESIAN_POINT ( 'NONE',  ( 39.64521430340304420, -24.81368208888610738, 69.45876917294174291 ) ) ;
#7909=CARTESIAN_POINT ( 'NONE',  ( 38.93987200065210175, -24.80384086642191477, 72.33091598616823603 ) ) ;
#7914=CARTESIAN_POINT ( 'NONE',  ( 36.49096545463212493, -0.1038408664219107880, 71.32335560751963044 ) ) ;
#7916=CARTESIAN_POINT ( 'NONE',  ( 40.26954217208371034, -2.713682088886101962, 69.89063713639259845 ) ) ;
#7928=CARTESIAN_POINT ( 'NONE',  ( 38.26194895904384907, -22.60384086642191548, 73.11602215082116629 ) ) ;
#7936=CARTESIAN_POINT ( 'NONE',  ( 39.24876120206129571, -6.903840866421912636, 72.12822762946750288 ) ) ;
#7945=CARTESIAN_POINT ( 'NONE',  ( 37.89291511884476904, -11.11368208888610276, 70.26206559358664094 ) ) ;
#7946=CARTESIAN_POINT ( 'NONE',  ( 38.93987200065208754, -10.81368208888610027, 70.42958956619168021 ) ) ;
#7954=CARTESIAN_POINT ( 'NONE',  ( 38.82593461698265003, -16.70384086642191690, 73.13360434286903455 ) ) ;
#7958=CARTESIAN_POINT ( 'NONE',  ( 39.02742774030102879, -16.21368208888609885, 72.26730301774234988 ) ) ;
#7962=CARTESIAN_POINT ( 'NONE',  ( 38.82593461698262871, -16.91368208888609814, 69.62690120949091011 ) ) ;
#7967=CARTESIAN_POINT ( 'NONE',  ( 39.38009889167650357, -28.21368208888610951, 72.75271321436730432 ) ) ;
#7977=CARTESIAN_POINT ( 'NONE',  ( 39.02088643472237806, -6.703840866421919564, 73.73360434286902887 ) ) ;
#7981=CARTESIAN_POINT ( 'NONE',  ( 39.98359781491296161, -8.413682088886105248, 71.86517103874048473 ) ) ;
#7986=CARTESIAN_POINT ( 'NONE',  ( 38.37017380507020192, -16.01368208888610667, 73.71602215082113219 ) ) ;
#7996=CARTESIAN_POINT ( 'NONE',  ( 38.00113996487112189, -13.70384086642191157, 70.22690120949090442 ) ) ;
#7997=CARTESIAN_POINT ( 'NONE',  ( 39.41296390513587511, -22.41368208888610525, 71.67976084211551324 ) ) ;
#8005=CARTESIAN_POINT ( 'NONE',  ( 37.61123632939164452, -21.70384086642190979, 69.02690120949091579 ) ) ;
#8006=CARTESIAN_POINT ( 'NONE',  ( 38.63098279924288647, -26.91368208888610170, 70.22690120949089021 ) ) ;
#8007=CARTESIAN_POINT ( 'NONE',  ( 35.86008812008917346, -3.513682088886104005, 71.43714994484035685 ) ) ;
#8010=CARTESIAN_POINT ( 'NONE',  ( 37.69225076346193504, -1.803840866421911215, 70.42958956619168021 ) ) ;
#8015=CARTESIAN_POINT ( 'NONE',  ( 40.26954217208372455, -4.903840866421919742, 72.86986841596736042 ) ) ;
#8019=CARTESIAN_POINT ( 'NONE',  ( 36.68196826583682935, -5.613682088886105426, 71.96809898377890136 ) ) ;
#8022=CARTESIAN_POINT ( 'NONE',  ( 36.80608444377001121, -27.31368208888610383, 70.35351908239857721 ) ) ;
#8025=CARTESIAN_POINT ( 'NONE',  ( 39.75915168707251723, -2.903840866421914413, 72.49904802271740323 ) ) ;
#8027=CARTESIAN_POINT ( 'NONE',  ( 36.64852494920107517, -17.41368208888610525, 70.89533451361947414 ) ) ;
#8031=CARTESIAN_POINT ( 'NONE',  ( 37.80618814713138676, -11.70384086642190624, 69.62690120949091011 ) ) ;
#8032=CARTESIAN_POINT ( 'NONE',  ( 39.75915168707250302, -10.71368208888609885, 70.26145752964252722 ) ) ;
#8034=CARTESIAN_POINT ( 'NONE',  ( 40.77203464402485622, -22.51368208888610667, 71.32335560751960202 ) ) ;
#8038=CARTESIAN_POINT ( 'NONE',  ( 39.02742774030101458, -15.40384086642191441, 70.49320253461759478 ) ) ;
#8044=CARTESIAN_POINT ( 'NONE',  ( 39.02088643472237806, -20.70384086642192401, 73.73360434286898624 ) ) ;
#8046=CARTESIAN_POINT ( 'NONE',  ( 40.33642880535524000, -4.313682088886108268, 72.77780686321128201 ) ) ;
#8052=CARTESIAN_POINT ( 'NONE',  ( 38.93415946300897446, -19.50384086642190695, 69.66206559358663242 ) ) ;
#8059=CARTESIAN_POINT ( 'NONE',  ( 38.26194895904384197, -6.603840866421913702, 72.51602215082118619 ) ) ;
#8067=CARTESIAN_POINT ( 'NONE',  ( 37.89291511884476904, -3.113682088886100097, 70.26206559358664094 ) ) ;
#8069=CARTESIAN_POINT ( 'NONE',  ( 38.26194895904383486, -3.013682088886100008, 70.24448340153877268 ) ) ;
#8077=CARTESIAN_POINT ( 'NONE',  ( 39.38009889167648936, -15.40384086642190908, 70.00779233799262613 ) ) ;
#8084=CARTESIAN_POINT ( 'NONE',  ( 39.98359781491296161, -16.41368208888610525, 71.86517103874047052 ) ) ;
#8090=PRODUCT_DEFINITION_SHAPE ( 'NONE', 'NONE',  #11212 ) ;
#8097=CARTESIAN_POINT ( 'NONE',  ( 37.61123632939164452, -5.703840866421911571, 69.02690120949094421 ) ) ;
#8100=CARTESIAN_POINT ( 'NONE',  ( 36.64852494920107517, -7.413682088886104360, 70.89533451361948835 ) ) ;
#8103=CARTESIAN_POINT ( 'NONE',  ( 39.73277004305198545, -14.21368208888610951, 73.23812341099225875 ) ) ;
#8114=CARTESIAN_POINT ( 'NONE',  ( 37.38336156205274818, -23.71368208888610241, 72.12822762946747446 ) ) ;
#8120=CARTESIAN_POINT ( 'NONE',  ( 36.36258059203030513, -23.90384086642191619, 69.89063713639258424 ) ) ;
#8121=CARTESIAN_POINT ( 'NONE',  ( 39.95015449827720744, -26.61368208888610809, 70.79240656858104330 ) ) ;
#8130=CARTESIAN_POINT ( 'NONE',  ( 38.37017380507018771, -1.603840866421912148, 69.04448340153881247 ) ) ;
#8133=CARTESIAN_POINT ( 'NONE',  ( 40.14115730948191185, -4.513682088886103116, 71.32335560751961623 ) ) ;
#8137=CARTESIAN_POINT ( 'NONE',  ( 38.93415946300897446, -1.503840866421909173, 69.66206559358664663 ) ) ;
#8141=CARTESIAN_POINT ( 'NONE',  ( 37.60469502381300799, -28.40384086642191264, 72.26730301774232146 ) ) ;
#8142=CARTESIAN_POINT ( 'NONE',  ( 36.80608444377001121, -9.313682088886100274, 70.35351908239860563 ) ) ;
#8146=CARTESIAN_POINT ( 'NONE',  ( 36.49096545463212493, -10.10384086642191193, 71.32335560751963044 ) ) ;
#8150=CARTESIAN_POINT ( 'NONE',  ( 36.80608444377001121, -9.313682088886100274, 70.35351908239860563 ) ) ;
#8151=VERTEX_POINT ( 'NONE', #10451 ) ;
#8152=CARTESIAN_POINT ( 'NONE',  ( 35.86008812008917346, -17.51368208888610667, 71.43714994484034264 ) ) ;
#8157=CARTESIAN_POINT ( 'NONE',  ( 38.26194895904384197, -20.60384086642191193, 72.51602215082118619 ) ) ;
#8164=CARTESIAN_POINT ( 'NONE',  ( 38.26194895904384197, -22.60384086642191903, 73.71602215082113219 ) ) ;
#8168=CARTESIAN_POINT ( 'NONE',  ( 37.25202387243752611, -25.21368208888610241, 70.00779233799262613 ) ) ;
#8175=CARTESIAN_POINT ( 'NONE',  ( 39.95015449827720744, -21.00384086642191406, 71.96809898377887293 ) ) ;
#8181=CARTESIAN_POINT ( 'NONE',  ( 39.37952058850012804, 0.9961591335780894951, 71.78268878715394408 ) ) ;
#8190=CARTESIAN_POINT ( 'NONE',  ( 37.21915885897815457, -5.413682088886103472, 71.08074471024443142 ) ) ;
#8192=CARTESIAN_POINT ( 'NONE',  ( 37.89291511884476904, -3.113682088886100097, 70.26206559358664094 ) ) ;
#8199=CARTESIAN_POINT ( 'NONE',  ( 39.38009889167648936, -13.40384086642191086, 70.00779233799262613 ) ) ;
#8208=CARTESIAN_POINT ( 'NONE',  ( 38.93415946300898867, -6.113682088886108090, 73.09843995877331224 ) ) ;
#8223=CARTESIAN_POINT ( 'NONE',  ( 39.12911128074872380, -7.503840866421911393, 69.06206559358666652 ) ) ;
#8227=CARTESIAN_POINT ( 'NONE',  ( 39.82603832034400426, -6.313682088886107380, 72.40698646996135324 ) ) ;
#8231=CARTESIAN_POINT ( 'NONE',  ( 40.52078840805428683, -12.61368208888610454, 70.60699637195608602 ) ) ;
#8242=CARTESIAN_POINT ( 'NONE',  ( 39.02742774030102879, -22.21368208888610241, 72.26730301774234988 ) ) ;
#8251=CARTESIAN_POINT ( 'NONE',  ( 39.73277004305197124, -23.40384086642191264, 69.52238214136768590 ) ) ;
#8253=CARTESIAN_POINT ( 'NONE',  ( 36.80608444377001121, -25.31368208888610383, 70.35351908239857721 ) ) ;
#8255=DIRECTION ( 'NONE',  ( 0.1803747433772539821, 0.9835979625596982245, 0.000000000000000000 ) ) ;
#8260=CARTESIAN_POINT ( 'NONE',  ( 37.61123632939164452, -1.703840866421911571, 69.02690120949094421 ) ) ;
#8263=CARTESIAN_POINT ( 'NONE',  ( 38.93415946300897446, -10.11368208888610987, 73.09843995877331224 ) ) ;
#8267=CARTESIAN_POINT ( 'NONE',  ( 36.64852494920107517, -27.41368208888610525, 70.89533451361945993 ) ) ;
#8273=CARTESIAN_POINT ( 'NONE',  ( 37.69225076346193504, -27.80384086642191477, 70.42958956619166599 ) ) ;
#8274=CARTESIAN_POINT ( 'NONE',  ( 39.82603832034400426, -14.31368208888610916, 72.40698646996133903 ) ) ;
#8276=CARTESIAN_POINT ( 'NONE',  ( 39.38009889167648936, -13.40384086642191086, 70.00779233799262613 ) ) ;
#8279=CARTESIAN_POINT ( 'NONE',  ( 39.82603832034400426, -12.31368208888610560, 72.40698646996133903 ) ) ;
#8281=CARTESIAN_POINT ( 'NONE',  ( 36.98690846071097837, -15.81368208888610916, 73.30173637941818754 ) ) ;
#8284=B_SPLINE_CURVE_WITH_KNOTS ( 'NONE', 3,
 ( #3913, #4035, #7656, #5716, #163, #12039, #17320, #1837, #11909, #15881, #13579, #19499, #23736, #19370 ),
 .UNSPECIFIED., .F., .F.,
 ( 4, 2, 2, 2, 2, 2, 4 ),
 ( 0.0007428411354317481169, 0.0009550568131542710483, 0.001167272490876794088, 0.001273380329738076858, 0.001379488168599359195, 0.001485596007460641965, 0.001591703846321924519 ),
 .UNSPECIFIED. ) ;
#8287=CARTESIAN_POINT ( 'NONE',  ( 39.37952058850012804, -17.00384086642191406, 71.78268878715390144 ) ) ;
#8292=CARTESIAN_POINT ( 'NONE',  ( 38.37017380507018771, -23.60384086642191903, 69.04448340153878405 ) ) ;
#8294=CARTESIAN_POINT ( 'NONE',  ( 39.02088643472237095, 1.086317911113899415, 69.02690120949095842 ) ) ;
#8302=CARTESIAN_POINT ( 'NONE',  ( 39.82603832034401137, -21.30384086642191122, 70.35351908239857721 ) ) ;
#8311=CARTESIAN_POINT ( 'NONE',  ( 39.37952058850012804, -3.003840866421910505, 71.78268878715392987 ) ) ;
#8320=CARTESIAN_POINT ( 'NONE',  ( 38.37017380507020192, -4.013682088886100452, 72.51602215082118619 ) ) ;
#8321=CARTESIAN_POINT ( 'NONE',  ( 37.69225076346193504, -7.813682088886102939, 72.33091598616827866 ) ) ;
#8328=CARTESIAN_POINT ( 'NONE',  ( 38.26194895904384907, -10.60384086642191726, 73.11602215082118050 ) ) ;
#8339=CARTESIAN_POINT ( 'NONE',  ( 38.93415946300898867, -10.11368208888610987, 73.09843995877331224 ) ) ;
#8354=CARTESIAN_POINT ( 'NONE',  ( 38.26194895904384197, -4.603840866421918143, 73.71602215082116061 ) ) ;
#8358=CARTESIAN_POINT ( 'NONE',  ( 39.82603832034400426, -8.313682088886110932, 72.40698646996135324 ) ) ;
#8363=CARTESIAN_POINT ( 'NONE',  ( 35.86008812008917346, -15.51368208888610667, 71.43714994484034264 ) ) ;
#8366=DIRECTION ( 'NONE',  ( 0.000000000000000000, 1.000000000000000000, 1.632680918566405215E-15 ) ) ;
#8373=CARTESIAN_POINT ( 'NONE',  ( 38.93987200065208754, -26.81368208888610738, 70.42958956619166599 ) ) ;
#8381=CARTESIAN_POINT ( 'NONE',  ( 35.86008812008917346, -26.10384086642191903, 71.32335560751960202 ) ) ;
#8383=CARTESIAN_POINT ( 'NONE',  ( 39.02088643472237095, 1.086317911113899415, 69.02690120949095842 ) ) ;
#8393=CARTESIAN_POINT ( 'NONE',  ( 36.29569395875881099, -2.303840866421917877, 72.77780686321129622 ) ) ;
#8396=CARTESIAN_POINT ( 'NONE',  ( 38.82593461698262871, -6.913682088886100807, 69.62690120949091011 ) ) ;
#8399=CARTESIAN_POINT ( 'NONE',  ( 40.14115730948191185, -28.51368208888610667, 71.32335560751960202 ) ) ;
#8405=CARTESIAN_POINT ( 'NONE',  ( 39.37952058850012804, -23.00384086642191050, 71.78268878715390144 ) ) ;
#8406=CARTESIAN_POINT ( 'NONE',  ( 39.75915168707250302, -12.71368208888610063, 70.26145752964251301 ) ) ;
#8408=CARTESIAN_POINT ( 'NONE',  ( 39.95015449827720744, -11.00384086642191050, 71.96809898377888715 ) ) ;
#8411=CARTESIAN_POINT ( 'NONE',  ( 39.98359781491296161, -14.41368208888610525, 71.86517103874047052 ) ) ;
#8413=CARTESIAN_POINT ( 'NONE',  ( 36.29569395875879678, -13.31368208888610205, 69.98269868914867686 ) ) ;
#8418=CARTESIAN_POINT ( 'NONE',  ( 39.51027997493896748, -19.10384086642191193, 71.43714994484032843 ) ) ;
#8424=CARTESIAN_POINT ( 'NONE',  ( 39.73277004305197124, -25.40384086642191264, 69.52238214136765748 ) ) ;
#8426=CARTESIAN_POINT ( 'NONE',  ( 39.29254315202756231, -24.81368208888610383, 69.94417936956671156 ) ) ;
#8433=CARTESIAN_POINT ( 'NONE',  ( 39.98359781491296161, -13.20384086642191157, 70.89533451361945993 ) ) ;
#8438=CARTESIAN_POINT ( 'NONE',  ( 36.49096545463212493, -28.10384086642190127, 71.32335560751960202 ) ) ;
#8446=UNCERTAINTY_MEASURE_WITH_UNIT (LENGTH_MEASURE( 1.000000000000000082E-05 ), #22278, 'distance_accuracy_value', 'NONE');
#8447=CARTESIAN_POINT ( 'NONE',  ( 39.41296390513587511, -4.413682088886102584, 71.67976084211552745 ) ) ;
#8449=CARTESIAN_POINT ( 'NONE',  ( 39.31564783533280405, -2.313682088886100718, 72.03616607671141026 ) ) ;
#8456=CARTESIAN_POINT ( 'NONE',  ( 39.75915168707251723, -12.90384086642191797, 72.49904802271738902 ) ) ;
#8464=CARTESIAN_POINT ( 'NONE',  ( 38.26194895904383486, -7.013682088886100452, 69.64448340153879258 ) ) ;
#8466=CARTESIAN_POINT ( 'NONE',  ( 40.03626012656804534, -29.10876147765398159, 71.40821190666599705 ) ) ;
#8468=CARTESIAN_POINT ( 'NONE',  ( 37.69796330110504101, -27.11368208888609388, 69.66206559358660400 ) ) ;
#8469=CARTESIAN_POINT ( 'NONE',  ( 39.76930122830209058, -29.10876147765397803, 69.95214500915298572 ) ) ;
#8476=CARTESIAN_POINT ( 'NONE',  ( 39.02088643472237806, -0.7038408664219175659, 73.73360434286902887 ) ) ;
#8480=CARTESIAN_POINT ( 'NONE',  ( 37.89291511884476904, -21.11368208888610098, 70.26206559358661252 ) ) ;
#8484=CARTESIAN_POINT ( 'NONE',  ( 38.82593461698262871, -8.913682088886101695, 69.62690120949091011 ) ) ;
#8485=CARTESIAN_POINT ( 'NONE',  ( 39.95015449827720744, -29.00384086642191406, 71.96809898377885872 ) ) ;
#8490=CARTESIAN_POINT ( 'NONE',  ( 37.50301148336529167, -11.11368208888610276, 69.06206559358666652 ) ) ;
#8506=CARTESIAN_POINT ( 'NONE',  ( 36.11133435605973574, -22.00384086642191761, 70.60699637195608602 ) ) ;
#8507=CARTESIAN_POINT ( 'NONE',  ( 39.38009889167650357, -26.21368208888610951, 72.75271321436730432 ) ) ;
#8508=CARTESIAN_POINT ( 'NONE',  ( 38.31606138205702194, 1.691238522345987150, 73.11602215082119471 ) ) ;
#8514=CARTESIAN_POINT ( 'NONE',  ( 39.12911128074872380, -1.503840866421912725, 69.06206559358666652 ) ) ;
#8518=CARTESIAN_POINT ( 'NONE',  ( 38.37017380507020192, -8.013682088886108446, 73.11602215082118050 ) ) ;
#8520=CARTESIAN_POINT ( 'NONE',  ( 39.95015449827720744, -20.61368208888610454, 70.79240656858105751 ) ) ;
#8524=CARTESIAN_POINT ( 'NONE',  ( 37.69225076346193504, -23.80384086642191477, 70.42958956619166599 ) ) ;
#8525=CARTESIAN_POINT ( 'NONE',  ( 38.37017380507020192, -12.01368208888610845, 73.11602215082116629 ) ) ;
#8532=CARTESIAN_POINT ( 'NONE',  ( 38.37017380507018771, -13.60384086642190837, 69.64448340153877837 ) ) ;
#8536=CARTESIAN_POINT ( 'NONE',  ( 36.64852494920107517, -3.413682088886104360, 70.89533451361948835 ) ) ;
#8538=CARTESIAN_POINT ( 'NONE',  ( 35.86008812008917346, -15.51368208888610667, 71.43714994484034264 ) ) ;
#8542=CARTESIAN_POINT ( 'NONE',  ( 37.89291511884479036, -20.50384086642191406, 72.49843995877330372 ) ) ;
#8547=CARTESIAN_POINT ( 'NONE',  ( 37.50301148336529877, -22.50384086642191761, 73.69843995877327814 ) ) ;
#8549=CARTESIAN_POINT ( 'NONE',  ( 39.75915168707250302, -24.71368208888610241, 70.26145752964249880 ) ) ;
#8558=CARTESIAN_POINT ( 'NONE',  ( 38.26194895904384907, -16.60384086642191548, 73.11602215082116629 ) ) ;
#8565=CARTESIAN_POINT ( 'NONE',  ( 39.29254315202757653, -28.80384086642191832, 72.81632618279320468 ) ) ;
#8568=CARTESIAN_POINT ( 'NONE',  ( 37.25202387243752611, -27.21368208888610241, 70.00779233799262613 ) ) ;
#8574=CARTESIAN_POINT ( 'NONE',  ( 38.63098279924288647, -8.913682088886103472, 70.22690120949091863 ) ) ;
#8577=CARTESIAN_POINT ( 'NONE',  ( 39.51027997493896748, -6.513682088886100452, 71.32335560751961623 ) ) ;
#8584=CARTESIAN_POINT ( 'NONE',  ( 39.75915168707251723, -10.90384086642191619, 72.49904802271740323 ) ) ;
#8590=CARTESIAN_POINT ( 'NONE',  ( 37.69796330110504101, -5.113682088886100985, 69.66206559358664663 ) ) ;
#8595=ADVANCED_BREP_SHAPE_REPRESENTATION ( '', ( #17243, #2000 ), #13127 ) ;
#8603=CARTESIAN_POINT ( 'NONE',  ( 39.73277004305198545, -26.21368208888610951, 73.23812341099225875 ) ) ;
#8605=CARTESIAN_POINT ( 'NONE',  ( 39.24876120206128860, -24.71368208888610241, 70.63227792289242757 ) ) ;
#8610=CARTESIAN_POINT ( 'NONE',  ( 39.82603832034400426, -4.313682088886107380, 72.40698646996135324 ) ) ;
#8611=CARTESIAN_POINT ( 'NONE',  ( 39.51027997493896748, 0.8961591335780900724, 71.43714994484035685 ) ) ;
#8613=CARTESIAN_POINT ( 'NONE',  ( 40.26954217208371034, -8.713682088886100630, 69.89063713639259845 ) ) ;
#8633=CARTESIAN_POINT ( 'NONE',  ( 36.11133435605973574, -20.00384086642191406, 70.60699637195608602 ) ) ;
#8637=CARTESIAN_POINT ( 'NONE',  ( 40.33642880535524000, 1.686317911113892620, 72.77780686321129622 ) ) ;
#8646=CARTESIAN_POINT ( 'NONE',  ( 40.33642880535521869, 0.6961591335780878964, 69.98269868914869107 ) ) ;
#8652=CARTESIAN_POINT ( 'NONE',  ( 39.95015449827720744, 1.386317911113894130, 70.79240656858108593 ) ) ;
#8655=CARTESIAN_POINT ( 'NONE',  ( 36.64852494920107517, -21.41368208888610525, 70.89533451361947414 ) ) ;
#8661=CARTESIAN_POINT ( 'NONE',  ( 37.38336156205273397, -27.90384086642191264, 70.63227792289245599 ) ) ;
#8662=CARTESIAN_POINT ( 'NONE',  ( 39.29254315202756231, -14.81368208888610205, 69.94417936956672577 ) ) ;
#8666=CARTESIAN_POINT ( 'NONE',  ( 36.80608444377001831, -8.303840866421916544, 72.40698646996136745 ) ) ;
#8669=CARTESIAN_POINT ( 'NONE',  ( 38.26194895904383486, -3.013682088886100008, 69.64448340153879258 ) ) ;
#8671=CARTESIAN_POINT ( 'NONE',  ( 40.52078840805428683, -16.61368208888610454, 70.60699637195608602 ) ) ;
#8675=CARTESIAN_POINT ( 'NONE',  ( 38.73920764526923932, -11.50384086642191050, 70.26206559358664094 ) ) ;
#8680=CARTESIAN_POINT ( 'NONE',  ( 38.37017380507018771, -19.60384086642191193, 69.04448340153878405 ) ) ;
#8682=CARTESIAN_POINT ( 'NONE',  ( 40.33642880535524000, 1.686317911113892620, 72.77780686321129622 ) ) ;
#8689=CARTESIAN_POINT ( 'NONE',  ( 36.64852494920107517, -16.20384086642190979, 71.86517103874048473 ) ) ;
#8697=CARTESIAN_POINT ( 'NONE',  ( 37.60469502381300799, -2.403840866421910416, 72.26730301774236409 ) ) ;
#8700=CARTESIAN_POINT ( 'NONE',  ( 36.64852494920107517, -25.41368208888610525, 70.89533451361945993 ) ) ;
#8705=CARTESIAN_POINT ( 'NONE',  ( 37.60469502381300799, -28.40384086642191264, 72.26730301774232146 ) ) ;
#8706=CARTESIAN_POINT ( 'NONE',  ( 38.37017380507018771, -29.60384086642191193, 70.24448340153875847 ) ) ;
#8712=CARTESIAN_POINT ( 'NONE',  ( 36.87297107704149823, -11.90384086642190731, 70.26145752964252722 ) ) ;
#8722=CARTESIAN_POINT ( 'NONE',  ( 36.49096545463212493, -9.513682088886104893, 71.43714994484035685 ) ) ;
#8735=CARTESIAN_POINT ( 'NONE',  ( 38.26194895904383486, -29.01368208888610312, 69.04448340153878405 ) ) ;
#8736=CARTESIAN_POINT ( 'NONE',  ( 38.63098279924288647, -18.91368208888609814, 70.22690120949090442 ) ) ;
#8741=CARTESIAN_POINT ( 'NONE',  ( 39.38009889167650357, -0.2136820888861065693, 72.75271321436733274 ) ) ;
#8742=CARTESIAN_POINT ( 'NONE',  ( 38.93415946300896024, -29.50384086642191050, 69.66206559358660400 ) ) ;
#8744=CARTESIAN_POINT ( 'NONE',  ( 36.36258059203031934, -5.713682088886106847, 72.86986841596736042 ) ) ;
#8762=CARTESIAN_POINT ( 'NONE',  ( 36.11133435605973574, -18.00384086642191050, 70.60699637195608602 ) ) ;
#8763=CARTESIAN_POINT ( 'NONE',  ( 39.98359781491296161, -22.41368208888610525, 71.86517103874047052 ) ) ;
#8773=CARTESIAN_POINT ( 'NONE',  ( 37.61123632939165873, -27.91368208888610880, 73.73360434286898624 ) ) ;
#8778=CARTESIAN_POINT ( 'NONE',  ( 40.14115730948191185, -2.513682088886103116, 71.32335560751961623 ) ) ;
#8781=CARTESIAN_POINT ( 'NONE',  ( 37.69796330110504101, -19.11368208888610098, 69.66206559358663242 ) ) ;
#8787=CARTESIAN_POINT ( 'NONE',  ( 39.37952058850012804, -17.00384086642191406, 71.78268878715390144 ) ) ;
#8788=CARTESIAN_POINT ( 'NONE',  ( 37.80618814713140097, -3.913682088886108801, 73.13360434286904876 ) ) ;
#8793=CARTESIAN_POINT ( 'NONE',  ( 38.37017380507018771, -3.603840866421907041, 69.64448340153879258 ) ) ;
#8795=CARTESIAN_POINT ( 'NONE',  ( 39.75915168707250302, -6.713682088886099741, 70.26145752964252722 ) ) ;
#8797=CARTESIAN_POINT ( 'NONE',  ( 39.02088643472237095, -8.913682088886103472, 69.02690120949094421 ) ) ;
#8800=CARTESIAN_POINT ( 'NONE',  ( 38.00113996487112189, -11.70384086642191335, 70.22690120949091863 ) ) ;
#8807=CARTESIAN_POINT ( 'NONE',  ( 38.37017380507018771, -13.60384086642191193, 69.04448340153878405 ) ) ;
#8812=FILL_AREA_STYLE ('',( #14710 ) ) ;
#8813=CARTESIAN_POINT ( 'NONE',  ( 37.80618814713140097, -21.91368208888610880, 73.13360434286903455 ) ) ;
#8821=CARTESIAN_POINT ( 'NONE',  ( 40.14115730948191185, -13.10384086642191015, 71.43714994484031422 ) ) ;
#8826=CARTESIAN_POINT ( 'NONE',  ( 37.33957961208645315, -23.80384086642191122, 69.94417936956671156 ) ) ;
#8831=CARTESIAN_POINT ( 'NONE',  ( 39.95015449827720744, -22.61368208888610809, 70.79240656858105751 ) ) ;
#8836=CARTESIAN_POINT ( 'NONE',  ( 39.51027997493896748, -2.513682088886099564, 71.32335560751961623 ) ) ;
#8837=CARTESIAN_POINT ( 'NONE',  ( 37.31647492878122563, 0.6863179111138985045, 70.72433947564853440 ) ) ;
#8843=CARTESIAN_POINT ( 'NONE',  ( 36.64852494920107517, -4.203840866421910683, 71.86517103874049894 ) ) ;
#8851=CARTESIAN_POINT ( 'NONE',  ( 38.37017380507020192, -4.013682088886107557, 73.11602215082118050 ) ) ;
#8868=CARTESIAN_POINT ( 'NONE',  ( 38.63098279924288647, -14.91368208888609992, 70.22690120949090442 ) ) ;
#8870=ORIENTED_EDGE ( 'NONE', *, *, #18953, .F. ) ;
#8872=CARTESIAN_POINT ( 'NONE',  ( 37.33957961208646736, 0.1863179111138910105, 72.81632618279323310 ) ) ;
#8873=CARTESIAN_POINT ( 'NONE',  ( 38.26194895904384907, -26.60384086642191548, 73.11602215082115208 ) ) ;
#8876=CARTESIAN_POINT ( 'NONE',  ( 40.52078840805428683, -10.61368208888610631, 70.60699637195608602 ) ) ;
#8891=CARTESIAN_POINT ( 'NONE',  ( 36.07789103942399578, -14.20384086642191512, 72.05058123536544201 ) ) ;
#8892=CARTESIAN_POINT ( 'NONE',  ( 39.29254315202756231, -20.81368208888610027, 69.94417936956672577 ) ) ;
#8895=( NAMED_UNIT ( * ) SI_UNIT ( $, .STERADIAN. ) SOLID_ANGLE_UNIT ( ) );
#8900=CARTESIAN_POINT ( 'NONE',  ( 39.64521430340305841, 1.196159133578081457, 73.30173637941821596 ) ) ;
#8904=CARTESIAN_POINT ( 'NONE',  ( 37.80618814713140097, -1.913682088886106136, 73.13360434286904876 ) ) ;
#8907=CARTESIAN_POINT ( 'NONE',  ( 39.98359781491296161, -20.41368208888610525, 71.86517103874047052 ) ) ;
#8910=CARTESIAN_POINT ( 'NONE',  ( 37.69225076346193504, -21.80384086642191122, 70.42958956619168021 ) ) ;
#8911=CARTESIAN_POINT ( 'NONE',  ( 39.38009889167650357, -4.213682088886106847, 72.75271321436733274 ) ) ;
#8914=CARTESIAN_POINT ( 'NONE',  ( 38.82593461698265003, -2.703840866421916012, 73.13360434286904876 ) ) ;
#8916=CARTESIAN_POINT ( 'NONE',  ( 36.68196826583682935, -5.613682088886105426, 71.96809898377890136 ) ) ;
#8918=CARTESIAN_POINT ( 'NONE',  ( 36.29569395875879678, -7.313682088886101162, 69.98269868914869107 ) ) ;
#8921=CARTESIAN_POINT ( 'NONE',  ( 37.12184278917507640, -10.10384086642191193, 71.32335560751961623 ) ) ;
#8927=CARTESIAN_POINT ( 'NONE',  ( 37.50301148336529877, -14.50384086642191761, 73.69843995877327814 ) ) ;
#8929=CARTESIAN_POINT ( 'NONE',  ( 38.82593461698262871, -22.91368208888609459, 69.62690120949091011 ) ) ;
#8935=CARTESIAN_POINT ( 'NONE',  ( 36.68196826583682935, -18.00384086642191406, 70.79240656858107172 ) ) ;
#8939=CARTESIAN_POINT ( 'NONE',  ( 37.69796330110504101, -23.11368208888609743, 69.66206559358660400 ) ) ;
#8945=CARTESIAN_POINT ( 'NONE',  ( 39.29254315202757653, -22.80384086642191477, 72.81632618279321889 ) ) ;
#8948=CARTESIAN_POINT ( 'NONE',  ( 37.33957961208646736, -23.81368208888611093, 72.81632618279320468 ) ) ;
#8953=CARTESIAN_POINT ( 'NONE',  ( 37.12184278917507640, -1.513682088886101784, 71.43714994484035685 ) ) ;
#8954=CARTESIAN_POINT ( 'NONE',  ( 37.69225076346193504, 0.1863179111138979493, 72.33091598616827866 ) ) ;
#8962=CARTESIAN_POINT ( 'NONE',  ( 37.25202387243754032, -4.403840866421916189, 72.75271321436733274 ) ) ;
#8972=CARTESIAN_POINT ( 'NONE',  ( 38.37017380507020192, -0.01368208888610777940, 73.11602215082118050 ) ) ;
#8990=CARTESIAN_POINT ( 'NONE',  ( 37.89291511884476904, -19.11368208888609388, 70.26206559358661252 ) ) ;
#8994=CARTESIAN_POINT ( 'NONE',  ( 40.14115730948191185, -0.5136820888861047818, 71.32335560751961623 ) ) ;
#8995=CARTESIAN_POINT ( 'NONE',  ( 39.98359781491296161, -23.20384086642191335, 70.89533451361945993 ) ) ;
#8997=CARTESIAN_POINT ( 'NONE',  ( 36.11133435605973574, -9.613682088886104538, 72.15350918040385864 ) ) ;
#9018=CARTESIAN_POINT ( 'NONE',  ( 37.50301148336529877, -16.50384086642191761, 73.69843995877327814 ) ) ;
#9020=CARTESIAN_POINT ( 'NONE',  ( 37.25202387243752611, -23.21368208888610241, 70.00779233799262613 ) ) ;
#9028=CARTESIAN_POINT ( 'NONE',  ( 39.02088643472237095, -26.91368208888610170, 69.02690120949091579 ) ) ;
#9035=CARTESIAN_POINT ( 'NONE',  ( 37.69796330110504101, -3.113682088886098764, 69.66206559358663242 ) ) ;
#9038=CARTESIAN_POINT ( 'NONE',  ( 40.14115730948191185, -22.51368208888610312, 71.32335560751960202 ) ) ;
#9044=CARTESIAN_POINT ( 'NONE',  ( 39.51027997493896748, -17.10384086642191193, 71.43714994484032843 ) ) ;
#9045=CARTESIAN_POINT ( 'NONE',  ( 36.49096545463212493, -7.513682088886102228, 71.43714994484035685 ) ) ;
#9051=CARTESIAN_POINT ( 'NONE',  ( 39.75915168707251723, -6.903840866421915301, 72.49904802271740323 ) ) ;
#9054=CARTESIAN_POINT ( 'NONE',  ( 36.49096545463212493, -5.513682088886105781, 71.43714994484035685 ) ) ;
#9056=CARTESIAN_POINT ( 'NONE',  ( 38.26194895904383486, -9.013682088886101340, 69.04448340153881247 ) ) ;
#9059=CARTESIAN_POINT ( 'NONE',  ( 37.25260217561390874, -10.00384086642191406, 70.97781676520604321 ) ) ;
#9065=CARTESIAN_POINT ( 'NONE',  ( 36.98690846071097127, -17.80384086642191122, 69.45876917294175712 ) ) ;
#9069=CARTESIAN_POINT ( 'NONE',  ( 38.37017380507020192, -22.01368208888611022, 73.11602215082116629 ) ) ;
#9076=CARTESIAN_POINT ( 'NONE',  ( 39.82603832034401137, -9.303840866421907663, 70.35351908239860563 ) ) ;
#9079=CARTESIAN_POINT ( 'NONE',  ( 39.82603832034400426, -22.31368208888610738, 72.40698646996133903 ) ) ;
#9082=CARTESIAN_POINT ( 'NONE',  ( 36.64852494920107517, -22.20384086642191335, 71.86517103874048473 ) ) ;
#9085=CARTESIAN_POINT ( 'NONE',  ( 39.98359781491296161, -24.41368208888610525, 71.86517103874045631 ) ) ;
#9091=CARTESIAN_POINT ( 'NONE',  ( 37.25260217561390874, -1.613682088886101651, 71.78268878715394408 ) ) ;
#9097=CARTESIAN_POINT ( 'NONE',  ( 38.37017380507018771, -1.603840866421908595, 69.64448340153879258 ) ) ;
#9109=CARTESIAN_POINT ( 'NONE',  ( 37.69796330110504101, -1.113682088886101207, 69.66206559358664663 ) ) ;
#9110=CARTESIAN_POINT ( 'NONE',  ( 37.25202387243754032, -28.40384086642191619, 72.75271321436730432 ) ) ;
#9124=CARTESIAN_POINT ( 'NONE',  ( 38.73920764526925353, -20.11368208888610098, 72.49843995877330372 ) ) ;
#9128=CARTESIAN_POINT ( 'NONE',  ( 39.38009889167650357, -4.213682088886106847, 72.75271321436733274 ) ) ;
#9129=CARTESIAN_POINT ( 'NONE',  ( 39.75915168707251723, -24.90384086642191619, 72.49904802271737481 ) ) ;
#9132=CARTESIAN_POINT ( 'NONE',  ( 39.73277004305198545, -2.213682088886108179, 73.23812341099225875 ) ) ;
#9146=STYLED_ITEM ( 'NONE', ( #4929 ), #17243 ) ;
#9150=CARTESIAN_POINT ( 'NONE',  ( 36.89935272106205133, -18.40384086642191974, 73.23812341099225875 ) ) ;
#9153=CARTESIAN_POINT ( 'NONE',  ( 39.98359781491296161, -20.41368208888610525, 71.86517103874047052 ) ) ;
#9158=CARTESIAN_POINT ( 'NONE',  ( 36.89935272106204422, -25.21368208888610241, 69.52238214136765748 ) ) ;
#9164=CARTESIAN_POINT ( 'NONE',  ( 37.33957961208646736, 0.1863179111138910105, 72.81632618279323310 ) ) ;
#9167=CARTESIAN_POINT ( 'NONE',  ( 36.80608444377001121, -11.31368208888610027, 70.35351908239860563 ) ) ;
#9171=CARTESIAN_POINT ( 'NONE',  ( 37.89291511884479036, -18.50384086642191406, 72.49843995877330372 ) ) ;
#9172=CARTESIAN_POINT ( 'NONE',  ( 38.37017380507020192, -6.013682088886109334, 73.11602215082118050 ) ) ;
#9178=CARTESIAN_POINT ( 'NONE',  ( 37.80618814713138676, -3.703840866421904909, 69.62690120949091011 ) ) ;
#9182=CARTESIAN_POINT ( 'NONE',  ( 38.93987200065208754, -28.81368208888610383, 70.42958956619166599 ) ) ;
#9184=CARTESIAN_POINT ( 'NONE',  ( 40.77203464402485622, -12.51368208888610667, 71.32335560751960202 ) ) ;
#9187=CARTESIAN_POINT ( 'NONE',  ( 39.24876120206129571, -8.903840866421910860, 72.12822762946750288 ) ) ;
#9193=CARTESIAN_POINT ( 'NONE',  ( 40.77203464402485622, -19.10384086642191193, 71.43714994484032843 ) ) ;
#9196=CARTESIAN_POINT ( 'NONE',  ( 36.68196826583682935, -19.61368208888610809, 71.96809898377888715 ) ) ;
#9205=CARTESIAN_POINT ( 'NONE',  ( 39.98359781491296161, -7.203840866421913347, 70.89533451361947414 ) ) ;
#9208=CARTESIAN_POINT ( 'NONE',  ( 36.64852494920107517, -25.41368208888610525, 70.89533451361945993 ) ) ;
#9211=CARTESIAN_POINT ( 'NONE',  ( 38.37017380507018771, -21.60384086642190837, 69.64448340153877837 ) ) ;
#9214=CARTESIAN_POINT ( 'NONE',  ( 39.38009889167650357, -18.21368208888610951, 72.75271321436731853 ) ) ;
#9216=CARTESIAN_POINT ( 'NONE',  ( 40.77203464402485622, -26.51368208888610667, 71.32335560751960202 ) ) ;
#9221=CARTESIAN_POINT ( 'NONE',  ( 38.73920764526925353, 1.886317911113897905, 72.49843995877333214 ) ) ;
#9229=CARTESIAN_POINT ( 'NONE',  ( 38.93415946300896024, -3.503840866421906952, 69.66206559358663242 ) ) ;
#9238=CARTESIAN_POINT ( 'NONE',  ( 40.14115730948191185, -0.5136820888861047818, 71.32335560751961623 ) ) ;
#9240=CARTESIAN_POINT ( 'NONE',  ( 40.04784734886185760, -29.05498820292889306, 71.69653269215241664 ) ) ;
#9256=CARTESIAN_POINT ( 'NONE',  ( 37.89291511884476904, -17.11368208888609743, 70.26206559358661252 ) ) ;
#9261=CARTESIAN_POINT ( 'NONE',  ( 36.80608444377001831, -24.30384086642191832, 72.40698646996133903 ) ) ;
#9265=CARTESIAN_POINT ( 'NONE',  ( 36.11133435605973574, -1.613682088886104982, 72.15350918040385864 ) ) ;
#9281=CARTESIAN_POINT ( 'NONE',  ( 40.55423172469004101, -11.20384086642191690, 70.70992431699450265 ) ) ;
#9285=CARTESIAN_POINT ( 'NONE',  ( 38.93415946300897446, -16.11368208888611164, 73.09843995877329803 ) ) ;
#9286=CARTESIAN_POINT ( 'NONE',  ( 0.000000000000000000, 0.000000000000000000, 0.000000000000000000 ) ) ;
#9291=CARTESIAN_POINT ( 'NONE',  ( 36.11133435605973574, -19.61368208888610454, 72.15350918040385864 ) ) ;
#9301=CARTESIAN_POINT ( 'NONE',  ( 37.21915885897815457, -22.20384086642191335, 71.67976084211552745 ) ) ;
#9302=CARTESIAN_POINT ( 'NONE',  ( 39.38009889167650357, -2.213682088886108179, 72.75271321436733274 ) ) ;
#9308=CARTESIAN_POINT ( 'NONE',  ( 38.37017380507018771, -1.603840866421908595, 69.64448340153879258 ) ) ;
#9310=CARTESIAN_POINT ( 'NONE',  ( 37.25202387243752611, -1.213682088886100630, 70.00779233799264034 ) ) ;
#9312=CARTESIAN_POINT ( 'NONE',  ( 38.37017380507020192, -8.013682088886108446, 73.71602215082116061 ) ) ;
#9315=CARTESIAN_POINT ( 'NONE',  ( 37.89291511884479036, -6.503840866421909617, 72.49843995877331793 ) ) ;
#9320=CARTESIAN_POINT ( 'NONE',  ( 39.12911128074872380, -7.503840866421911393, 69.06206559358666652 ) ) ;
#9323=CARTESIAN_POINT ( 'NONE',  ( 37.69796330110504101, -23.11368208888609743, 69.66206559358660400 ) ) ;
#9328=CARTESIAN_POINT ( 'NONE',  ( 39.66066260159757917, -29.10876147765399580, 70.75778293607493197 ) ) ;
#9329=CARTESIAN_POINT ( 'NONE',  ( 37.25202387243754032, -8.403840866421916189, 72.75271321436733274 ) ) ;
#9332=CARTESIAN_POINT ( 'NONE',  ( 36.49096545463212493, -25.51368208888609956, 71.43714994484030001 ) ) ;
#9334=CARTESIAN_POINT ( 'NONE',  ( 37.80618814713138676, -27.70384086642190269, 69.62690120949091011 ) ) ;
#9336=CARTESIAN_POINT ( 'NONE',  ( 38.82593461698262871, -16.91368208888610170, 69.62690120949091011 ) ) ;
#9338=CARTESIAN_POINT ( 'NONE',  ( 36.98690846071097127, 0.1961591335780874246, 69.45876917294177133 ) ) ;
#9342=CARTESIAN_POINT ( 'NONE',  ( 37.12184278917507640, -26.10384086642191193, 71.32335560751960202 ) ) ;
#9348=CARTESIAN_POINT ( 'NONE',  ( 37.69796330110505522, -6.503840866421914058, 73.09843995877331224 ) ) ;
#9359=CARTESIAN_POINT ( 'NONE',  ( 38.37017380507020192, -2.013682088886109334, 73.11602215082118050 ) ) ;
#9360=CARTESIAN_POINT ( 'NONE',  ( 36.49096545463212493, -28.10384086642190837, 71.32335560751960202 ) ) ;
#9373=CARTESIAN_POINT ( 'NONE',  ( 39.02742774030102879, -14.21368208888610241, 72.26730301774234988 ) ) ;
#9375=CARTESIAN_POINT ( 'NONE',  ( 37.69225076346193504, -11.81368208888610205, 72.33091598616826445 ) ) ;
#9380=CARTESIAN_POINT ( 'NONE',  ( 36.80608444377001831, -22.30384086642191477, 72.40698646996135324 ) ) ;
#9399=CARTESIAN_POINT ( 'NONE',  ( 39.02088643472237806, -10.70384086642192045, 73.73360434286902887 ) ) ;
#9401=CARTESIAN_POINT ( 'NONE',  ( 39.38009889167650357, -12.21368208888610596, 72.75271321436731853 ) ) ;
#9407=CARTESIAN_POINT ( 'NONE',  ( 37.50301148336529167, -21.11368208888610098, 69.06206559358665231 ) ) ;
#9420=CARTESIAN_POINT ( 'NONE',  ( 37.69225076346193504, -13.80384086642191122, 70.42958956619168021 ) ) ;
#9421=CARTESIAN_POINT ( 'NONE',  ( 38.93415946300897446, -0.1136820888861071466, 73.09843995877331224 ) ) ;
#9430=CARTESIAN_POINT ( 'NONE',  ( 37.61123632939164452, -27.70384086642191690, 69.02690120949091579 ) ) ;
#9431=CARTESIAN_POINT ( 'NONE',  ( 36.80608444377001121, -1.313682088886099386, 70.35351908239860563 ) ) ;
#9432=CARTESIAN_POINT ( 'NONE',  ( 36.36258059203031934, -1.713682088886108179, 72.86986841596736042 ) ) ;
#9435=CARTESIAN_POINT ( 'NONE',  ( 39.41296390513587511, -7.203840866421913347, 71.08074471024443142 ) ) ;
#9441=CARTESIAN_POINT ( 'NONE',  ( 40.33642880535521869, -11.30384086642191299, 69.98269868914867686 ) ) ;
#9446=CARTESIAN_POINT ( 'NONE',  ( 36.80608444377001121, -15.31368208888610383, 70.35351908239857721 ) ) ;
#9452=CARTESIAN_POINT ( 'NONE',  ( 38.37017380507018771, -5.603840866421908373, 69.64448340153879258 ) ) ;
#9456=CARTESIAN_POINT ( 'NONE',  ( 36.68196826583682935, -15.61368208888610454, 71.96809898377888715 ) ) ;
#9458=CARTESIAN_POINT ( 'NONE',  ( 39.75915168707251723, -18.90384086642190553, 72.49904802271738902 ) ) ;
#9461=CARTESIAN_POINT ( 'NONE',  ( 36.80608444377001121, -19.31368208888609672, 70.35351908239857721 ) ) ;
#9463=CARTESIAN_POINT ( 'NONE',  ( 40.55423172469004811, -22.41368208888610525, 72.05058123536544201 ) ) ;
#9467=CARTESIAN_POINT ( 'NONE',  ( 38.63098279924290068, -26.70384086642191690, 72.53360434286901182 ) ) ;
#9475=CARTESIAN_POINT ( 'NONE',  ( 36.07789103942399578, -26.20384086642191335, 72.05058123536544201 ) ) ;
#9483=CARTESIAN_POINT ( 'NONE',  ( 37.80618814713138676, -25.70384086642190979, 69.62690120949091011 ) ) ;
#9491=CARTESIAN_POINT ( 'NONE',  ( 39.31564783533279694, -5.303840866421911215, 70.72433947564853440 ) ) ;
#9500=CARTESIAN_POINT ( 'NONE',  ( 38.26194895904383486, -9.013682088886101340, 70.24448340153877268 ) ) ;
#9502=CARTESIAN_POINT ( 'NONE',  ( 38.26194895904383486, -13.01368208888610312, 70.24448340153875847 ) ) ;
#9509=CARTESIAN_POINT ( 'NONE',  ( 38.26194895904384907, -14.60384086642191548, 73.11602215082116629 ) ) ;
#9512=CARTESIAN_POINT ( 'NONE',  ( 37.38336156205274818, -15.71368208888609885, 72.12822762946750288 ) ) ;
#9530=CARTESIAN_POINT ( 'NONE',  ( 36.89935272106205133, -8.403840866421919742, 73.23812341099225875 ) ) ;
#9532=CARTESIAN_POINT ( 'NONE',  ( 36.64852494920107517, -17.41368208888610525, 70.89533451361947414 ) ) ;
#9536=CARTESIAN_POINT ( 'NONE',  ( 37.50301148336529167, -19.11368208888609388, 69.06206559358665231 ) ) ;
#9544=CARTESIAN_POINT ( 'NONE',  ( 37.12184278917507640, -10.10384086642191193, 71.32335560751961623 ) ) ;
#9545=CARTESIAN_POINT ( 'NONE',  ( 36.64852494920107517, -1.413682088886102806, 70.89533451361948835 ) ) ;
#9551=CARTESIAN_POINT ( 'NONE',  ( 35.86008812008917346, -28.10384086642191903, 71.32335560751960202 ) ) ;
#9554=CARTESIAN_POINT ( 'NONE',  ( 37.69225076346193504, -27.81368208888610383, 72.33091598616823603 ) ) ;
#9555=CARTESIAN_POINT ( 'NONE',  ( 36.36258059203031934, -3.713682088886109955, 72.86986841596736042 ) ) ;
#9561=CARTESIAN_POINT ( 'NONE',  ( 37.12184278917507640, -6.103840866421912814, 71.32335560751961623 ) ) ;
#9568=CARTESIAN_POINT ( 'NONE',  ( 37.61123632939164452, -9.703840866421911571, 69.02690120949094421 ) ) ;
#9571=CARTESIAN_POINT ( 'NONE',  ( 37.25202387243752611, -17.21368208888610241, 70.00779233799262613 ) ) ;
#9577=CARTESIAN_POINT ( 'NONE',  ( 38.93415946300897446, -9.503840866421908729, 69.66206559358664663 ) ) ;
#9578=SHAPE_DEFINITION_REPRESENTATION ( #8090, #24379 ) ;
#9581=CARTESIAN_POINT ( 'NONE',  ( 36.64852494920107517, -19.41368208888610525, 70.89533451361947414 ) ) ;
#9584=CARTESIAN_POINT ( 'NONE',  ( 38.82593461698265003, -16.70384086642191690, 73.13360434286903455 ) ) ;
#9589=CARTESIAN_POINT ( 'NONE',  ( 36.80608444377001121, -17.31368208888609672, 70.35351908239857721 ) ) ;
#9591=CARTESIAN_POINT ( 'NONE',  ( 36.89935272106204422, -21.21368208888610241, 69.52238214136768590 ) ) ;
#9596=CARTESIAN_POINT ( 'NONE',  ( 37.38336156205273397, -21.90384086642191619, 70.63227792289247020 ) ) ;
#9597=ADVANCED_FACE ( 'NONE', ( #16205 ), #2288, .F. ) ;
#9605=CARTESIAN_POINT ( 'NONE',  ( 36.89935272106205133, -28.40384086642191619, 73.23812341099225875 ) ) ;
#9612=DIRECTION ( 'NONE',  ( 0.1803747433772539821, 0.9835979625596982245, 0.000000000000000000 ) ) ;
#9623=CARTESIAN_POINT ( 'NONE',  ( 39.51027997493896748, -7.103840866421911038, 71.43714994484034264 ) ) ;
#9630=CARTESIAN_POINT ( 'NONE',  ( 39.24876120206128860, -14.71368208888610241, 70.63227792289245599 ) ) ;
#9631=CARTESIAN_POINT ( 'NONE',  ( 38.00113996487114321, -13.91368208888610347, 72.53360434286904024 ) ) ;
#9639=CARTESIAN_POINT ( 'NONE',  ( 38.82593461698265003, -18.70384086642191690, 73.13360434286903455 ) ) ;
#9642=CARTESIAN_POINT ( 'NONE',  ( 38.00113996487114321, -17.91368208888609459, 72.53360434286904024 ) ) ;
#9646=CARTESIAN_POINT ( 'NONE',  ( 39.29254315202756231, -16.81368208888610383, 69.94417936956672577 ) ) ;
#9660=CARTESIAN_POINT ( 'NONE',  ( 36.36258059203030513, -9.903840866421909084, 69.89063713639259845 ) ) ;
#9665=CARTESIAN_POINT ( 'NONE',  ( 37.69796330110504101, -13.11368208888609743, 69.66206559358661821 ) ) ;
#9669=CARTESIAN_POINT ( 'NONE',  ( 35.86008812008917346, -21.51368208888609956, 71.43714994484034264 ) ) ;
#9679=CARTESIAN_POINT ( 'NONE',  ( 39.02742774030101458, -13.40384086642191619, 70.49320253461759478 ) ) ;
#9680=CARTESIAN_POINT ( 'NONE',  ( 36.64852494920107517, 0.5863179111138955291, 70.89533451361948835 ) ) ;
#9686=CARTESIAN_POINT ( 'NONE',  ( 39.38009889167648936, 0.5961591335780919154, 70.00779233799265455 ) ) ;
#9688=CARTESIAN_POINT ( 'NONE',  ( 38.93415946300897446, 1.886317911113891244, 73.09843995877332645 ) ) ;
#9689=CARTESIAN_POINT ( 'NONE',  ( 36.98690846071097837, 0.1863179111138910382, 73.30173637941818754 ) ) ;
#9692=CARTESIAN_POINT ( 'NONE',  ( 38.26194895904384197, -8.603840866421911926, 72.51602215082118619 ) ) ;
#9697=CARTESIAN_POINT ( 'NONE',  ( 39.02088643472237806, -12.70384086642191690, 73.73360434286898624 ) ) ;
#9700=CARTESIAN_POINT ( 'NONE',  ( 38.26194895904383486, -11.01368208888609956, 69.64448340153879258 ) ) ;
#9704=CARTESIAN_POINT ( 'NONE',  ( 38.82593461698264292, -4.703840866421914235, 73.13360434286904876 ) ) ;
#9707=CARTESIAN_POINT ( 'NONE',  ( 40.14115730948191185, -16.51368208888610667, 71.32335560751960202 ) ) ;
#9709=CARTESIAN_POINT ( 'NONE',  ( 39.82603832034400426, -15.30384086642190589, 70.35351908239857721 ) ) ;
#9711=CARTESIAN_POINT ( 'NONE',  ( 38.82593461698262871, -20.91368208888609459, 69.62690120949091011 ) ) ;
#9713=CARTESIAN_POINT ( 'NONE',  ( 36.98690846071097837, -19.81368208888611093, 73.30173637941818754 ) ) ;
#9717=CARTESIAN_POINT ( 'NONE',  ( 39.41296390513587511, -23.20384086642191335, 71.08074471024441721 ) ) ;
#9723=CARTESIAN_POINT ( 'NONE',  ( 36.29569395875881099, -28.30384086642192187, 72.77780686321126780 ) ) ;
#9724=CARTESIAN_POINT ( 'NONE',  ( 38.26194895904383486, -1.013682088886101784, 69.04448340153881247 ) ) ;
#9733=CARTESIAN_POINT ( 'NONE',  ( 39.95015449827720744, -19.00384086642191406, 71.96809898377887293 ) ) ;
#9743=CARTESIAN_POINT ( 'NONE',  ( 39.02742774030101458, -3.403840866421911748, 70.49320253461759478 ) ) ;
#9751=CARTESIAN_POINT ( 'NONE',  ( 37.60469502381300089, -11.21368208888610241, 70.49320253461759478 ) ) ;
#9752=CARTESIAN_POINT ( 'NONE',  ( 37.60469502381300089, -9.213682088886100630, 70.49320253461759478 ) ) ;
#9758=CARTESIAN_POINT ( 'NONE',  ( 39.98359781491296161, 1.586317911113896528, 71.86517103874049894 ) ) ;
#9759=CARTESIAN_POINT ( 'NONE',  ( 38.26194895904384907, -16.60384086642191548, 73.11602215082116629 ) ) ;
#9761=CARTESIAN_POINT ( 'NONE',  ( 37.60469502381300089, -21.21368208888610241, 70.49320253461759478 ) ) ;
#9764=CARTESIAN_POINT ( 'NONE',  ( 36.87297107704153376, -11.71368208888611129, 72.49904802271740323 ) ) ;
#9778=CARTESIAN_POINT ( 'NONE',  ( 38.37017380507018771, -13.60384086642191193, 69.04448340153878405 ) ) ;
#9781=CARTESIAN_POINT ( 'NONE',  ( 38.82593461698262871, -14.91368208888609637, 69.62690120949091011 ) ) ;
#9786=CARTESIAN_POINT ( 'NONE',  ( 37.61123632939165873, -23.91368208888611235, 73.73360434286898624 ) ) ;
#9797=CARTESIAN_POINT ( 'NONE',  ( 38.63098279924290068, -12.70384086642191157, 72.53360434286904024 ) ) ;
#9798=CARTESIAN_POINT ( 'NONE',  ( 37.21915885897815457, -27.41368208888609814, 71.08074471024441721 ) ) ;
#9805=CARTESIAN_POINT ( 'NONE',  ( 37.80618814713138676, -1.703840866421908018, 69.62690120949091011 ) ) ;
#9808=CARTESIAN_POINT ( 'NONE',  ( 39.41296390513587511, -22.41368208888610525, 71.67976084211551324 ) ) ;
#9809=CARTESIAN_POINT ( 'NONE',  ( 39.73277004305198545, -2.213682088886108179, 73.23812341099225875 ) ) ;
#9812=CARTESIAN_POINT ( 'NONE',  ( 39.02742774030101458, -1.403840866421909972, 70.49320253461759478 ) ) ;
#9819=CARTESIAN_POINT ( 'NONE',  ( 40.55423172469004101, -9.203840866421915123, 70.70992431699450265 ) ) ;
#9821=CARTESIAN_POINT ( 'NONE',  ( 36.87297107704152666, -15.71368208888610596, 72.49904802271740323 ) ) ;
#9827=CARTESIAN_POINT ( 'NONE',  ( 39.75915168707251723, -4.903840866421915301, 72.49904802271740323 ) ) ;
#9830=CARTESIAN_POINT ( 'NONE',  ( 40.14115730948191185, -20.51368208888609601, 71.32335560751960202 ) ) ;
#9832=CARTESIAN_POINT ( 'NONE',  ( 39.95015449827720744, -21.00384086642191406, 71.96809898377887293 ) ) ;
#9834=CARTESIAN_POINT ( 'NONE',  ( 39.38009889167650357, -10.21368208888610773, 72.75271321436733274 ) ) ;
#9836=CARTESIAN_POINT ( 'NONE',  ( 36.07789103942398867, -23.41368208888610525, 70.70992431699450265 ) ) ;
#9840=CARTESIAN_POINT ( 'NONE',  ( 38.93987200065210175, -26.80384086642191122, 72.33091598616823603 ) ) ;
#9848=CARTESIAN_POINT ( 'NONE',  ( 37.50301148336529877, -26.50384086642192116, 73.69843995877326392 ) ) ;
#9850=CARTESIAN_POINT ( 'NONE',  ( 37.50301148336529167, -3.113682088886100097, 69.06206559358666652 ) ) ;
#9858=CARTESIAN_POINT ( 'NONE',  ( 36.64852494920107517, -22.20384086642191335, 71.86517103874048473 ) ) ;
#9865=CARTESIAN_POINT ( 'NONE',  ( 39.31564783533279694, -3.303840866421912548, 70.72433947564853440 ) ) ;
#9868=CARTESIAN_POINT ( 'NONE',  ( 39.38009889167650357, -28.21368208888610951, 72.75271321436730432 ) ) ;
#9872=CARTESIAN_POINT ( 'NONE',  ( 37.12184278917507640, -13.51368208888610312, 71.43714994484034264 ) ) ;
#9875=CARTESIAN_POINT ( 'NONE',  ( 38.73920764526925353, -10.11368208888610276, 72.49843995877331793 ) ) ;
#9882=CARTESIAN_POINT ( 'NONE',  ( 36.87297107704149823, -19.90384086642190198, 70.26145752964252722 ) ) ;
#9888=CARTESIAN_POINT ( 'NONE',  ( 39.31564783533280405, -16.31368208888610383, 72.03616607671141026 ) ) ;
#9894=CARTESIAN_POINT ( 'NONE',  ( 39.29254315202756231, -14.81368208888610205, 69.94417936956672577 ) ) ;
#9899=CARTESIAN_POINT ( 'NONE',  ( 39.75915168707250302, -28.71368208888609175, 70.26145752964249880 ) ) ;
#9900=CARTESIAN_POINT ( 'NONE',  ( 40.17825961694035186, -29.10876147764803079, 70.72098503771240985 ) ) ;
#9906=CARTESIAN_POINT ( 'NONE',  ( 38.37017380507018771, -5.603840866421911926, 69.04448340153881247 ) ) ;
#9910=CARTESIAN_POINT ( 'NONE',  ( 38.93415946300897446, -10.11368208888610987, 73.09843995877331224 ) ) ;
#9917=CARTESIAN_POINT ( 'NONE',  ( 36.11133435605973574, -13.61368208888610454, 72.15350918040385864 ) ) ;
#9926=CARTESIAN_POINT ( 'NONE',  ( 37.12184278917507640, -12.10384086642191193, 71.32335560751961623 ) ) ;
#9927=CARTESIAN_POINT ( 'NONE',  ( 38.93987200065208754, -22.81368208888610383, 70.42958956619168021 ) ) ;
#9933=CARTESIAN_POINT ( 'NONE',  ( 36.07789103942399578, -24.20384086642191690, 72.05058123536544201 ) ) ;
#9934=CARTESIAN_POINT ( 'NONE',  ( 37.69225076346193504, -23.81368208888610027, 72.33091598616823603 ) ) ;
#9936=CARTESIAN_POINT ( 'NONE',  ( 39.12911128074873801, -0.1136820888861071882, 73.69843995877330656 ) ) ;
#9939=CARTESIAN_POINT ( 'NONE',  ( 39.31564783533279694, 0.6961591335780878964, 70.72433947564853440 ) ) ;
#9944=CARTESIAN_POINT ( 'NONE',  ( 35.86008812008917346, -6.103840866421916367, 71.32335560751961623 ) ) ;
#9948=CARTESIAN_POINT ( 'NONE',  ( 36.80608444377001121, -11.31368208888609672, 70.35351908239857721 ) ) ;
#9951=CARTESIAN_POINT ( 'NONE',  ( 39.75915168707250302, -24.71368208888609885, 70.26145752964251301 ) ) ;
#9953=CARTESIAN_POINT ( 'NONE',  ( 39.38009889167648936, -3.403840866421908196, 70.00779233799264034 ) ) ;
#9956=CARTESIAN_POINT ( 'NONE',  ( 39.95015449827720744, -18.61368208888610454, 70.79240656858105751 ) ) ;
#9961=CARTESIAN_POINT ( 'NONE',  ( 37.69796330110505522, -18.50384086642191406, 73.09843995877329803 ) ) ;
#9964=CARTESIAN_POINT ( 'NONE',  ( 39.98359781491296161, -12.41368208888610525, 71.86517103874047052 ) ) ;
#9966=CARTESIAN_POINT ( 'NONE',  ( 36.29569395875879678, -19.31368208888610027, 69.98269868914867686 ) ) ;
#9970=CARTESIAN_POINT ( 'NONE',  ( 38.73920764526923932, -15.50384086642191228, 70.26206559358661252 ) ) ;
#9976=CARTESIAN_POINT ( 'NONE',  ( 36.07789103942399578, -28.20384086642191690, 72.05058123536544201 ) ) ;
#9978=CARTESIAN_POINT ( 'NONE',  ( 35.86008812008917346, -1.513682088886105781, 71.43714994484035685 ) ) ;
#9985=CARTESIAN_POINT ( 'NONE',  ( 36.87297107704151244, -21.90384086642190553, 70.26145752964255564 ) ) ;
#9993=CARTESIAN_POINT ( 'NONE',  ( 38.37017380507018771, -7.603840866421910150, 70.24448340153877268 ) ) ;
#10000=CARTESIAN_POINT ( 'NONE',  ( 37.12184278917507640, -5.513682088886102228, 71.43714994484035685 ) ) ;
#10001=CARTESIAN_POINT ( 'NONE',  ( 37.89291511884476904, -5.113682088886100985, 70.26206559358664094 ) ) ;
#10010=CARTESIAN_POINT ( 'NONE',  ( 39.95015449827720744, -15.00384086642191228, 71.96809898377887293 ) ) ;
#10014=CARTESIAN_POINT ( 'NONE',  ( 39.41296390513587511, -18.41368208888610170, 71.67976084211551324 ) ) ;
#10018=CARTESIAN_POINT ( 'NONE',  ( 38.37017380507020192, -16.01368208888610667, 73.11602215082116629 ) ) ;
#10033=CARTESIAN_POINT ( 'NONE',  ( 39.64521430340305841, -2.803840866421918765, 73.30173637941818754 ) ) ;
#10036=CARTESIAN_POINT ( 'NONE',  ( 39.29254315202756231, -10.81368208888610205, 69.94417936956673998 ) ) ;
#10041=CARTESIAN_POINT ( 'NONE',  ( 37.61123632939165873, -13.91368208888610525, 73.73360434286898624 ) ) ;
#10043=CARTESIAN_POINT ( 'NONE',  ( 1.805559322863034488E-31, -29.10876147765387856, -4.761918834291073356E-14 ) ) ;
#10044=CARTESIAN_POINT ( 'NONE',  ( 39.62658885603860881, -28.92295460646453265, 69.87450580589076310 ) ) ;
#10055=CARTESIAN_POINT ( 'NONE',  ( 38.37017380507020192, -24.01368208888609956, 72.51602215082114355 ) ) ;
#10063=CARTESIAN_POINT ( 'NONE',  ( 36.29569395875881099, -26.30384086642192187, 72.77780686321126780 ) ) ;
#10065=CARTESIAN_POINT ( 'NONE',  ( 37.25202387243752611, -27.21368208888610241, 70.00779233799262613 ) ) ;
#10068=CARTESIAN_POINT ( 'NONE',  ( 38.26194895904384197, -0.6038408664219111488, 72.51602215082118619 ) ) ;
#10074=CARTESIAN_POINT ( 'NONE',  ( 38.26194895904384197, -6.603840866421920808, 73.71602215082116061 ) ) ;
#10078=CARTESIAN_POINT ( 'NONE',  ( 39.98359781491296161, -10.41368208888610347, 71.86517103874048473 ) ) ;
#10081=CARTESIAN_POINT ( 'NONE',  ( 40.14115730948191185, -24.51368208888610312, 71.32335560751960202 ) ) ;
#10084=CARTESIAN_POINT ( 'NONE',  ( 38.82593461698264292, -0.7038408664219141242, 73.13360434286904876 ) ) ;
#10086=CARTESIAN_POINT ( 'NONE',  ( 37.60469502381300799, -26.40384086642190908, 72.26730301774232146 ) ) ;
#10087=CARTESIAN_POINT ( 'NONE',  ( 38.82593461698262871, -14.91368208888609637, 69.62690120949091011 ) ) ;
#10090=CARTESIAN_POINT ( 'NONE',  ( 36.87297107704149823, -11.90384086642190731, 70.26145752964252722 ) ) ;
#10093=CARTESIAN_POINT ( 'NONE',  ( 37.80618814713140097, -11.91368208888611058, 73.13360434286903455 ) ) ;
#10095=CARTESIAN_POINT ( 'NONE',  ( 40.52078840805428683, -18.61368208888610098, 70.60699637195608602 ) ) ;
#10099=CARTESIAN_POINT ( 'NONE',  ( 38.63098279924290068, -20.70384086642191335, 72.53360434286904024 ) ) ;
#10104=CARTESIAN_POINT ( 'NONE',  ( 36.36258059203030513, -19.90384086642191264, 69.89063713639259845 ) ) ;
#10106=CARTESIAN_POINT ( 'NONE',  ( 40.52078840805428683, 1.386317911113894130, 70.60699637195612866 ) ) ;
#10113=CARTESIAN_POINT ( 'NONE',  ( 36.87297107704151244, -23.90384086642190553, 70.26145752964252722 ) ) ;
#10118=CARTESIAN_POINT ( 'NONE',  ( 38.73920764526923932, -1.503840866421912725, 70.26206559358664094 ) ) ;
#10121=CARTESIAN_POINT ( 'NONE',  ( 38.82593461698262871, -28.91368208888610525, 69.62690120949091011 ) ) ;
#10126=CARTESIAN_POINT ( 'NONE',  ( 38.73920764526925353, -6.113682088886101873, 72.49843995877331793 ) ) ;
#10127=CARTESIAN_POINT ( 'NONE',  ( 39.41296390513587511, -2.413682088886099919, 71.67976084211552745 ) ) ;
#10134=CARTESIAN_POINT ( 'NONE',  ( 38.82593461698265003, -8.703840866421909794, 73.13360434286904876 ) ) ;
#10142=CARTESIAN_POINT ( 'NONE',  ( 37.33957961208646736, -9.813682088886107380, 72.81632618279323310 ) ) ;
#10156=CARTESIAN_POINT ( 'NONE',  ( 40.52078840805429394, -7.003840866421914058, 72.15350918040385864 ) ) ;
#10159=CARTESIAN_POINT ( 'NONE',  ( 39.95015449827720744, -10.61368208888610631, 70.79240656858107172 ) ) ;
#10162=CARTESIAN_POINT ( 'NONE',  ( 36.07789103942398867, -17.41368208888610525, 70.70992431699450265 ) ) ;
#10172=CARTESIAN_POINT ( 'NONE',  ( 38.73920764526925353, -26.11368208888610454, 72.49843995877328950 ) ) ;
#10178=CARTESIAN_POINT ( 'NONE',  ( 40.55423172469004101, -21.20384086642191690, 70.70992431699450265 ) ) ;
#10179=CARTESIAN_POINT ( 'NONE',  ( 36.49096545463212493, -25.51368208888609956, 71.43714994484030001 ) ) ;
#10190=CARTESIAN_POINT ( 'NONE',  ( 37.50301148336529877, -2.503840866421917166, 73.69843995877330656 ) ) ;
#10196=CARTESIAN_POINT ( 'NONE',  ( 39.95015449827720744, -10.61368208888610631, 70.79240656858107172 ) ) ;
#10205=CARTESIAN_POINT ( 'NONE',  ( 37.38336156205273397, -25.90384086642191264, 70.63227792289245599 ) ) ;
#10206=CARTESIAN_POINT ( 'NONE',  ( 39.82603832034400426, -12.31368208888610560, 72.40698646996133903 ) ) ;
#10210=CARTESIAN_POINT ( 'NONE',  ( 37.25202387243754032, -12.40384086642191619, 72.75271321436731853 ) ) ;
#10212=CARTESIAN_POINT ( 'NONE',  ( 39.95015449827720744, -14.61368208888610454, 70.79240656858105751 ) ) ;
#10214=CARTESIAN_POINT ( 'NONE',  ( 40.55423172469004811, -14.41368208888610347, 72.05058123536544201 ) ) ;
#10218=CARTESIAN_POINT ( 'NONE',  ( 37.21915885897815457, -16.20384086642190979, 71.67976084211552745 ) ) ;
#10223=CARTESIAN_POINT ( 'NONE',  ( 40.26954217208372455, -24.90384086642191619, 72.86986841596730358 ) ) ;
#10228=CARTESIAN_POINT ( 'NONE',  ( 37.33957961208646736, -25.81368208888610738, 72.81632618279320468 ) ) ;
#10234=CARTESIAN_POINT ( 'NONE',  ( 38.26194895904384907, -18.60384086642191548, 73.11602215082116629 ) ) ;
#10240=CARTESIAN_POINT ( 'NONE',  ( 38.93415946300896024, -29.50384086642191050, 69.66206559358660400 ) ) ;
#10250=CARTESIAN_POINT ( 'NONE',  ( 39.51027997493896748, -4.513682088886101340, 71.32335560751961623 ) ) ;
#10252=CARTESIAN_POINT ( 'NONE',  ( 38.73920764526925353, -2.113682088886101873, 72.49843995877331793 ) ) ;
#10258=CARTESIAN_POINT ( 'NONE',  ( 36.87297107704149823, -13.90384086642190908, 70.26145752964252722 ) ) ;
#10268=CARTESIAN_POINT ( 'NONE',  ( 39.75915168707250302, -6.713682088886100630, 70.26145752964255564 ) ) ;
#10284=CARTESIAN_POINT ( 'NONE',  ( 40.55423172469004101, -5.203840866421914235, 70.70992431699450265 ) ) ;
#10288=CARTESIAN_POINT ( 'NONE',  ( 39.38009889167650357, -8.213682088886105959, 72.75271321436733274 ) ) ;
#10292=CARTESIAN_POINT ( 'NONE',  ( 36.36258059203031934, -15.71368208888610773, 72.86986841596736042 ) ) ;
#10301=CARTESIAN_POINT ( 'NONE',  ( 37.69225076346193504, -25.81368208888610027, 72.33091598616823603 ) ) ;
#10310=CARTESIAN_POINT ( 'NONE',  ( 39.02088643472237806, -20.70384086642192401, 73.73360434286898624 ) ) ;
#10311=CARTESIAN_POINT ( 'NONE',  ( 39.95015449827720744, -24.61368208888610454, 70.79240656858104330 ) ) ;
#10318=CARTESIAN_POINT ( 'NONE',  ( 36.29569395875881099, -6.303840866421917433, 72.77780686321129622 ) ) ;
#10321=CARTESIAN_POINT ( 'NONE',  ( 37.80618814713140097, -5.913682088886107024, 73.13360434286904876 ) ) ;
#10324=CARTESIAN_POINT ( 'NONE',  ( 36.49096545463212493, -27.51368208888610312, 71.43714994484031422 ) ) ;
#10329=CARTESIAN_POINT ( 'NONE',  ( 38.73920764526923932, -23.50384086642191050, 70.26206559358661252 ) ) ;
#10330=CARTESIAN_POINT ( 'NONE',  ( 40.14115730948191185, -14.51368208888610667, 71.32335560751960202 ) ) ;
#10333=CARTESIAN_POINT ( 'NONE',  ( 39.75915168707251723, -12.90384086642191797, 72.49904802271738902 ) ) ;
#10336=CARTESIAN_POINT ( 'NONE',  ( 38.82593461698262871, -8.913682088886101695, 69.62690120949091011 ) ) ;
#10338=CARTESIAN_POINT ( 'NONE',  ( 37.61123632939165873, -15.91368208888610880, 73.73360434286898624 ) ) ;
#10343=CARTESIAN_POINT ( 'NONE',  ( 38.37017380507018771, -17.60384086642191193, 70.24448340153875847 ) ) ;
#10348=CARTESIAN_POINT ( 'NONE',  ( 40.33642880535521869, -23.30384086642191477, 69.98269868914866265 ) ) ;
#10350=CARTESIAN_POINT ( 'NONE',  ( 38.82593461698262871, -28.91368208888610525, 69.62690120949091011 ) ) ;
#10356=CARTESIAN_POINT ( 'NONE',  ( 36.64852494920107517, -12.20384086642190979, 71.86517103874048473 ) ) ;
#10365=CARTESIAN_POINT ( 'NONE',  ( 37.69796330110505522, -28.50384086642191406, 73.09843995877328382 ) ) ;
#10374=CARTESIAN_POINT ( 'NONE',  ( 38.37017380507020192, -6.013682088886104005, 72.51602215082118619 ) ) ;
#10375=CARTESIAN_POINT ( 'NONE',  ( 37.89291511884476904, -7.113682088886103649, 70.26206559358664094 ) ) ;
#10384=CARTESIAN_POINT ( 'NONE',  ( 36.68196826583682935, -10.00384086642191406, 70.79240656858108593 ) ) ;
#10394=CARTESIAN_POINT ( 'NONE',  ( 36.49096545463212493, -7.513682088886103116, 71.43714994484035685 ) ) ;
#10399=CARTESIAN_POINT ( 'NONE',  ( 36.87297107704152666, -23.71368208888610951, 72.49904802271738902 ) ) ;
#10400=CARTESIAN_POINT ( 'NONE',  ( 39.86436010876736447, -29.10876147765401711, 70.06288980751138240 ) ) ;
#10409=CARTESIAN_POINT ( 'NONE',  ( 39.02088643472237806, -2.703840866421919120, 73.73360434286902887 ) ) ;
#10410=CARTESIAN_POINT ( 'NONE',  ( 37.31647492878122563, -23.31368208888610383, 70.72433947564853440 ) ) ;
#10415=CARTESIAN_POINT ( 'NONE',  ( 36.87297107704152666, -9.713682088886107735, 72.49904802271743165 ) ) ;
#10419=CARTESIAN_POINT ( 'NONE',  ( 36.07789103942398867, -13.41368208888610525, 70.70992431699450265 ) ) ;
#10426=CARTESIAN_POINT ( 'NONE',  ( 39.60177068742361683, -28.78761913971833408, 70.01260438786866303 ) ) ;
#10431=CARTESIAN_POINT ( 'NONE',  ( 39.37952058850012804, -26.61368208888610809, 70.97781676520600058 ) ) ;
#10439=CARTESIAN_POINT ( 'NONE',  ( 39.02088643472237806, -24.70384086642192401, 73.73360434286898624 ) ) ;
#10441=CARTESIAN_POINT ( 'NONE',  ( 36.64852494920107517, -27.41368208888610525, 70.89533451361945993 ) ) ;
#10449=CARTESIAN_POINT ( 'NONE',  ( 36.98690846071097127, -1.803840866421911215, 69.45876917294177133 ) ) ;
#10451=CARTESIAN_POINT ( 'NONE',  ( 38.37017380507020192, 1.986317911113890444, 73.11602215082119471 ) ) ;
#10455=CARTESIAN_POINT ( 'NONE',  ( 38.93415946300897446, -8.113682088886108090, 73.09843995877331224 ) ) ;
#10461=( BOUNDED_SURFACE ( )  B_SPLINE_SURFACE ( 3, 2, ( 
 ( #15680, #23527, #13760, #9899, #3962, #11834, #2017, #82, #7967, #22585, #14723, #7257, #11129, #1061, #15105, #16663, #1322, #13062, #591, #8468, #5201, #2518, #7001, #4941, #20915, #5328, #3251, #12810, #11263, #20185, #24492, #22841, #22965, #10996, #10875, #9332, #9208, #6868, #16923, #5073, #18981, #15232, #23083, #12938, #18728, #20658, #2993, #17176, #17054, #14850, #24878, #20793, #21042, #10399, #16788, #13190, #12343, #18263, #3384, #8939, #25001, #24619, #22710, #19112, #3127, #18850, #1190, #9079, #1450, #24754, #7131, #7390, #14985, #17684, #11641, #21666, #15611, #19477, #17430, #1944, #11769, #17817, #3895, #1688, #21286, #9830, #23465, #15, #23598, #7898, #23332, #3629, #21549, #19603, #11514, #4019, #9581, #148, #15745, #5830, #13436, #25125, #25259, #5962, #9956, #13811, #25384, #5699, #7642, #7768, #1821, #17557, #11893, #19354, #15484, #19735, #8027, #5448, #13563, #2076, #15867, #21416, #3759, #13317, #15359, #9707, #21169, #7508, #3510, #13689, #11383, #23209, #19225, #1564, #9456, #17305, #5579, #6461, #21923, #18440, #4285, #10087, #8662, #14319, #4156, #10330, #24210, #8274, #16114, #22173, #20240, #22046, #23968, #6343, #2328, #771, #521, #12401, #12275, #18068, #12535, #14203, #2702, #8406, #16244, #10584, #4407, #10206, #24090, #20118, #8525, #14069, #14446, #2452, #19992, #23716, #6586, #16362, #2579, #18191, #4536, #10463, #18322, #641, #12024, #12155, #20371, #390, #6084, #22294, #13942, #4657, #21798, #19866, #2209, #17946, #264, #8142, #15987, #23841, #6212, #14567, #22678, #6709, #22926, #16889, #15072, #21008, #13156, #20878, #3350, #1418, #18950, #24720, #11226, #9045, #3216, #16493, #6969, #14952, #10842, #18564, #7094, #22424, #18693, #12782, #20493, #1289, #22809, #1027, #9172, #19076, #14820, #5287, #4775, #5034, #24586, #12905, #20759, #20625, #12654, #14688, #1152, #24337, #3092, #16624, #2828, #2957, #8911, #10719, #895, #8788, #17019, #24464, #16751, #6836, #5171, #4905, #10962, #18815, #13026, #11094, #24852, #7227, #22553, #23178, #17653, #21637, #9302, #1654, #23436, #20343, #13406, #19320, #15711, #19196, #9545, #21512, #11353, #5928, #3598, #21254, #25092, #11480, #24968, #17395, #3478, #21135, #1530, #9421, #3862, #7733, #5546, #11741, #13284, #5801, #9680, #23052, #5417, #1788, #7349, #25228, #17267, #17529, #1914, #25353, #7475, #7868, #17143, #15327, #19442 ),
 ( #11865, #19700, #7612, #15454, #23298, #5664, #13785, #15577, #13529, #13659, #21383, #23562, #15196, #3727, #19575, #11604, #9798, #3989, #17916, #4501, #11996, #23811, #8373, #13910, #10431, #19834, #14039, #12241, #2297, #10172, #2424, #6054, #10301, #19965, #24066, #16087, #18039, #15956, #20084, #4378, #20214, #22018, #234, #2175, #18164, #23937, #488, #16215, #6435, #21894, #10055, #14289, #22139, #8114, #12374, #6184, #2550, #2048, #14173, #4254, #21765, #12124, #9927, #17785, #113, #6312, #7997, #15835, #8242, #23689, #358, #4125, #7694, #5757, #15540, #3688, #5511, #23268, #9761, #4084, #23389, #25182, #21728, #11572, #1745, #2133, #23660, #7440, #17742, #15288, #25319, #15422, #25446, #13491, #11956, #19281, #15671, #13375, #23520, #2005, #21606, #7825, #5629, #19795, #21341, #11438, #10014, #5889, #21222, #11701, #75, #9642, #17494, #13750, #3952, #13621, #21473, #3818, #19407, #25054, #1876, #11826, #19540, #17614, #13872, #19665, #23139, #9888, #7958, #3559, #15803, #6016, #1618, #9512, #17356, #7574, #1481, #15658, #1609, #23507, #23256, #3676, #19528, #9630, #17730, #7431, #13478, #17600, #9373, #15279, #1990, #5615, #13858, #17346, #11559, #9872, #11426, #19781, #25170, #17481, #5876, #23378, #5745, #13736, #21209, #21594, #15526, #61, #1865, #13611, #21329, #3941, #11812, #21714, #7813, #19395, #7563, #19651, #9751, #7945, #15789, #23646, #1732, #15412, #25428, #6005, #25308, #4070, #7683, #11942, #17223, #25044, #21460, #3549, #23128, #5500, #3803, #13363, #19271, #11690, #9500, #8574, #12067, #12195, #14363, #4195, #24259, #21968, #14114, #17986, #4331, #17864, #20033, #21840, #13991, #19914, #2252, #22218, #566, #16037, #4583, #6131, #16283, #2500, #15908, #23764, #20164, #188, #2373, #10126, #10374, #20295, #18241, #311, #686, #10000, #8190, #12319, #12450, #439, #23889, #6629, #24130, #6253, #6387, #10250, #8447, #4706, #12581, #18117, #8320, #6506, #16159, #2629, #24010, #14243, #10507, #22088, #18360, #8067, #4451, #16410, #2119, #14489, #22347, #8836, #24888, #2873, #22597, #13074, #22470, #5339, #10763, #20670, #9091, #8953, #16798, #24764, #6761, #7144, #1070, #11142, #5086, #24631, #6881, #16933, #1202, #7267, #18863, #16674, #18603, #14997, #12950, #22850, #20925, #5211, #12822, #945, #11007, #3266, #24507, #18993, #14736, #15118, #1334, #20802, #4953, #14614, #3004, #9221, #22975 ),
 ( #10885, #17069, #20411, #18738, #2744, #3137, #10633, #18484, #7012, #14860, #819, #22722, #8705, #16536, #24388, #4819, #12699, #20539, #25273, #25012, #17568, #11526, #23223, #3771, #5712, #5589, #19123, #19236, #9840, #9467, #28, #11782, #3398, #13447, #17317, #9342, #13575, #17446, #17188, #19614, #1957, #13331, #25396, #11278, #19366, #1462, #17697, #21428, #7909, #15756, #23612, #7782, #13205, #21055, #15625, #11655, #7402, #19493, #23477, #15247, #3640, #1834, #7526, #23099, #9717, #5461, #15373, #25138, #21182, #5841, #13702, #21298, #21561, #3520, #1700, #11395, #1574, #9596, #7653, #15494, #23346, #3909, #11905, #4168, #16128, #10478, #14082, #6096, #2593, #10099, #8157, #8542, #4550, #13824, #24102, #21681, #6225, #21809, #6359, #19880, #18333, #160, #22056, #19746, #4420, #8418, #2466, #14216, #12036, #657, #2221, #17829, #16375, #12287, #2090, #18082, #6475, #16000, #23851, #20130, #10343, #4300, #21936, #12166, #17957, #5973, #8287, #18205, #20002, #277, #533, #2342, #22185, #23980, #10218, #403, #16257, #14332, #4032, #12416, #20255, #9970, #8038, #15878, #23731, #13952, #20773, #16640, #22438, #14832, #5047, #4788, #14964, #20509, #11108, #3103, #24599, #6725, #18453, #2841, #10976, #3229, #7109, #18705, #24474, #910, #1041, #4920, #10856, #18828, #12667, #10729, #22823, #18962, #24223, #6847, #12919, #5184, #18575, #8800, #13037, #8675, #14703, #1166, #783, #20894, #22565, #12792, #14580, #20636, #14458, #2971, #16506, #10602, #24350, #8921, #9059, #22690, #16765, #16901, #2714, #24733, #6982, #12548, #20384, #1301, #22312, #9187, #6599, #4670, #9692, #25241, #19092, #15591, #24863, #13169, #1666, #11617, #15342, #15212, #13671, #5679, #3365, #21267, #9435, #23313, #19588, #1927, #17281, #23064, #13542, #9315, #21398, #5430, #11366, #9561, #25105, #25365, #15086, #21149, #7624, #17033, #22940, #17542, #13298, #21526, #24983, #19208, #7750, #1432, #7240, #7362, #7488, #3740, #5559, #13419, #19458, #11242, #1800, #3492, #23449, #1545, #3874, #5815, #17408, #23191, #17157, #3611, #11753, #5305, #21023, #11494, #19334, #15466, #12490, #16319, #22256, #6666, #8010, #23701, #18520, #22509, #9812, #2188, #24298, #851, #13925, #19846, #16578, #19714, #10068, #22385, #11879, #6800, #4138, #21780, #129, #12007, #25488, #17927, #4003, #21650, #2061, #9939, #4741, #8611, #6065, #12614, #13796, #14528, #10547 ),
 ( #17798, #8742, #17668, #5940, #20333, #20453, #8485, #15846, #14649, #2784, #608, #14401, #24167, #16449, #12736, #20579, #6542, #4616, #10674, #2665, #24427, #18396, #727, #4862, #7880, #15727, #23577, #7050, #11184, #2912, #8873, #21095, #16843, #7437, #10926, #5129, #3440, #4992, #13371, #18774, #3177, #17107, #16973, #24806, #7309, #14778, #15160, #9129, #19157, #13116, #7186, #14902, #24924, #9261, #15285, #1375, #24678, #1110, #23013, #20967, #5378, #11317, #13245, #20839, #8995, #19033, #18646, #12990, #22636, #12858, #20712, #3047, #1494, #9380, #22762, #17229, #6926, #25052, #3308, #16711, #24544, #23135, #985, #11047, #18904, #5507, #10795, #1248, #15033, #22888, #5250, #17353, #5884, #15798, #19537, #19405, #17872, #9882, #7571, #25439, #13618, #1999, #23774, #6138, #21468, #1741, #17738, #13488, #70, #9639, #15536, #13747, #3814, #4079, #19278, #25316, #3949, #21217, #1616, #13866, #17491, #196, #3685, #23385, #21725, #23264, #3556, #11567, #11699, #7954, #9759, #17610, #23656, #15420, #6013, #1874, #11951, #21602, #7821, #7690, #19790, #2127, #8077, #19661, #5754, #15667, #10010, #11821, #15916, #11436, #9509, #23515, #25178, #5625, #21338, #12202, #4713, #10258, #825, #10514, #14371, #21975, #8199, #18124, #18367, #18494, #22355, #8456, #6395, #16167, #16291, #20172, #573, #694, #20041, #2384, #12588, #8712, #13999, #14252, #2636, #20419, #448, #24020, #2751, #23897, #22096, #8584, #16047, #10643, #8328, #4461, #4340, #12330, #2508, #4205, #10384, #6262, #320, #14125, #18249, #16419, #12459, #24139, #24267, #17995, #6637, #22228, #2260, #10134, #6514, #12075, #4590, #20304, #14497, #16544, #24396, #21847, #19922, #14623, #2882, #16940, #1341, #5095, #4962, #3405, #20934, #18611, #11016, #24640, #13080, #9348, #17195, #7020, #12831, #3275, #24516, #11148, #20677, #1079, #24771, #14868, #15126, #4826, #10893, #15004, #6770, #12707, #24895, #3013, #11286, #14744, #8962, #7274, #8843, #22478, #22605, #22729, #19000, #20811, #3145, #9229, #954, #17077, #12958, #22982, #7153, #18872, #18746, #5348, #13213, #19129, #5218, #16807, #1209, #21062, #22857, #1470, #20548, #10770, #9097, #16683, #6889, #5848, #23230, #15763, #21306, #11913, #21568, #25402, #7535, #19243, #3647, #3916, #4038, #7914, #19503, #17455, #1707, #1842, #5719, #11662, #11789, #5595, #13453, #23622, #19753, #25021, #25280, #13710, #5980 ),
 ( #11534, #15381, #2096, #15500, #13832, #15256, #23352, #7659, #13582, #21434, #19374, #5468, #9605, #9723, #9976, #3778, #25147, #21687, #17575, #7787, #7410, #23105, #13338, #17705, #21189, #15635, #23483, #19620, #1963, #3527, #1581, #9848, #11403, #36, #9475, #17323, #539, #16007, #12554, #23857, #4174, #2719, #8424, #23738, #4425, #18338, #2348, #10223, #16262, #14337, #16133, #18090, #410, #21941, #20389, #20136, #6480, #6364, #12171, #6604, #8292, #22319, #2474, #10348, #4677, #23985, #4307, #18210, #14222, #2598, #8164, #8547, #22061, #17835, #24107, #12293, #12041, #22192, #4555, #12423, #20262, #10484, #662, #6102, #6230, #14463, #14087, #166, #16380, #8044, #24229, #20007, #13958, #15883, #21814, #19887, #2227, #10104, #17963, #282, #8680, #16770, #790, #17039, #10982, #9193, #15093, #7245, #14970, #22947, #21029, #13044, #18834, #5312, #3110, #22828, #10607, #1048, #9065, #4926, #12672, #1172, #16513, #12798, #6852, #14586, #20900, #16909, #20641, #3235, #13176, #18458, #10862, #16647, #24739, #2846, #7115, #24480, #2977, #20779, #18712, #18968, #24357, #14708, #5189, #6733, #22443, #11114, #22570, #4793, #18580, #8927, #1307, #20514, #10735, #917, #24605, #24868, #6988, #14838, #8807, #22696, #5053, #12924, #19593, #13548, #17416, #15347, #25374, #9697, #15734, #1806, #25112, #19214, #7755, #21403, #15597, #21534, #23453, #21274, #1550, #19465, #17547, #9441, #1934, #7495, #23583, #5820, #3745, #11371, #23070, #23196, #13677, #7885, #11759, #23320, #3616, #5565, #5685, #9568, #15472, #3882, #17288, #13424, #9819, #5947, #3371, #11500, #17673, #5, #19340, #1673, #13801, #13304, #25247, #11249, #5436, #19098, #7630, #11625, #1437, #9320, #17164, #24989, #21155, #15218, #3497, #7370, #16235, #20102, #10074, #24080, #135, #10318, #22035, #9944, #17804, #14189, #11883, #15973, #23706, #4396, #14308, #12258, #6073, #20229, #4010, #8015, #6329, #6451, #19982, #19852, #18311, #18181, #15853, #376, #14056, #2441, #21656, #2065, #22155, #17932, #632, #4145, #23828, #4520, #13930, #6570, #12012, #21909, #505, #10190, #18053, #8393, #21786, #12389, #2312, #2568, #10449, #8260, #8130, #8514, #16351, #24199, #19721, #249, #2195, #6201, #4272, #12142, #16101, #23955, #6826, #12640, #5022, #20743, #20482, #5155, #10708, #1279, #10950, #14808, #22413, #8646, #18553, #18802, #18937, #22796, #8900, #14672, #16609 ),
 ( #22542, #3079, #13014, #877, #24454, #20864, #24323, #4891, #1141, #16476, #11082, #8773, #12770, #4763, #20614, #4645, #2944, #6695, #759, #14556, #2816, #9028, #12893, #10825, #16877, #18429, #24708, #22667, #2692, #10572, #6956, #12523, #18679, #1015, #7080, #14938, #3206, #16740, #9158, #22282, #24573, #17006, #24839, #14432, #20359, #3848, #21367, #19065, #11468, #25080, #13520, #9786, #17644, #7466, #13269, #3711, #24952, #11594, #21125, #1519, #17383, #15315, #15566, #5277, #11344, #15443, #19428, #1407, #19305, #23164, #1777, #7216, #15058, #5537, #3469, #9669, #7338, #17517, #19187, #9407, #25214, #13399, #23421, #13144, #17255, #23291, #22914, #20998, #25342, #21246, #11730, #15184, #3585, #7722, #9291, #3337, #23042, #1642, #5786, #9536, #7600, #13645, #17133, #21499, #5652, #19564, #1899, #11214, #5407, #22011, #6300, #12363, #23927, #21753, #15826, #4365, #10162, #12227, #18153, #20073, #17903, #23681, #16076, #14162, #6043, #16203, #4115, #20205, #2414, #349, #7986, #19691, #11986, #10292, #4493, #8363, #19952, #226, #2164, #2286, #6169, #12113, #476, #13897, #19824, #24056, #2537, #25475, #8103, #6427, #14276, #10041, #15947, #22127, #9917, #23801, #10419, #2036, #7857, #14030, #21884, #4243, #18028, #15698, #8231, #17773, #11851, #99, #23546, #5917, #13776, #21630, #3977, #22259, #6929, #18650, #6545, #14405, #10797, #8490, #12617, #20337, #990, #10928, #8876, #2668, #16847, #610, #4619, #2915, #12860, #16581, #16452, #14905, #8997, #16713, #6802, #4743, #14781, #24546, #5134, #22641, #14532, #8613, #4995, #20714, #3052, #18777, #1112, #10678, #24300, #24681, #7055, #6668, #22764, #22389, #12992, #20841, #3179, #730, #12493, #20455, #18285, #16322, #24169, #12742, #18523, #2789, #20582, #24431, #4864, #10549, #854, #8744, #18401, #14651, #22512, #3780, #38, #19756, #15502, #21438, #17838, #20970, #11665, #23625, #13118, #8046, #5722, #23356, #1380, #13585, #1252, #19505, #5252, #22890, #3311, #11188, #5982, #9850, #24926, #13834, #15035, #7916, #11791, #24810, #7190, #3918, #9132, #1844, #19036, #19622, #4041, #1968, #9265, #9978, #18907, #17109, #21570, #21689, #9724, #7311, #15885, #15767, #17578, #15638, #25407, #17708, #13961, #21816, #7790, #23484, #11916, #5852, #2097, #13713, #167, #23740, #6105, #11049, #16978, #8294, #12425, #4176, #10106, #22321, #18092, #8682, #12173, #6366, #4680 ),
 ( #16383, #10350, #12296, #18212, #20141, #16135, #17965, #2350, #14339, #16515, #2477, #4309, #793, #23988, #14224, #6737, #2721, #12043, #12556, #19890, #4427, #20010, #4560, #413, #24362, #23860, #20264, #286, #2601, #6607, #664, #10486, #10228, #14590, #22063, #16010, #2229, #18340, #8168, #16264, #20391, #542, #8426, #8549, #24231, #24109, #6482, #22194, #14467, #6232, #10609, #18460, #14089, #21944, #11252, #22699, #1440, #7119, #14974, #9323, #5058, #8929, #22830, #6990, #7247, #12800, #13179, #3116, #22446, #5192, #9069, #8813, #1310, #20782, #14841, #13050, #20903, #12927, #2850, #2980, #19102, #18718, #17167, #21033, #12675, #10986, #1051, #18583, #3239, #1177, #920, #3374, #24991, #22573, #9196, #20517, #18837, #10739, #7378, #11117, #4796, #16651, #24482, #17043, #6855, #14711, #24870, #18972, #4930, #15095, #22953, #20644, #16913, #5316, #16773, #10866, #24609, #24742, #9571, #11503, #19216, #7, #21540, #17419, #7888, #2068, #5688, #4013, #5439, #13552, #1553, #25116, #17294, #9821, #13680, #3619, #17676, #9446, #3886, #15601, #3500, #11374, #7758, #13307, #25250, #7498, #23456, #15736, #5822, #15350, #13804, #23074, #23200, #25376, #23587, #21406, #13427, #11887, #11762, #5568, #19467, #7633, #19596, #17807, #139, #15475, #21277, #1937, #19342, #5953, #1679, #23322, #21659, #3749, #19725, #21159, #11630, #9948, #15220, #1811, #9700, #17550, #12527, #15975, #10196, #635, #10078, #18432, #23832, #8263, #22160, #22038, #4399, #12392, #19855, #20233, #14193, #24201, #18184, #12262, #19985, #4526, #14311, #20365, #6454, #4275, #6203, #2570, #510, #10455, #8518, #18314, #380, #14059, #24083, #16354, #21912, #6574, #12146, #2695, #14437, #8396, #2316, #2198, #18057, #22286, #10578, #4648, #2445, #16106, #23958, #10321, #20109, #16238, #8019, #6333, #15858, #23709, #6076, #13934, #21790, #4147, #12016, #17936, #255, #8133, #10711, #10830, #13018, #2820, #22919, #20618, #12774, #16614, #2949, #16481, #18684, #20486, #4896, #9035, #762, #6699, #18943, #14681, #5280, #8778, #1020, #1282, #18557, #11218, #24458, #8904, #14943, #14812, #22671, #5160, #12647, #20871, #6961, #17010, #10955, #5027, #16745, #22800, #7086, #13148, #24712, #22546, #6830, #3210, #18809, #11087, #9164, #24845, #24580, #12897, #16880, #7220, #20747, #15062, #3085, #21000, #3342, #1145, #8652, #884, #24329, #14560, #22418, #4769, #17387 ) ),
 .UNSPECIFIED., .T., .F., .F. ) 
 B_SPLINE_SURFACE_WITH_KNOTS ( ( 4, 3, 4 ),
 ( 3, 2, 2, 2, 2, 2, 2, 2, 2, 2, 2, 2, 2, 2, 2, 2, 2, 2, 2, 2, 2, 2, 2, 2, 2, 2, 2, 2, 2, 2, 2, 2, 2, 2, 2, 2, 2, 2, 2, 2, 2, 2, 2, 2, 2, 2, 2, 2, 2, 2, 2, 2, 2, 2, 2, 2, 2, 2, 2, 2, 2, 2, 2, 2, 2, 2, 2, 2, 2, 2, 2, 2, 2, 2, 2, 2, 2, 2, 2, 2, 2, 2, 2, 2, 2, 2, 2, 2, 2, 2, 2, 2, 2, 2, 2, 2, 2, 2, 2, 2, 2, 2, 2, 2, 2, 2, 2, 2, 2, 2, 2, 2, 2, 2, 2, 2, 2, 2, 2, 2, 2, 2, 2, 2, 2, 2, 2, 2, 2, 2, 2, 2, 2, 2, 2, 2, 2, 2, 2, 2, 2, 2, 2, 2, 2, 2, 2, 2, 2, 2, 2, 2, 2, 2, 2, 3 ),
 ( 0.000000000000000000, 0.5000000000000000000, 1.000000000000000000 ),
 ( 0.000000000000000000, 0.006250000000000000347, 0.01250000000000000069, 0.01874999999999999931, 0.02500000000000000139, 0.03125000000000000000, 0.03749999999999999861, 0.04374999999999999722, 0.05000000000000000278, 0.05625000000000000139, 0.06250000000000000000, 0.06875000000000000555, 0.07499999999999999722, 0.08125000000000000278, 0.08749999999999999445, 0.09375000000000000000, 0.1000000000000000056, 0.1062499999999999972, 0.1125000000000000028, 0.1187499999999999944, 0.1250000000000000000, 0.1312500000000000056, 0.1375000000000000111, 0.1437499999999999889, 0.1499999999999999944, 0.1562500000000000000, 0.1625000000000000056, 0.1687500000000000111, 0.1749999999999999889, 0.1812499999999999944, 0.1875000000000000000, 0.1937500000000000056, 0.2000000000000000111, 0.2062499999999999889, 0.2124999999999999944, 0.2187500000000000000, 0.2250000000000000056, 0.2312500000000000111, 0.2374999999999999889, 0.2437499999999999944, 0.2500000000000000000, 0.2562499999999999778, 0.2625000000000000111, 0.2687499999999999889, 0.2750000000000000222, 0.2812500000000000000, 0.2874999999999999778, 0.2937500000000000111, 0.2999999999999999889, 0.3062500000000000222, 0.3125000000000000000, 0.3187499999999999778, 0.3250000000000000111, 0.3312499999999999889, 0.3375000000000000222, 0.3437500000000000000, 0.3499999999999999778, 0.3562500000000000111, 0.3624999999999999889, 0.3687500000000000222, 0.3750000000000000000, 0.3812499999999999778, 0.3875000000000000111, 0.3937499999999999889, 0.4000000000000000222, 0.4062500000000000000, 0.4124999999999999778, 0.4187500000000000111, 0.4249999999999999889, 0.4312500000000000222, 0.4375000000000000000, 0.4437499999999999778, 0.4500000000000000111, 0.4562499999999999889, 0.4625000000000000222, 0.4687500000000000000, 0.4749999999999999778, 0.4812500000000000111, 0.4874999999999999889, 0.4937500000000000222, 0.5000000000000000000, 0.5062499999999999778, 0.5124999999999999556, 0.5187500000000000444, 0.5250000000000000222, 0.5312500000000000000, 0.5374999999999999778, 0.5437499999999999556, 0.5500000000000000444, 0.5562500000000000222, 0.5625000000000000000, 0.5687499999999999778, 0.5749999999999999556, 0.5812500000000000444, 0.5875000000000000222, 0.5937500000000000000, 0.5999999999999999778, 0.6062499999999999556, 0.6125000000000000444, 0.6187500000000000222, 0.6250000000000000000, 0.6312499999999999778, 0.6374999999999999556, 0.6437500000000000444, 0.6500000000000000222, 0.6562500000000000000, 0.6624999999999999778, 0.6687499999999999556, 0.6750000000000000444, 0.6812500000000000222, 0.6875000000000000000, 0.6937499999999999778, 0.6999999999999999556, 0.7062500000000000444, 0.7125000000000000222, 0.7187500000000000000, 0.7249999999999999778, 0.7312499999999999556, 0.7375000000000000444, 0.7437500000000000222, 0.7500000000000000000, 0.7562499999999999778, 0.7624999999999999556, 0.7687500000000000444, 0.7750000000000000222, 0.7812500000000000000, 0.7874999999999999778, 0.7937499999999999556, 0.8000000000000000444, 0.8062500000000000222, 0.8125000000000000000, 0.8187499999999999778, 0.8249999999999999556, 0.8312500000000000444, 0.8375000000000000222, 0.8437500000000000000, 0.8499999999999999778, 0.8562499999999999556, 0.8625000000000000444, 0.8687500000000000222, 0.8750000000000000000, 0.8812499999999999778, 0.8874999999999999556, 0.8937500000000000444, 0.9000000000000000222, 0.9062500000000000000, 0.9124999999999999778, 0.9187499999999999556, 0.9250000000000000444, 0.9312500000000000222, 0.9375000000000000000, 0.9437499999999999778, 0.9499999999999999556, 0.9562500000000000444, 0.9625000000000000222, 0.9687500000000000000 ),
 .UNSPECIFIED. ) 
 GEOMETRIC_REPRESENTATION_ITEM ( )  RATIONAL_B_SPLINE_SURFACE ( (
 ( 1.000000000000000000, 0.9510565162951535312, 1.000000000000000000, 0.9510565162951535312, 1.000000000000000000, 0.9510565162951535312, 1.000000000000000000, 0.9510565162951535312, 1.000000000000000000, 0.9510565162951535312, 1.000000000000000000, 0.9510565162951535312, 1.000000000000000000, 0.9510565162951535312, 1.000000000000000000, 0.9510565162951535312, 1.000000000000000000, 0.9510565162951535312, 1.000000000000000000, 0.9510565162951535312, 1.000000000000000000, 0.9510565162951535312, 1.000000000000000000, 0.9510565162951535312, 1.000000000000000000, 0.9510565162951535312, 1.000000000000000000, 0.9510565162951535312, 1.000000000000000000, 0.9510565162951535312, 1.000000000000000000, 0.9510565162951535312, 1.000000000000000000, 0.9510565162951535312, 1.000000000000000000, 0.9510565162951535312, 1.000000000000000000, 0.9510565162951535312, 1.000000000000000000, 0.9510565162951535312, 1.000000000000000000, 0.9510565162951535312, 1.000000000000000000, 0.9510565162951535312, 1.000000000000000000, 0.9510565162951535312, 1.000000000000000000, 0.9510565162951535312, 1.000000000000000000, 0.9510565162951535312, 1.000000000000000000, 0.9510565162951535312, 1.000000000000000000, 0.9510565162951535312, 1.000000000000000000, 0.9510565162951535312, 1.000000000000000000, 0.9510565162951535312, 1.000000000000000000, 0.9510565162951535312, 1.000000000000000000, 0.9510565162951535312, 1.000000000000000000, 0.9510565162951535312, 1.000000000000000000, 0.9510565162951535312, 1.000000000000000000, 0.9510565162951535312, 1.000000000000000000, 0.9510565162951535312, 1.000000000000000000, 0.9510565162951535312, 1.000000000000000000, 0.9510565162951535312, 1.000000000000000000, 0.9510565162951535312, 1.000000000000000000, 0.9510565162951535312, 1.000000000000000000, 0.9510565162951535312, 1.000000000000000000, 0.9510565162951535312, 1.000000000000000000, 0.9510565162951535312, 1.000000000000000000, 0.9510565162951535312, 1.000000000000000000, 0.9510565162951535312, 1.000000000000000000, 0.9510565162951535312, 1.000000000000000000, 0.9510565162951535312, 1.000000000000000000, 0.9510565162951535312, 1.000000000000000000, 0.9510565162951535312, 1.000000000000000000, 0.9510565162951535312, 1.000000000000000000, 0.9510565162951535312, 1.000000000000000000, 0.9510565162951535312, 1.000000000000000000, 0.9510565162951535312, 1.000000000000000000, 0.9510565162951535312, 1.000000000000000000, 0.9510565162951535312, 1.000000000000000000, 0.9510565162951535312, 1.000000000000000000, 0.9510565162951535312, 1.000000000000000000, 0.9510565162951535312, 1.000000000000000000, 0.9510565162951535312, 1.000000000000000000, 0.9510565162951535312, 1.000000000000000000, 0.9510565162951535312, 1.000000000000000000, 0.9510565162951535312, 1.000000000000000000, 0.9510565162951535312, 1.000000000000000000, 0.9510565162951535312, 1.000000000000000000, 0.9510565162951535312, 1.000000000000000000, 0.9510565162951535312, 1.000000000000000000, 0.9510565162951535312, 1.000000000000000000, 0.9510565162951535312, 1.000000000000000000, 0.9510565162951535312, 1.000000000000000000, 0.9510565162951535312, 1.000000000000000000, 0.9510565162951535312, 1.000000000000000000, 0.9510565162951535312, 1.000000000000000000, 0.9510565162951535312, 1.000000000000000000, 0.9510565162951535312, 1.000000000000000000, 0.9510565162951535312, 1.000000000000000000, 0.9510565162951535312, 1.000000000000000000, 0.9510565162951535312, 1.000000000000000000, 0.9510565162951535312, 1.000000000000000000, 0.9510565162951535312, 1.000000000000000000, 0.9510565162951535312, 1.000000000000000000, 0.9510565162951535312, 1.000000000000000000, 0.9510565162951535312, 1.000000000000000000, 0.9510565162951535312, 1.000000000000000000, 0.9510565162951535312, 1.000000000000000000, 0.9510565162951535312, 1.000000000000000000, 0.9510565162951535312, 1.000000000000000000, 0.9510565162951535312, 1.000000000000000000, 0.9510565162951535312, 1.000000000000000000, 0.9510565162951535312, 1.000000000000000000, 0.9510565162951535312, 1.000000000000000000, 0.9510565162951535312, 1.000000000000000000, 0.9510565162951535312, 1.000000000000000000, 0.9510565162951535312, 1.000000000000000000, 0.9510565162951535312, 1.000000000000000000, 0.9510565162951535312, 1.000000000000000000, 0.9510565162951535312, 1.000000000000000000, 0.9510565162951535312, 1.000000000000000000, 0.9510565162951535312, 1.000000000000000000, 0.9510565162951535312, 1.000000000000000000, 0.9510565162951535312, 1.000000000000000000, 0.9510565162951535312, 1.000000000000000000, 0.9510565162951535312, 1.000000000000000000, 0.9510565162951535312, 1.000000000000000000, 0.9510565162951535312, 1.000000000000000000, 0.9510565162951535312, 1.000000000000000000, 0.9510565162951535312, 1.000000000000000000, 0.9510565162951535312, 1.000000000000000000, 0.9510565162951535312, 1.000000000000000000, 0.9510565162951535312, 1.000000000000000000, 0.9510565162951535312, 1.000000000000000000, 0.9510565162951535312, 1.000000000000000000, 0.9510565162951535312, 1.000000000000000000, 0.9510565162951535312, 1.000000000000000000, 0.9510565162951535312, 1.000000000000000000, 0.9510565162951535312, 1.000000000000000000, 0.9510565162951535312, 1.000000000000000000, 0.9510565162951535312, 1.000000000000000000, 0.9510565162951535312, 1.000000000000000000, 0.9510565162951535312, 1.000000000000000000, 0.9510565162951535312, 1.000000000000000000, 0.9510565162951535312, 1.000000000000000000, 0.9510565162951535312, 1.000000000000000000, 0.9510565162951535312, 1.000000000000000000, 0.9510565162951535312, 1.000000000000000000, 0.9510565162951535312, 1.000000000000000000, 0.9510565162951535312, 1.000000000000000000, 0.9510565162951535312, 1.000000000000000000, 0.9510565162951535312, 1.000000000000000000, 0.9510565162951535312, 1.000000000000000000, 0.9510565162951535312, 1.000000000000000000, 0.9510565162951535312, 1.000000000000000000, 0.9510565162951535312, 1.000000000000000000, 0.9510565162951535312, 1.000000000000000000, 0.9510565162951535312, 1.000000000000000000, 0.9510565162951535312, 1.000000000000000000, 0.9510565162951535312, 1.000000000000000000, 0.9510565162951535312, 1.000000000000000000, 0.9510565162951535312, 1.000000000000000000, 0.9510565162951535312, 1.000000000000000000, 0.9510565162951535312, 1.000000000000000000, 0.9510565162951535312, 1.000000000000000000, 0.9510565162951535312, 1.000000000000000000, 0.9510565162951535312, 1.000000000000000000, 0.9510565162951535312, 1.000000000000000000, 0.9510565162951535312, 1.000000000000000000, 0.9510565162951535312, 1.000000000000000000, 0.9510565162951535312, 1.000000000000000000, 0.9510565162951535312, 1.000000000000000000, 0.9510565162951535312, 1.000000000000000000, 0.9510565162951535312, 1.000000000000000000, 0.9510565162951535312, 1.000000000000000000, 0.9510565162951535312, 1.000000000000000000, 0.9510565162951535312, 1.000000000000000000, 0.9510565162951535312, 1.000000000000000000, 0.9510565162951535312, 1.000000000000000000, 0.9510565162951535312, 1.000000000000000000),
 ( 0.3333333333333333703, 0.3170188387650512141, 0.3333333333333333703, 0.3170188387650512141, 0.3333333333333333703, 0.3170188387650512141, 0.3333333333333333703, 0.3170188387650512141, 0.3333333333333333703, 0.3170188387650512141, 0.3333333333333333703, 0.3170188387650512141, 0.3333333333333333703, 0.3170188387650512141, 0.3333333333333333703, 0.3170188387650512141, 0.3333333333333333703, 0.3170188387650512141, 0.3333333333333333703, 0.3170188387650512141, 0.3333333333333333703, 0.3170188387650512141, 0.3333333333333333703, 0.3170188387650512141, 0.3333333333333333703, 0.3170188387650512141, 0.3333333333333333703, 0.3170188387650512141, 0.3333333333333333703, 0.3170188387650512141, 0.3333333333333333703, 0.3170188387650512141, 0.3333333333333333703, 0.3170188387650512141, 0.3333333333333333703, 0.3170188387650512141, 0.3333333333333333703, 0.3170188387650512141, 0.3333333333333333703, 0.3170188387650512141, 0.3333333333333333703, 0.3170188387650512141, 0.3333333333333333703, 0.3170188387650512141, 0.3333333333333333703, 0.3170188387650512141, 0.3333333333333333703, 0.3170188387650512141, 0.3333333333333333703, 0.3170188387650512141, 0.3333333333333333703, 0.3170188387650512141, 0.3333333333333333703, 0.3170188387650512141, 0.3333333333333333703, 0.3170188387650512141, 0.3333333333333333703, 0.3170188387650512141, 0.3333333333333333703, 0.3170188387650512141, 0.3333333333333333703, 0.3170188387650512141, 0.3333333333333333703, 0.3170188387650512141, 0.3333333333333333703, 0.3170188387650512141, 0.3333333333333333703, 0.3170188387650512141, 0.3333333333333333703, 0.3170188387650512141, 0.3333333333333333703, 0.3170188387650512141, 0.3333333333333333703, 0.3170188387650512141, 0.3333333333333333703, 0.3170188387650512141, 0.3333333333333333703, 0.3170188387650512141, 0.3333333333333333703, 0.3170188387650512141, 0.3333333333333333703, 0.3170188387650512141, 0.3333333333333333703, 0.3170188387650512141, 0.3333333333333333703, 0.3170188387650512141, 0.3333333333333333703, 0.3170188387650512141, 0.3333333333333333703, 0.3170188387650512141, 0.3333333333333333703, 0.3170188387650512141, 0.3333333333333333703, 0.3170188387650512141, 0.3333333333333333703, 0.3170188387650512141, 0.3333333333333333703, 0.3170188387650512141, 0.3333333333333333703, 0.3170188387650512141, 0.3333333333333333703, 0.3170188387650512141, 0.3333333333333333703, 0.3170188387650512141, 0.3333333333333333703, 0.3170188387650512141, 0.3333333333333333703, 0.3170188387650512141, 0.3333333333333333703, 0.3170188387650512141, 0.3333333333333333703, 0.3170188387650512141, 0.3333333333333333703, 0.3170188387650512141, 0.3333333333333333703, 0.3170188387650512141, 0.3333333333333333703, 0.3170188387650512141, 0.3333333333333333703, 0.3170188387650512141, 0.3333333333333333703, 0.3170188387650512141, 0.3333333333333333703, 0.3170188387650512141, 0.3333333333333333703, 0.3170188387650512141, 0.3333333333333333703, 0.3170188387650512141, 0.3333333333333333703, 0.3170188387650512141, 0.3333333333333333703, 0.3170188387650512141, 0.3333333333333333703, 0.3170188387650512141, 0.3333333333333333703, 0.3170188387650512141, 0.3333333333333333703, 0.3170188387650512141, 0.3333333333333333703, 0.3170188387650512141, 0.3333333333333333703, 0.3170188387650512141, 0.3333333333333333703, 0.3170188387650512141, 0.3333333333333333703, 0.3170188387650512141, 0.3333333333333333703, 0.3170188387650512141, 0.3333333333333333703, 0.3170188387650512141, 0.3333333333333333703, 0.3170188387650512141, 0.3333333333333333703, 0.3170188387650512141, 0.3333333333333333703, 0.3170188387650512141, 0.3333333333333333703, 0.3170188387650512141, 0.3333333333333333703, 0.3170188387650512141, 0.3333333333333333703, 0.3170188387650512141, 0.3333333333333333703, 0.3170188387650512141, 0.3333333333333333703, 0.3170188387650512141, 0.3333333333333333703, 0.3170188387650512141, 0.3333333333333333703, 0.3170188387650512141, 0.3333333333333333703, 0.3170188387650512141, 0.3333333333333333703, 0.3170188387650512141, 0.3333333333333333703, 0.3170188387650512141, 0.3333333333333333703, 0.3170188387650512141, 0.3333333333333333703, 0.3170188387650512141, 0.3333333333333333703, 0.3170188387650512141, 0.3333333333333333703, 0.3170188387650512141, 0.3333333333333333703, 0.3170188387650512141, 0.3333333333333333703, 0.3170188387650512141, 0.3333333333333333703, 0.3170188387650512141, 0.3333333333333333703, 0.3170188387650512141, 0.3333333333333333703, 0.3170188387650512141, 0.3333333333333333703, 0.3170188387650512141, 0.3333333333333333703, 0.3170188387650512141, 0.3333333333333333703, 0.3170188387650512141, 0.3333333333333333703, 0.3170188387650512141, 0.3333333333333333703, 0.3170188387650512141, 0.3333333333333333703, 0.3170188387650512141, 0.3333333333333333703, 0.3170188387650512141, 0.3333333333333333703, 0.3170188387650512141, 0.3333333333333333703, 0.3170188387650512141, 0.3333333333333333703, 0.3170188387650512141, 0.3333333333333333703, 0.3170188387650512141, 0.3333333333333333703, 0.3170188387650512141, 0.3333333333333333703, 0.3170188387650512141, 0.3333333333333333703, 0.3170188387650512141, 0.3333333333333333703, 0.3170188387650512141, 0.3333333333333333703, 0.3170188387650512141, 0.3333333333333333703, 0.3170188387650512141, 0.3333333333333333703, 0.3170188387650512141, 0.3333333333333333703, 0.3170188387650512141, 0.3333333333333333703, 0.3170188387650512141, 0.3333333333333333703, 0.3170188387650512141, 0.3333333333333333703, 0.3170188387650512141, 0.3333333333333333703, 0.3170188387650512141, 0.3333333333333333703, 0.3170188387650512141, 0.3333333333333333703, 0.3170188387650512141, 0.3333333333333333703, 0.3170188387650512141, 0.3333333333333333703, 0.3170188387650512141, 0.3333333333333333703, 0.3170188387650512141, 0.3333333333333333703, 0.3170188387650512141, 0.3333333333333333703, 0.3170188387650512141, 0.3333333333333333703, 0.3170188387650512141, 0.3333333333333333703, 0.3170188387650512141, 0.3333333333333333703, 0.3170188387650512141, 0.3333333333333333703, 0.3170188387650512141, 0.3333333333333333703, 0.3170188387650512141, 0.3333333333333333703, 0.3170188387650512141, 0.3333333333333333703, 0.3170188387650512141, 0.3333333333333333703, 0.3170188387650512141, 0.3333333333333333703, 0.3170188387650512141, 0.3333333333333333703, 0.3170188387650512141, 0.3333333333333333703, 0.3170188387650512141, 0.3333333333333333703, 0.3170188387650512141, 0.3333333333333333703, 0.3170188387650512141, 0.3333333333333333703, 0.3170188387650512141, 0.3333333333333333703, 0.3170188387650512141, 0.3333333333333333703, 0.3170188387650512141, 0.3333333333333333703, 0.3170188387650512141, 0.3333333333333333703, 0.3170188387650512141, 0.3333333333333333703, 0.3170188387650512141, 0.3333333333333333703, 0.3170188387650512141, 0.3333333333333333703, 0.3170188387650512141, 0.3333333333333333703, 0.3170188387650512141, 0.3333333333333333703, 0.3170188387650512141, 0.3333333333333333703, 0.3170188387650512141, 0.3333333333333333703, 0.3170188387650512141, 0.3333333333333333703, 0.3170188387650512141, 0.3333333333333333703, 0.3170188387650512141, 0.3333333333333333703, 0.3170188387650512141, 0.3333333333333333703),
 ( 0.3333333333333333703, 0.3170188387650512141, 0.3333333333333333703, 0.3170188387650512141, 0.3333333333333333703, 0.3170188387650512141, 0.3333333333333333703, 0.3170188387650512141, 0.3333333333333333703, 0.3170188387650512141, 0.3333333333333333703, 0.3170188387650512141, 0.3333333333333333703, 0.3170188387650512141, 0.3333333333333333703, 0.3170188387650512141, 0.3333333333333333703, 0.3170188387650512141, 0.3333333333333333703, 0.3170188387650512141, 0.3333333333333333703, 0.3170188387650512141, 0.3333333333333333703, 0.3170188387650512141, 0.3333333333333333703, 0.3170188387650512141, 0.3333333333333333703, 0.3170188387650512141, 0.3333333333333333703, 0.3170188387650512141, 0.3333333333333333703, 0.3170188387650512141, 0.3333333333333333703, 0.3170188387650512141, 0.3333333333333333703, 0.3170188387650512141, 0.3333333333333333703, 0.3170188387650512141, 0.3333333333333333703, 0.3170188387650512141, 0.3333333333333333703, 0.3170188387650512141, 0.3333333333333333703, 0.3170188387650512141, 0.3333333333333333703, 0.3170188387650512141, 0.3333333333333333703, 0.3170188387650512141, 0.3333333333333333703, 0.3170188387650512141, 0.3333333333333333703, 0.3170188387650512141, 0.3333333333333333703, 0.3170188387650512141, 0.3333333333333333703, 0.3170188387650512141, 0.3333333333333333703, 0.3170188387650512141, 0.3333333333333333703, 0.3170188387650512141, 0.3333333333333333703, 0.3170188387650512141, 0.3333333333333333703, 0.3170188387650512141, 0.3333333333333333703, 0.3170188387650512141, 0.3333333333333333703, 0.3170188387650512141, 0.3333333333333333703, 0.3170188387650512141, 0.3333333333333333703, 0.3170188387650512141, 0.3333333333333333703, 0.3170188387650512141, 0.3333333333333333703, 0.3170188387650512141, 0.3333333333333333703, 0.3170188387650512141, 0.3333333333333333703, 0.3170188387650512141, 0.3333333333333333703, 0.3170188387650512141, 0.3333333333333333703, 0.3170188387650512141, 0.3333333333333333703, 0.3170188387650512141, 0.3333333333333333703, 0.3170188387650512141, 0.3333333333333333703, 0.3170188387650512141, 0.3333333333333333703, 0.3170188387650512141, 0.3333333333333333703, 0.3170188387650512141, 0.3333333333333333703, 0.3170188387650512141, 0.3333333333333333703, 0.3170188387650512141, 0.3333333333333333703, 0.3170188387650512141, 0.3333333333333333703, 0.3170188387650512141, 0.3333333333333333703, 0.3170188387650512141, 0.3333333333333333703, 0.3170188387650512141, 0.3333333333333333703, 0.3170188387650512141, 0.3333333333333333703, 0.3170188387650512141, 0.3333333333333333703, 0.3170188387650512141, 0.3333333333333333703, 0.3170188387650512141, 0.3333333333333333703, 0.3170188387650512141, 0.3333333333333333703, 0.3170188387650512141, 0.3333333333333333703, 0.3170188387650512141, 0.3333333333333333703, 0.3170188387650512141, 0.3333333333333333703, 0.3170188387650512141, 0.3333333333333333703, 0.3170188387650512141, 0.3333333333333333703, 0.3170188387650512141, 0.3333333333333333703, 0.3170188387650512141, 0.3333333333333333703, 0.3170188387650512141, 0.3333333333333333703, 0.3170188387650512141, 0.3333333333333333703, 0.3170188387650512141, 0.3333333333333333703, 0.3170188387650512141, 0.3333333333333333703, 0.3170188387650512141, 0.3333333333333333703, 0.3170188387650512141, 0.3333333333333333703, 0.3170188387650512141, 0.3333333333333333703, 0.3170188387650512141, 0.3333333333333333703, 0.3170188387650512141, 0.3333333333333333703, 0.3170188387650512141, 0.3333333333333333703, 0.3170188387650512141, 0.3333333333333333703, 0.3170188387650512141, 0.3333333333333333703, 0.3170188387650512141, 0.3333333333333333703, 0.3170188387650512141, 0.3333333333333333703, 0.3170188387650512141, 0.3333333333333333703, 0.3170188387650512141, 0.3333333333333333703, 0.3170188387650512141, 0.3333333333333333703, 0.3170188387650512141, 0.3333333333333333703, 0.3170188387650512141, 0.3333333333333333703, 0.3170188387650512141, 0.3333333333333333703, 0.3170188387650512141, 0.3333333333333333703, 0.3170188387650512141, 0.3333333333333333703, 0.3170188387650512141, 0.3333333333333333703, 0.3170188387650512141, 0.3333333333333333703, 0.3170188387650512141, 0.3333333333333333703, 0.3170188387650512141, 0.3333333333333333703, 0.3170188387650512141, 0.3333333333333333703, 0.3170188387650512141, 0.3333333333333333703, 0.3170188387650512141, 0.3333333333333333703, 0.3170188387650512141, 0.3333333333333333703, 0.3170188387650512141, 0.3333333333333333703, 0.3170188387650512141, 0.3333333333333333703, 0.3170188387650512141, 0.3333333333333333703, 0.3170188387650512141, 0.3333333333333333703, 0.3170188387650512141, 0.3333333333333333703, 0.3170188387650512141, 0.3333333333333333703, 0.3170188387650512141, 0.3333333333333333703, 0.3170188387650512141, 0.3333333333333333703, 0.3170188387650512141, 0.3333333333333333703, 0.3170188387650512141, 0.3333333333333333703, 0.3170188387650512141, 0.3333333333333333703, 0.3170188387650512141, 0.3333333333333333703, 0.3170188387650512141, 0.3333333333333333703, 0.3170188387650512141, 0.3333333333333333703, 0.3170188387650512141, 0.3333333333333333703, 0.3170188387650512141, 0.3333333333333333703, 0.3170188387650512141, 0.3333333333333333703, 0.3170188387650512141, 0.3333333333333333703, 0.3170188387650512141, 0.3333333333333333703, 0.3170188387650512141, 0.3333333333333333703, 0.3170188387650512141, 0.3333333333333333703, 0.3170188387650512141, 0.3333333333333333703, 0.3170188387650512141, 0.3333333333333333703, 0.3170188387650512141, 0.3333333333333333703, 0.3170188387650512141, 0.3333333333333333703, 0.3170188387650512141, 0.3333333333333333703, 0.3170188387650512141, 0.3333333333333333703, 0.3170188387650512141, 0.3333333333333333703, 0.3170188387650512141, 0.3333333333333333703, 0.3170188387650512141, 0.3333333333333333703, 0.3170188387650512141, 0.3333333333333333703, 0.3170188387650512141, 0.3333333333333333703, 0.3170188387650512141, 0.3333333333333333703, 0.3170188387650512141, 0.3333333333333333703, 0.3170188387650512141, 0.3333333333333333703, 0.3170188387650512141, 0.3333333333333333703, 0.3170188387650512141, 0.3333333333333333703, 0.3170188387650512141, 0.3333333333333333703, 0.3170188387650512141, 0.3333333333333333703, 0.3170188387650512141, 0.3333333333333333703, 0.3170188387650512141, 0.3333333333333333703, 0.3170188387650512141, 0.3333333333333333703, 0.3170188387650512141, 0.3333333333333333703, 0.3170188387650512141, 0.3333333333333333703, 0.3170188387650512141, 0.3333333333333333703, 0.3170188387650512141, 0.3333333333333333703, 0.3170188387650512141, 0.3333333333333333703, 0.3170188387650512141, 0.3333333333333333703, 0.3170188387650512141, 0.3333333333333333703, 0.3170188387650512141, 0.3333333333333333703, 0.3170188387650512141, 0.3333333333333333703, 0.3170188387650512141, 0.3333333333333333703, 0.3170188387650512141, 0.3333333333333333703, 0.3170188387650512141, 0.3333333333333333703, 0.3170188387650512141, 0.3333333333333333703, 0.3170188387650512141, 0.3333333333333333703, 0.3170188387650512141, 0.3333333333333333703, 0.3170188387650512141, 0.3333333333333333703, 0.3170188387650512141, 0.3333333333333333703, 0.3170188387650512141, 0.3333333333333333703),
 ( 1.000000000000000000, 0.9510565162951535312, 1.000000000000000000, 0.9510565162951535312, 1.000000000000000000, 0.9510565162951535312, 1.000000000000000000, 0.9510565162951535312, 1.000000000000000000, 0.9510565162951535312, 1.000000000000000000, 0.9510565162951535312, 1.000000000000000000, 0.9510565162951535312, 1.000000000000000000, 0.9510565162951535312, 1.000000000000000000, 0.9510565162951535312, 1.000000000000000000, 0.9510565162951535312, 1.000000000000000000, 0.9510565162951535312, 1.000000000000000000, 0.9510565162951535312, 1.000000000000000000, 0.9510565162951535312, 1.000000000000000000, 0.9510565162951535312, 1.000000000000000000, 0.9510565162951535312, 1.000000000000000000, 0.9510565162951535312, 1.000000000000000000, 0.9510565162951535312, 1.000000000000000000, 0.9510565162951535312, 1.000000000000000000, 0.9510565162951535312, 1.000000000000000000, 0.9510565162951535312, 1.000000000000000000, 0.9510565162951535312, 1.000000000000000000, 0.9510565162951535312, 1.000000000000000000, 0.9510565162951535312, 1.000000000000000000, 0.9510565162951535312, 1.000000000000000000, 0.9510565162951535312, 1.000000000000000000, 0.9510565162951535312, 1.000000000000000000, 0.9510565162951535312, 1.000000000000000000, 0.9510565162951535312, 1.000000000000000000, 0.9510565162951535312, 1.000000000000000000, 0.9510565162951535312, 1.000000000000000000, 0.9510565162951535312, 1.000000000000000000, 0.9510565162951535312, 1.000000000000000000, 0.9510565162951535312, 1.000000000000000000, 0.9510565162951535312, 1.000000000000000000, 0.9510565162951535312, 1.000000000000000000, 0.9510565162951535312, 1.000000000000000000, 0.9510565162951535312, 1.000000000000000000, 0.9510565162951535312, 1.000000000000000000, 0.9510565162951535312, 1.000000000000000000, 0.9510565162951535312, 1.000000000000000000, 0.9510565162951535312, 1.000000000000000000, 0.9510565162951535312, 1.000000000000000000, 0.9510565162951535312, 1.000000000000000000, 0.9510565162951535312, 1.000000000000000000, 0.9510565162951535312, 1.000000000000000000, 0.9510565162951535312, 1.000000000000000000, 0.9510565162951535312, 1.000000000000000000, 0.9510565162951535312, 1.000000000000000000, 0.9510565162951535312, 1.000000000000000000, 0.9510565162951535312, 1.000000000000000000, 0.9510565162951535312, 1.000000000000000000, 0.9510565162951535312, 1.000000000000000000, 0.9510565162951535312, 1.000000000000000000, 0.9510565162951535312, 1.000000000000000000, 0.9510565162951535312, 1.000000000000000000, 0.9510565162951535312, 1.000000000000000000, 0.9510565162951535312, 1.000000000000000000, 0.9510565162951535312, 1.000000000000000000, 0.9510565162951535312, 1.000000000000000000, 0.9510565162951535312, 1.000000000000000000, 0.9510565162951535312, 1.000000000000000000, 0.9510565162951535312, 1.000000000000000000, 0.9510565162951535312, 1.000000000000000000, 0.9510565162951535312, 1.000000000000000000, 0.9510565162951535312, 1.000000000000000000, 0.9510565162951535312, 1.000000000000000000, 0.9510565162951535312, 1.000000000000000000, 0.9510565162951535312, 1.000000000000000000, 0.9510565162951535312, 1.000000000000000000, 0.9510565162951535312, 1.000000000000000000, 0.9510565162951535312, 1.000000000000000000, 0.9510565162951535312, 1.000000000000000000, 0.9510565162951535312, 1.000000000000000000, 0.9510565162951535312, 1.000000000000000000, 0.9510565162951535312, 1.000000000000000000, 0.9510565162951535312, 1.000000000000000000, 0.9510565162951535312, 1.000000000000000000, 0.9510565162951535312, 1.000000000000000000, 0.9510565162951535312, 1.000000000000000000, 0.9510565162951535312, 1.000000000000000000, 0.9510565162951535312, 1.000000000000000000, 0.9510565162951535312, 1.000000000000000000, 0.9510565162951535312, 1.000000000000000000, 0.9510565162951535312, 1.000000000000000000, 0.9510565162951535312, 1.000000000000000000, 0.9510565162951535312, 1.000000000000000000, 0.9510565162951535312, 1.000000000000000000, 0.9510565162951535312, 1.000000000000000000, 0.9510565162951535312, 1.000000000000000000, 0.9510565162951535312, 1.000000000000000000, 0.9510565162951535312, 1.000000000000000000, 0.9510565162951535312, 1.000000000000000000, 0.9510565162951535312, 1.000000000000000000, 0.9510565162951535312, 1.000000000000000000, 0.9510565162951535312, 1.000000000000000000, 0.9510565162951535312, 1.000000000000000000, 0.9510565162951535312, 1.000000000000000000, 0.9510565162951535312, 1.000000000000000000, 0.9510565162951535312, 1.000000000000000000, 0.9510565162951535312, 1.000000000000000000, 0.9510565162951535312, 1.000000000000000000, 0.9510565162951535312, 1.000000000000000000, 0.9510565162951535312, 1.000000000000000000, 0.9510565162951535312, 1.000000000000000000, 0.9510565162951535312, 1.000000000000000000, 0.9510565162951535312, 1.000000000000000000, 0.9510565162951535312, 1.000000000000000000, 0.9510565162951535312, 1.000000000000000000, 0.9510565162951535312, 1.000000000000000000, 0.9510565162951535312, 1.000000000000000000, 0.9510565162951535312, 1.000000000000000000, 0.9510565162951535312, 1.000000000000000000, 0.9510565162951535312, 1.000000000000000000, 0.9510565162951535312, 1.000000000000000000, 0.9510565162951535312, 1.000000000000000000, 0.9510565162951535312, 1.000000000000000000, 0.9510565162951535312, 1.000000000000000000, 0.9510565162951535312, 1.000000000000000000, 0.9510565162951535312, 1.000000000000000000, 0.9510565162951535312, 1.000000000000000000, 0.9510565162951535312, 1.000000000000000000, 0.9510565162951535312, 1.000000000000000000, 0.9510565162951535312, 1.000000000000000000, 0.9510565162951535312, 1.000000000000000000, 0.9510565162951535312, 1.000000000000000000, 0.9510565162951535312, 1.000000000000000000, 0.9510565162951535312, 1.000000000000000000, 0.9510565162951535312, 1.000000000000000000, 0.9510565162951535312, 1.000000000000000000, 0.9510565162951535312, 1.000000000000000000, 0.9510565162951535312, 1.000000000000000000, 0.9510565162951535312, 1.000000000000000000, 0.9510565162951535312, 1.000000000000000000, 0.9510565162951535312, 1.000000000000000000, 0.9510565162951535312, 1.000000000000000000, 0.9510565162951535312, 1.000000000000000000, 0.9510565162951535312, 1.000000000000000000, 0.9510565162951535312, 1.000000000000000000, 0.9510565162951535312, 1.000000000000000000, 0.9510565162951535312, 1.000000000000000000, 0.9510565162951535312, 1.000000000000000000, 0.9510565162951535312, 1.000000000000000000, 0.9510565162951535312, 1.000000000000000000, 0.9510565162951535312, 1.000000000000000000, 0.9510565162951535312, 1.000000000000000000, 0.9510565162951535312, 1.000000000000000000, 0.9510565162951535312, 1.000000000000000000, 0.9510565162951535312, 1.000000000000000000, 0.9510565162951535312, 1.000000000000000000, 0.9510565162951535312, 1.000000000000000000, 0.9510565162951535312, 1.000000000000000000, 0.9510565162951535312, 1.000000000000000000, 0.9510565162951535312, 1.000000000000000000, 0.9510565162951535312, 1.000000000000000000, 0.9510565162951535312, 1.000000000000000000),
 ( 0.3333333333333333703, 0.3170188387650512141, 0.3333333333333333703, 0.3170188387650512141, 0.3333333333333333703, 0.3170188387650512141, 0.3333333333333333703, 0.3170188387650512141, 0.3333333333333333703, 0.3170188387650512141, 0.3333333333333333703, 0.3170188387650512141, 0.3333333333333333703, 0.3170188387650512141, 0.3333333333333333703, 0.3170188387650512141, 0.3333333333333333703, 0.3170188387650512141, 0.3333333333333333703, 0.3170188387650512141, 0.3333333333333333703, 0.3170188387650512141, 0.3333333333333333703, 0.3170188387650512141, 0.3333333333333333703, 0.3170188387650512141, 0.3333333333333333703, 0.3170188387650512141, 0.3333333333333333703, 0.3170188387650512141, 0.3333333333333333703, 0.3170188387650512141, 0.3333333333333333703, 0.3170188387650512141, 0.3333333333333333703, 0.3170188387650512141, 0.3333333333333333703, 0.3170188387650512141, 0.3333333333333333703, 0.3170188387650512141, 0.3333333333333333703, 0.3170188387650512141, 0.3333333333333333703, 0.3170188387650512141, 0.3333333333333333703, 0.3170188387650512141, 0.3333333333333333703, 0.3170188387650512141, 0.3333333333333333703, 0.3170188387650512141, 0.3333333333333333703, 0.3170188387650512141, 0.3333333333333333703, 0.3170188387650512141, 0.3333333333333333703, 0.3170188387650512141, 0.3333333333333333703, 0.3170188387650512141, 0.3333333333333333703, 0.3170188387650512141, 0.3333333333333333703, 0.3170188387650512141, 0.3333333333333333703, 0.3170188387650512141, 0.3333333333333333703, 0.3170188387650512141, 0.3333333333333333703, 0.3170188387650512141, 0.3333333333333333703, 0.3170188387650512141, 0.3333333333333333703, 0.3170188387650512141, 0.3333333333333333703, 0.3170188387650512141, 0.3333333333333333703, 0.3170188387650512141, 0.3333333333333333703, 0.3170188387650512141, 0.3333333333333333703, 0.3170188387650512141, 0.3333333333333333703, 0.3170188387650512141, 0.3333333333333333703, 0.3170188387650512141, 0.3333333333333333703, 0.3170188387650512141, 0.3333333333333333703, 0.3170188387650512141, 0.3333333333333333703, 0.3170188387650512141, 0.3333333333333333703, 0.3170188387650512141, 0.3333333333333333703, 0.3170188387650512141, 0.3333333333333333703, 0.3170188387650512141, 0.3333333333333333703, 0.3170188387650512141, 0.3333333333333333703, 0.3170188387650512141, 0.3333333333333333703, 0.3170188387650512141, 0.3333333333333333703, 0.3170188387650512141, 0.3333333333333333703, 0.3170188387650512141, 0.3333333333333333703, 0.3170188387650512141, 0.3333333333333333703, 0.3170188387650512141, 0.3333333333333333703, 0.3170188387650512141, 0.3333333333333333703, 0.3170188387650512141, 0.3333333333333333703, 0.3170188387650512141, 0.3333333333333333703, 0.3170188387650512141, 0.3333333333333333703, 0.3170188387650512141, 0.3333333333333333703, 0.3170188387650512141, 0.3333333333333333703, 0.3170188387650512141, 0.3333333333333333703, 0.3170188387650512141, 0.3333333333333333703, 0.3170188387650512141, 0.3333333333333333703, 0.3170188387650512141, 0.3333333333333333703, 0.3170188387650512141, 0.3333333333333333703, 0.3170188387650512141, 0.3333333333333333703, 0.3170188387650512141, 0.3333333333333333703, 0.3170188387650512141, 0.3333333333333333703, 0.3170188387650512141, 0.3333333333333333703, 0.3170188387650512141, 0.3333333333333333703, 0.3170188387650512141, 0.3333333333333333703, 0.3170188387650512141, 0.3333333333333333703, 0.3170188387650512141, 0.3333333333333333703, 0.3170188387650512141, 0.3333333333333333703, 0.3170188387650512141, 0.3333333333333333703, 0.3170188387650512141, 0.3333333333333333703, 0.3170188387650512141, 0.3333333333333333703, 0.3170188387650512141, 0.3333333333333333703, 0.3170188387650512141, 0.3333333333333333703, 0.3170188387650512141, 0.3333333333333333703, 0.3170188387650512141, 0.3333333333333333703, 0.3170188387650512141, 0.3333333333333333703, 0.3170188387650512141, 0.3333333333333333703, 0.3170188387650512141, 0.3333333333333333703, 0.3170188387650512141, 0.3333333333333333703, 0.3170188387650512141, 0.3333333333333333703, 0.3170188387650512141, 0.3333333333333333703, 0.3170188387650512141, 0.3333333333333333703, 0.3170188387650512141, 0.3333333333333333703, 0.3170188387650512141, 0.3333333333333333703, 0.3170188387650512141, 0.3333333333333333703, 0.3170188387650512141, 0.3333333333333333703, 0.3170188387650512141, 0.3333333333333333703, 0.3170188387650512141, 0.3333333333333333703, 0.3170188387650512141, 0.3333333333333333703, 0.3170188387650512141, 0.3333333333333333703, 0.3170188387650512141, 0.3333333333333333703, 0.3170188387650512141, 0.3333333333333333703, 0.3170188387650512141, 0.3333333333333333703, 0.3170188387650512141, 0.3333333333333333703, 0.3170188387650512141, 0.3333333333333333703, 0.3170188387650512141, 0.3333333333333333703, 0.3170188387650512141, 0.3333333333333333703, 0.3170188387650512141, 0.3333333333333333703, 0.3170188387650512141, 0.3333333333333333703, 0.3170188387650512141, 0.3333333333333333703, 0.3170188387650512141, 0.3333333333333333703, 0.3170188387650512141, 0.3333333333333333703, 0.3170188387650512141, 0.3333333333333333703, 0.3170188387650512141, 0.3333333333333333703, 0.3170188387650512141, 0.3333333333333333703, 0.3170188387650512141, 0.3333333333333333703, 0.3170188387650512141, 0.3333333333333333703, 0.3170188387650512141, 0.3333333333333333703, 0.3170188387650512141, 0.3333333333333333703, 0.3170188387650512141, 0.3333333333333333703, 0.3170188387650512141, 0.3333333333333333703, 0.3170188387650512141, 0.3333333333333333703, 0.3170188387650512141, 0.3333333333333333703, 0.3170188387650512141, 0.3333333333333333703, 0.3170188387650512141, 0.3333333333333333703, 0.3170188387650512141, 0.3333333333333333703, 0.3170188387650512141, 0.3333333333333333703, 0.3170188387650512141, 0.3333333333333333703, 0.3170188387650512141, 0.3333333333333333703, 0.3170188387650512141, 0.3333333333333333703, 0.3170188387650512141, 0.3333333333333333703, 0.3170188387650512141, 0.3333333333333333703, 0.3170188387650512141, 0.3333333333333333703, 0.3170188387650512141, 0.3333333333333333703, 0.3170188387650512141, 0.3333333333333333703, 0.3170188387650512141, 0.3333333333333333703, 0.3170188387650512141, 0.3333333333333333703, 0.3170188387650512141, 0.3333333333333333703, 0.3170188387650512141, 0.3333333333333333703, 0.3170188387650512141, 0.3333333333333333703, 0.3170188387650512141, 0.3333333333333333703, 0.3170188387650512141, 0.3333333333333333703, 0.3170188387650512141, 0.3333333333333333703, 0.3170188387650512141, 0.3333333333333333703, 0.3170188387650512141, 0.3333333333333333703, 0.3170188387650512141, 0.3333333333333333703, 0.3170188387650512141, 0.3333333333333333703, 0.3170188387650512141, 0.3333333333333333703, 0.3170188387650512141, 0.3333333333333333703, 0.3170188387650512141, 0.3333333333333333703, 0.3170188387650512141, 0.3333333333333333703, 0.3170188387650512141, 0.3333333333333333703, 0.3170188387650512141, 0.3333333333333333703, 0.3170188387650512141, 0.3333333333333333703, 0.3170188387650512141, 0.3333333333333333703, 0.3170188387650512141, 0.3333333333333333703, 0.3170188387650512141, 0.3333333333333333703, 0.3170188387650512141, 0.3333333333333333703),
 ( 0.3333333333333333703, 0.3170188387650512141, 0.3333333333333333703, 0.3170188387650512141, 0.3333333333333333703, 0.3170188387650512141, 0.3333333333333333703, 0.3170188387650512141, 0.3333333333333333703, 0.3170188387650512141, 0.3333333333333333703, 0.3170188387650512141, 0.3333333333333333703, 0.3170188387650512141, 0.3333333333333333703, 0.3170188387650512141, 0.3333333333333333703, 0.3170188387650512141, 0.3333333333333333703, 0.3170188387650512141, 0.3333333333333333703, 0.3170188387650512141, 0.3333333333333333703, 0.3170188387650512141, 0.3333333333333333703, 0.3170188387650512141, 0.3333333333333333703, 0.3170188387650512141, 0.3333333333333333703, 0.3170188387650512141, 0.3333333333333333703, 0.3170188387650512141, 0.3333333333333333703, 0.3170188387650512141, 0.3333333333333333703, 0.3170188387650512141, 0.3333333333333333703, 0.3170188387650512141, 0.3333333333333333703, 0.3170188387650512141, 0.3333333333333333703, 0.3170188387650512141, 0.3333333333333333703, 0.3170188387650512141, 0.3333333333333333703, 0.3170188387650512141, 0.3333333333333333703, 0.3170188387650512141, 0.3333333333333333703, 0.3170188387650512141, 0.3333333333333333703, 0.3170188387650512141, 0.3333333333333333703, 0.3170188387650512141, 0.3333333333333333703, 0.3170188387650512141, 0.3333333333333333703, 0.3170188387650512141, 0.3333333333333333703, 0.3170188387650512141, 0.3333333333333333703, 0.3170188387650512141, 0.3333333333333333703, 0.3170188387650512141, 0.3333333333333333703, 0.3170188387650512141, 0.3333333333333333703, 0.3170188387650512141, 0.3333333333333333703, 0.3170188387650512141, 0.3333333333333333703, 0.3170188387650512141, 0.3333333333333333703, 0.3170188387650512141, 0.3333333333333333703, 0.3170188387650512141, 0.3333333333333333703, 0.3170188387650512141, 0.3333333333333333703, 0.3170188387650512141, 0.3333333333333333703, 0.3170188387650512141, 0.3333333333333333703, 0.3170188387650512141, 0.3333333333333333703, 0.3170188387650512141, 0.3333333333333333703, 0.3170188387650512141, 0.3333333333333333703, 0.3170188387650512141, 0.3333333333333333703, 0.3170188387650512141, 0.3333333333333333703, 0.3170188387650512141, 0.3333333333333333703, 0.3170188387650512141, 0.3333333333333333703, 0.3170188387650512141, 0.3333333333333333703, 0.3170188387650512141, 0.3333333333333333703, 0.3170188387650512141, 0.3333333333333333703, 0.3170188387650512141, 0.3333333333333333703, 0.3170188387650512141, 0.3333333333333333703, 0.3170188387650512141, 0.3333333333333333703, 0.3170188387650512141, 0.3333333333333333703, 0.3170188387650512141, 0.3333333333333333703, 0.3170188387650512141, 0.3333333333333333703, 0.3170188387650512141, 0.3333333333333333703, 0.3170188387650512141, 0.3333333333333333703, 0.3170188387650512141, 0.3333333333333333703, 0.3170188387650512141, 0.3333333333333333703, 0.3170188387650512141, 0.3333333333333333703, 0.3170188387650512141, 0.3333333333333333703, 0.3170188387650512141, 0.3333333333333333703, 0.3170188387650512141, 0.3333333333333333703, 0.3170188387650512141, 0.3333333333333333703, 0.3170188387650512141, 0.3333333333333333703, 0.3170188387650512141, 0.3333333333333333703, 0.3170188387650512141, 0.3333333333333333703, 0.3170188387650512141, 0.3333333333333333703, 0.3170188387650512141, 0.3333333333333333703, 0.3170188387650512141, 0.3333333333333333703, 0.3170188387650512141, 0.3333333333333333703, 0.3170188387650512141, 0.3333333333333333703, 0.3170188387650512141, 0.3333333333333333703, 0.3170188387650512141, 0.3333333333333333703, 0.3170188387650512141, 0.3333333333333333703, 0.3170188387650512141, 0.3333333333333333703, 0.3170188387650512141, 0.3333333333333333703, 0.3170188387650512141, 0.3333333333333333703, 0.3170188387650512141, 0.3333333333333333703, 0.3170188387650512141, 0.3333333333333333703, 0.3170188387650512141, 0.3333333333333333703, 0.3170188387650512141, 0.3333333333333333703, 0.3170188387650512141, 0.3333333333333333703, 0.3170188387650512141, 0.3333333333333333703, 0.3170188387650512141, 0.3333333333333333703, 0.3170188387650512141, 0.3333333333333333703, 0.3170188387650512141, 0.3333333333333333703, 0.3170188387650512141, 0.3333333333333333703, 0.3170188387650512141, 0.3333333333333333703, 0.3170188387650512141, 0.3333333333333333703, 0.3170188387650512141, 0.3333333333333333703, 0.3170188387650512141, 0.3333333333333333703, 0.3170188387650512141, 0.3333333333333333703, 0.3170188387650512141, 0.3333333333333333703, 0.3170188387650512141, 0.3333333333333333703, 0.3170188387650512141, 0.3333333333333333703, 0.3170188387650512141, 0.3333333333333333703, 0.3170188387650512141, 0.3333333333333333703, 0.3170188387650512141, 0.3333333333333333703, 0.3170188387650512141, 0.3333333333333333703, 0.3170188387650512141, 0.3333333333333333703, 0.3170188387650512141, 0.3333333333333333703, 0.3170188387650512141, 0.3333333333333333703, 0.3170188387650512141, 0.3333333333333333703, 0.3170188387650512141, 0.3333333333333333703, 0.3170188387650512141, 0.3333333333333333703, 0.3170188387650512141, 0.3333333333333333703, 0.3170188387650512141, 0.3333333333333333703, 0.3170188387650512141, 0.3333333333333333703, 0.3170188387650512141, 0.3333333333333333703, 0.3170188387650512141, 0.3333333333333333703, 0.3170188387650512141, 0.3333333333333333703, 0.3170188387650512141, 0.3333333333333333703, 0.3170188387650512141, 0.3333333333333333703, 0.3170188387650512141, 0.3333333333333333703, 0.3170188387650512141, 0.3333333333333333703, 0.3170188387650512141, 0.3333333333333333703, 0.3170188387650512141, 0.3333333333333333703, 0.3170188387650512141, 0.3333333333333333703, 0.3170188387650512141, 0.3333333333333333703, 0.3170188387650512141, 0.3333333333333333703, 0.3170188387650512141, 0.3333333333333333703, 0.3170188387650512141, 0.3333333333333333703, 0.3170188387650512141, 0.3333333333333333703, 0.3170188387650512141, 0.3333333333333333703, 0.3170188387650512141, 0.3333333333333333703, 0.3170188387650512141, 0.3333333333333333703, 0.3170188387650512141, 0.3333333333333333703, 0.3170188387650512141, 0.3333333333333333703, 0.3170188387650512141, 0.3333333333333333703, 0.3170188387650512141, 0.3333333333333333703, 0.3170188387650512141, 0.3333333333333333703, 0.3170188387650512141, 0.3333333333333333703, 0.3170188387650512141, 0.3333333333333333703, 0.3170188387650512141, 0.3333333333333333703, 0.3170188387650512141, 0.3333333333333333703, 0.3170188387650512141, 0.3333333333333333703, 0.3170188387650512141, 0.3333333333333333703, 0.3170188387650512141, 0.3333333333333333703, 0.3170188387650512141, 0.3333333333333333703, 0.3170188387650512141, 0.3333333333333333703, 0.3170188387650512141, 0.3333333333333333703, 0.3170188387650512141, 0.3333333333333333703, 0.3170188387650512141, 0.3333333333333333703, 0.3170188387650512141, 0.3333333333333333703, 0.3170188387650512141, 0.3333333333333333703, 0.3170188387650512141, 0.3333333333333333703, 0.3170188387650512141, 0.3333333333333333703, 0.3170188387650512141, 0.3333333333333333703, 0.3170188387650512141, 0.3333333333333333703, 0.3170188387650512141, 0.3333333333333333703, 0.3170188387650512141, 0.3333333333333333703, 0.3170188387650512141, 0.3333333333333333703),
 ( 1.000000000000000000, 0.9510565162951535312, 1.000000000000000000, 0.9510565162951535312, 1.000000000000000000, 0.9510565162951535312, 1.000000000000000000, 0.9510565162951535312, 1.000000000000000000, 0.9510565162951535312, 1.000000000000000000, 0.9510565162951535312, 1.000000000000000000, 0.9510565162951535312, 1.000000000000000000, 0.9510565162951535312, 1.000000000000000000, 0.9510565162951535312, 1.000000000000000000, 0.9510565162951535312, 1.000000000000000000, 0.9510565162951535312, 1.000000000000000000, 0.9510565162951535312, 1.000000000000000000, 0.9510565162951535312, 1.000000000000000000, 0.9510565162951535312, 1.000000000000000000, 0.9510565162951535312, 1.000000000000000000, 0.9510565162951535312, 1.000000000000000000, 0.9510565162951535312, 1.000000000000000000, 0.9510565162951535312, 1.000000000000000000, 0.9510565162951535312, 1.000000000000000000, 0.9510565162951535312, 1.000000000000000000, 0.9510565162951535312, 1.000000000000000000, 0.9510565162951535312, 1.000000000000000000, 0.9510565162951535312, 1.000000000000000000, 0.9510565162951535312, 1.000000000000000000, 0.9510565162951535312, 1.000000000000000000, 0.9510565162951535312, 1.000000000000000000, 0.9510565162951535312, 1.000000000000000000, 0.9510565162951535312, 1.000000000000000000, 0.9510565162951535312, 1.000000000000000000, 0.9510565162951535312, 1.000000000000000000, 0.9510565162951535312, 1.000000000000000000, 0.9510565162951535312, 1.000000000000000000, 0.9510565162951535312, 1.000000000000000000, 0.9510565162951535312, 1.000000000000000000, 0.9510565162951535312, 1.000000000000000000, 0.9510565162951535312, 1.000000000000000000, 0.9510565162951535312, 1.000000000000000000, 0.9510565162951535312, 1.000000000000000000, 0.9510565162951535312, 1.000000000000000000, 0.9510565162951535312, 1.000000000000000000, 0.9510565162951535312, 1.000000000000000000, 0.9510565162951535312, 1.000000000000000000, 0.9510565162951535312, 1.000000000000000000, 0.9510565162951535312, 1.000000000000000000, 0.9510565162951535312, 1.000000000000000000, 0.9510565162951535312, 1.000000000000000000, 0.9510565162951535312, 1.000000000000000000, 0.9510565162951535312, 1.000000000000000000, 0.9510565162951535312, 1.000000000000000000, 0.9510565162951535312, 1.000000000000000000, 0.9510565162951535312, 1.000000000000000000, 0.9510565162951535312, 1.000000000000000000, 0.9510565162951535312, 1.000000000000000000, 0.9510565162951535312, 1.000000000000000000, 0.9510565162951535312, 1.000000000000000000, 0.9510565162951535312, 1.000000000000000000, 0.9510565162951535312, 1.000000000000000000, 0.9510565162951535312, 1.000000000000000000, 0.9510565162951535312, 1.000000000000000000, 0.9510565162951535312, 1.000000000000000000, 0.9510565162951535312, 1.000000000000000000, 0.9510565162951535312, 1.000000000000000000, 0.9510565162951535312, 1.000000000000000000, 0.9510565162951535312, 1.000000000000000000, 0.9510565162951535312, 1.000000000000000000, 0.9510565162951535312, 1.000000000000000000, 0.9510565162951535312, 1.000000000000000000, 0.9510565162951535312, 1.000000000000000000, 0.9510565162951535312, 1.000000000000000000, 0.9510565162951535312, 1.000000000000000000, 0.9510565162951535312, 1.000000000000000000, 0.9510565162951535312, 1.000000000000000000, 0.9510565162951535312, 1.000000000000000000, 0.9510565162951535312, 1.000000000000000000, 0.9510565162951535312, 1.000000000000000000, 0.9510565162951535312, 1.000000000000000000, 0.9510565162951535312, 1.000000000000000000, 0.9510565162951535312, 1.000000000000000000, 0.9510565162951535312, 1.000000000000000000, 0.9510565162951535312, 1.000000000000000000, 0.9510565162951535312, 1.000000000000000000, 0.9510565162951535312, 1.000000000000000000, 0.9510565162951535312, 1.000000000000000000, 0.9510565162951535312, 1.000000000000000000, 0.9510565162951535312, 1.000000000000000000, 0.9510565162951535312, 1.000000000000000000, 0.9510565162951535312, 1.000000000000000000, 0.9510565162951535312, 1.000000000000000000, 0.9510565162951535312, 1.000000000000000000, 0.9510565162951535312, 1.000000000000000000, 0.9510565162951535312, 1.000000000000000000, 0.9510565162951535312, 1.000000000000000000, 0.9510565162951535312, 1.000000000000000000, 0.9510565162951535312, 1.000000000000000000, 0.9510565162951535312, 1.000000000000000000, 0.9510565162951535312, 1.000000000000000000, 0.9510565162951535312, 1.000000000000000000, 0.9510565162951535312, 1.000000000000000000, 0.9510565162951535312, 1.000000000000000000, 0.9510565162951535312, 1.000000000000000000, 0.9510565162951535312, 1.000000000000000000, 0.9510565162951535312, 1.000000000000000000, 0.9510565162951535312, 1.000000000000000000, 0.9510565162951535312, 1.000000000000000000, 0.9510565162951535312, 1.000000000000000000, 0.9510565162951535312, 1.000000000000000000, 0.9510565162951535312, 1.000000000000000000, 0.9510565162951535312, 1.000000000000000000, 0.9510565162951535312, 1.000000000000000000, 0.9510565162951535312, 1.000000000000000000, 0.9510565162951535312, 1.000000000000000000, 0.9510565162951535312, 1.000000000000000000, 0.9510565162951535312, 1.000000000000000000, 0.9510565162951535312, 1.000000000000000000, 0.9510565162951535312, 1.000000000000000000, 0.9510565162951535312, 1.000000000000000000, 0.9510565162951535312, 1.000000000000000000, 0.9510565162951535312, 1.000000000000000000, 0.9510565162951535312, 1.000000000000000000, 0.9510565162951535312, 1.000000000000000000, 0.9510565162951535312, 1.000000000000000000, 0.9510565162951535312, 1.000000000000000000, 0.9510565162951535312, 1.000000000000000000, 0.9510565162951535312, 1.000000000000000000, 0.9510565162951535312, 1.000000000000000000, 0.9510565162951535312, 1.000000000000000000, 0.9510565162951535312, 1.000000000000000000, 0.9510565162951535312, 1.000000000000000000, 0.9510565162951535312, 1.000000000000000000, 0.9510565162951535312, 1.000000000000000000, 0.9510565162951535312, 1.000000000000000000, 0.9510565162951535312, 1.000000000000000000, 0.9510565162951535312, 1.000000000000000000, 0.9510565162951535312, 1.000000000000000000, 0.9510565162951535312, 1.000000000000000000, 0.9510565162951535312, 1.000000000000000000, 0.9510565162951535312, 1.000000000000000000, 0.9510565162951535312, 1.000000000000000000, 0.9510565162951535312, 1.000000000000000000, 0.9510565162951535312, 1.000000000000000000, 0.9510565162951535312, 1.000000000000000000, 0.9510565162951535312, 1.000000000000000000, 0.9510565162951535312, 1.000000000000000000, 0.9510565162951535312, 1.000000000000000000, 0.9510565162951535312, 1.000000000000000000, 0.9510565162951535312, 1.000000000000000000, 0.9510565162951535312, 1.000000000000000000, 0.9510565162951535312, 1.000000000000000000, 0.9510565162951535312, 1.000000000000000000, 0.9510565162951535312, 1.000000000000000000, 0.9510565162951535312, 1.000000000000000000, 0.9510565162951535312, 1.000000000000000000, 0.9510565162951535312, 1.000000000000000000, 0.9510565162951535312, 1.000000000000000000, 0.9510565162951535312, 1.000000000000000000) ) ) 
 REPRESENTATION_ITEM ( '' )  SURFACE ( )  );
#10462=CARTESIAN_POINT ( 'NONE',  ( 37.31647492878124694, -24.30384086642191122, 72.03616607671141026 ) ) ;
#10463=CARTESIAN_POINT ( 'NONE',  ( 38.82593461698262871, -10.91368208888609992, 69.62690120949091011 ) ) ;
#10469=CARTESIAN_POINT ( 'NONE',  ( 39.95015449827720744, -13.00384086642191228, 71.96809898377887293 ) ) ;
#10472=CARTESIAN_POINT ( 'NONE',  ( 40.14115730948191185, -8.513682088886104893, 71.32335560751961623 ) ) ;
#10474=CARTESIAN_POINT ( 'NONE',  ( 39.73277004305198545, -16.21368208888610596, 73.23812341099225875 ) ) ;
#10478=CARTESIAN_POINT ( 'NONE',  ( 39.51027997493896748, -21.10384086642191193, 71.43714994484032843 ) ) ;
#10484=CARTESIAN_POINT ( 'NONE',  ( 39.12911128074872380, -21.50384086642191406, 69.06206559358665231 ) ) ;
#10486=CARTESIAN_POINT ( 'NONE',  ( 37.80618814713140097, -25.91368208888610880, 73.13360434286902034 ) ) ;
#10493=CARTESIAN_POINT ( 'NONE',  ( 36.68196826583682935, -16.00384086642191050, 70.79240656858107172 ) ) ;
#10499=CARTESIAN_POINT ( 'NONE',  ( 37.69225076346193504, -1.803840866421911215, 70.42958956619168021 ) ) ;
#10502=CARTESIAN_POINT ( 'NONE',  ( 36.68196826583682935, -25.61368208888610454, 71.96809898377887293 ) ) ;
#10507=CARTESIAN_POINT ( 'NONE',  ( 37.21915885897815457, -3.413682088886101251, 71.08074471024443142 ) ) ;
#10508=CARTESIAN_POINT ( 'NONE',  ( 39.51027997493896748, -2.513682088886099564, 71.32335560751961623 ) ) ;
#10514=CARTESIAN_POINT ( 'NONE',  ( 37.80618814713138676, -13.70384086642190979, 69.62690120949091011 ) ) ;
#10527=CARTESIAN_POINT ( 'NONE',  ( 39.75915168707250302, -10.71368208888610063, 70.26145752964255564 ) ) ;
#10528=CARTESIAN_POINT ( 'NONE',  ( 39.95532413685785400, -29.10876147765399580, 71.32982406108487794 ) ) ;
#10532=EDGE_CURVE ( 'NONE', #8151, #12953, #24819, .T. ) ;
#10540=CARTESIAN_POINT ( 'NONE',  ( 36.36258059203030513, 0.09615913357808798800, 69.89063713639259845 ) ) ;
#10541=CARTESIAN_POINT ( 'NONE',  ( 37.38336156205274818, -25.71368208888610241, 72.12822762946747446 ) ) ;
#10546=CARTESIAN_POINT ( 'NONE',  ( 38.37017380507020192, -4.013682088886107557, 73.11602215082118050 ) ) ;
#10547=CARTESIAN_POINT ( 'NONE',  ( 38.26194895904384197, 1.396159133578087186, 72.51602215082118619 ) ) ;
#10549=CARTESIAN_POINT ( 'NONE',  ( 37.61123632939165873, -5.913682088886105248, 73.73360434286902887 ) ) ;
#10563=CARTESIAN_POINT ( 'NONE',  ( 39.73277004305197124, -17.40384086642191264, 69.52238214136768590 ) ) ;
#10565=CARTESIAN_POINT ( 'NONE',  ( 37.25202387243752611, -25.21368208888610241, 70.00779233799262613 ) ) ;
#10572=CARTESIAN_POINT ( 'NONE',  ( 39.12911128074873801, -26.11368208888610809, 73.69843995877326392 ) ) ;
#10578=CARTESIAN_POINT ( 'NONE',  ( 39.98359781491296161, -6.413682088886103472, 71.86517103874048473 ) ) ;
#10580=CARTESIAN_POINT ( 'NONE',  ( 36.68196826583682935, -21.61368208888610454, 71.96809898377888715 ) ) ;
#10583=CARTESIAN_POINT ( 'NONE',  ( 38.37017380507018771, -27.60384086642191548, 70.24448340153875847 ) ) ;
#10584=CARTESIAN_POINT ( 'NONE',  ( 40.14115730948191185, -12.51368208888610489, 71.32335560751960202 ) ) ;
#10590=CARTESIAN_POINT ( 'NONE',  ( 40.14115730948191185, -9.103840866421911926, 71.43714994484034264 ) ) ;
#10596=CARTESIAN_POINT ( 'NONE',  ( 40.14115730948191185, -6.513682088886103116, 71.32335560751961623 ) ) ;
#10598=CARTESIAN_POINT ( 'NONE',  ( 40.26954217208371034, -12.71368208888610241, 69.89063713639258424 ) ) ;
#10602=CARTESIAN_POINT ( 'NONE',  ( 37.31647492878124694, -10.30384086642191122, 72.03616607671141026 ) ) ;
#10607=CARTESIAN_POINT ( 'NONE',  ( 36.11133435605973574, -18.00384086642191050, 70.60699637195608602 ) ) ;
#10609=CARTESIAN_POINT ( 'NONE',  ( 38.37017380507020192, -24.01368208888610667, 73.11602215082115208 ) ) ;
#10619=CARTESIAN_POINT ( 'NONE',  ( 39.95015449827720744, -15.00384086642191228, 71.96809898377887293 ) ) ;
#10624=CARTESIAN_POINT ( 'NONE',  ( 37.25260217561390874, -2.003840866421909617, 70.97781676520604321 ) ) ;
#10627=CARTESIAN_POINT ( 'NONE',  ( 37.80618814713140097, -27.91368208888610880, 73.13360434286902034 ) ) ;
#10633=CARTESIAN_POINT ( 'NONE',  ( 39.37952058850012804, -29.00384086642191406, 71.78268878715390144 ) ) ;
#10636=CARTESIAN_POINT ( 'NONE',  ( 37.12184278917507640, 0.4863179111138996036, 71.43714994484035685 ) ) ;
#10643=CARTESIAN_POINT ( 'NONE',  ( 38.82593461698265003, -10.70384086642191690, 73.13360434286904876 ) ) ;
#10652=CARTESIAN_POINT ( 'NONE',  ( 38.93415946300898867, -8.113682088886108090, 73.09843995877331224 ) ) ;
#10654=CARTESIAN_POINT ( 'NONE',  ( 39.99513520555235857, -29.10876147765277722, 71.38080556064524274 ) ) ;
#10666=CARTESIAN_POINT ( 'NONE',  ( 35.86008812008917346, -0.1038408664219142574, 71.32335560751961623 ) ) ;
#10669=CARTESIAN_POINT ( 'NONE',  ( 39.02742774030102879, -16.21368208888609885, 72.26730301774234988 ) ) ;
#10673=CARTESIAN_POINT ( 'NONE',  ( 37.25202387243752611, -1.213682088886100630, 70.00779233799264034 ) ) ;
#10674=CARTESIAN_POINT ( 'NONE',  ( 37.33957961208645315, -27.80384086642191122, 69.94417936956671156 ) ) ;
#10678=CARTESIAN_POINT ( 'NONE',  ( 39.12911128074873801, -8.113682088886108090, 73.69843995877330656 ) ) ;
#10695=CARTESIAN_POINT ( 'NONE',  ( 36.36258059203030513, -15.90384086642191264, 69.89063713639259845 ) ) ;
#10700=CARTESIAN_POINT ( 'NONE',  ( 36.49096545463212493, -21.51368208888609956, 71.43714994484034264 ) ) ;
#10708=CARTESIAN_POINT ( 'NONE',  ( 36.98690846071097127, 0.1961591335780874246, 69.45876917294177133 ) ) ;
#10711=CARTESIAN_POINT ( 'NONE',  ( 39.98359781491296161, -4.413682088886105248, 71.86517103874048473 ) ) ;
#10713=CARTESIAN_POINT ( 'NONE',  ( 37.33957961208646736, -17.81368208888611093, 72.81632618279321889 ) ) ;
#10718=CARTESIAN_POINT ( 'NONE',  ( 39.31564783533279694, -19.30384086642191477, 70.72433947564853440 ) ) ;
#10719=CARTESIAN_POINT ( 'NONE',  ( 38.93415946300897446, -4.113682088886107202, 73.09843995877331224 ) ) ;
#10722=CARTESIAN_POINT ( 'NONE',  ( 40.14115730948191185, -3.103840866421910150, 71.43714994484034264 ) ) ;
#10724=CARTESIAN_POINT ( 'NONE',  ( 38.82593461698262871, -4.913682088886100807, 69.62690120949091011 ) ) ;
#10726=CARTESIAN_POINT ( 'NONE',  ( 36.89935272106204422, -11.21368208888610241, 69.52238214136768590 ) ) ;
#10729=CARTESIAN_POINT ( 'NONE',  ( 37.89291511884479036, -12.50384086642191228, 72.49843995877330372 ) ) ;
#10735=CARTESIAN_POINT ( 'NONE',  ( 36.07789103942399578, -14.20384086642191512, 72.05058123536544201 ) ) ;
#10739=CARTESIAN_POINT ( 'NONE',  ( 36.80608444377001121, -19.31368208888609672, 70.35351908239857721 ) ) ;
#10748=CARTESIAN_POINT ( 'NONE',  ( 37.33957961208645315, -15.80384086642190589, 69.94417936956672577 ) ) ;
#10754=CARTESIAN_POINT ( 'NONE',  ( 36.80608444377001831, -26.30384086642191477, 72.40698646996133903 ) ) ;
#10758=CARTESIAN_POINT ( 'NONE',  ( 38.93415946300897446, -26.11368208888610098, 73.09843995877328382 ) ) ;
#10763=CARTESIAN_POINT ( 'NONE',  ( 37.69225076346193504, -1.813682088886100274, 72.33091598616827866 ) ) ;
#10764=CARTESIAN_POINT ( 'NONE',  ( 37.38336156205274818, 0.2863179111139008137, 72.12822762946751709 ) ) ;
#10770=CARTESIAN_POINT ( 'NONE',  ( 37.80618814713138676, -1.703840866421908018, 69.62690120949091011 ) ) ;
#10776=CARTESIAN_POINT ( 'NONE',  ( 39.98359781491296161, 1.586317911113896528, 71.86517103874049894 ) ) ;
#10789=CARTESIAN_POINT ( 'NONE',  ( 38.73920764526925353, -18.11368208888610098, 72.49843995877330372 ) ) ;
#10794=CARTESIAN_POINT ( 'NONE',  ( 38.37017380507020192, -0.01368208888610777940, 73.11602215082118050 ) ) ;
#10795=CARTESIAN_POINT ( 'NONE',  ( 39.95015449827720744, -21.00384086642191406, 71.96809898377887293 ) ) ;
#10797=CARTESIAN_POINT ( 'NONE',  ( 36.89935272106204422, -11.21368208888610241, 69.52238214136768590 ) ) ;
#10815=CARTESIAN_POINT ( 'NONE',  ( 40.52078840805429394, -19.00384086642191406, 72.15350918040381600 ) ) ;
#10817=CARTESIAN_POINT ( 'NONE',  ( 38.26194895904383486, -23.01368208888609956, 69.64448340153877837 ) ) ;
#10825=CARTESIAN_POINT ( 'NONE',  ( 40.26954217208371034, -26.71368208888610596, 69.89063713639254161 ) ) ;
#10830=CARTESIAN_POINT ( 'NONE',  ( 39.82603832034400426, -4.313682088886107380, 72.40698646996135324 ) ) ;
#10834=CARTESIAN_POINT ( 'NONE',  ( 39.75915168707250302, -22.71368208888610241, 70.26145752964252722 ) ) ;
#10841=CARTESIAN_POINT ( 'NONE',  ( 38.00113996487112189, -19.70384086642190979, 70.22690120949090442 ) ) ;
#10842=CARTESIAN_POINT ( 'NONE',  ( 38.26194895904383486, -7.013682088886100452, 69.64448340153879258 ) ) ;
#10848=CARTESIAN_POINT ( 'NONE',  ( 37.25202387243754032, -4.403840866421916189, 72.75271321436733274 ) ) ;
#10851=CARTESIAN_POINT ( 'NONE',  ( 39.82603832034400426, -6.313682088886107380, 72.40698646996135324 ) ) ;
#10853=CARTESIAN_POINT ( 'NONE',  ( 40.33642880535524000, -12.31368208888611093, 72.77780686321126780 ) ) ;
#10856=CARTESIAN_POINT ( 'NONE',  ( 38.93987200065210175, -12.80384086642190944, 72.33091598616826445 ) ) ;
#10862=CARTESIAN_POINT ( 'NONE',  ( 36.89935272106205133, -16.40384086642191974, 73.23812341099225875 ) ) ;
#10866=CARTESIAN_POINT ( 'NONE',  ( 36.49096545463212493, -17.51368208888610667, 71.43714994484034264 ) ) ;
#10873=CARTESIAN_POINT ( 'NONE',  ( 38.37017380507018771, -13.60384086642190837, 69.64448340153877837 ) ) ;
#10875=CARTESIAN_POINT ( 'NONE',  ( 36.68196826583682935, -25.61368208888610454, 71.96809898377887293 ) ) ;
#10878=CARTESIAN_POINT ( 'NONE',  ( 38.93415946300896024, -23.50384086642189985, 69.66206559358661821 ) ) ;
#10880=CARTESIAN_POINT ( 'NONE',  ( 36.87297107704152666, -23.71368208888610951, 72.49904802271738902 ) ) ;
#10885=CARTESIAN_POINT ( 'NONE',  ( 38.37017380507018771, -29.60384086642191193, 70.24448340153875847 ) ) ;
#10886=CARTESIAN_POINT ( 'NONE',  ( 37.25260217561390874, 0.3863179111139002364, 71.78268878715394408 ) ) ;
#10893=CARTESIAN_POINT ( 'NONE',  ( 39.98359781491296161, -5.203840866421911571, 70.89533451361947414 ) ) ;
#10902=CARTESIAN_POINT ( 'NONE',  ( 38.93415946300898867, -2.113682088886109423, 73.09843995877331224 ) ) ;
#10920=CARTESIAN_POINT ( 'NONE',  ( 37.60469502381300089, -19.21368208888609885, 70.49320253461759478 ) ) ;
#10925=CARTESIAN_POINT ( 'NONE',  ( 39.82603832034400426, -2.313682088886107380, 72.40698646996135324 ) ) ;
#10926=CARTESIAN_POINT ( 'NONE',  ( 36.64852494920107517, -26.20384086642191335, 71.86517103874047052 ) ) ;
#10928=CARTESIAN_POINT ( 'NONE',  ( 40.26954217208371034, -10.71368208888610063, 69.89063713639259845 ) ) ;
#10943=CARTESIAN_POINT ( 'NONE',  ( 40.55423172469004101, -19.20384086642191335, 70.70992431699450265 ) ) ;
#10944=CARTESIAN_POINT ( 'NONE',  ( 39.75915168707250302, -22.71368208888610241, 70.26145752964251301 ) ) ;
#10950=CARTESIAN_POINT ( 'NONE',  ( 38.37017380507018771, 0.3961591335780896284, 69.04448340153882668 ) ) ;
#10953=APPLICATION_CONTEXT ( 'automotive_design' ) ;
#10955=CARTESIAN_POINT ( 'NONE',  ( 38.26194895904383486, -1.013682088886101784, 69.64448340153879258 ) ) ;
#10958=CARTESIAN_POINT ( 'NONE',  ( 39.38009889167650357, -22.21368208888610951, 72.75271321436731853 ) ) ;
#10961=CARTESIAN_POINT ( 'NONE',  ( 38.63098279924290068, -18.70384086642191335, 72.53360434286904024 ) ) ;
#10962=CARTESIAN_POINT ( 'NONE',  ( 37.25202387243752611, -3.213682088886102406, 70.00779233799264034 ) ) ;
#10966=CARTESIAN_POINT ( 'NONE',  ( 36.87297107704149823, -5.903840866421907307, 70.26145752964255564 ) ) ;
#10970=CARTESIAN_POINT ( 'NONE',  ( 37.25202387243752611, -3.213682088886102406, 70.00779233799264034 ) ) ;
#10972=CARTESIAN_POINT ( 'NONE',  ( 36.89935272106204422, -7.213682088886102406, 69.52238214136768590 ) ) ;
#10976=CARTESIAN_POINT ( 'NONE',  ( 38.37017380507018771, -13.60384086642191193, 70.24448340153875847 ) ) ;
#10982=CARTESIAN_POINT ( 'NONE',  ( 40.55423172469004101, -19.20384086642191335, 70.70992431699450265 ) ) ;
#10986=CARTESIAN_POINT ( 'NONE',  ( 40.14115730948191185, -20.51368208888609601, 71.32335560751960202 ) ) ;
#10992=CARTESIAN_POINT ( 'NONE',  ( 39.98359781491296161, -11.20384086642191335, 70.89533451361947414 ) ) ;
#10996=CARTESIAN_POINT ( 'NONE',  ( 36.87297107704152666, -25.71368208888609885, 72.49904802271738902 ) ) ;
#11000=CARTESIAN_POINT ( 'NONE',  ( 37.25202387243754032, -22.40384086642191619, 72.75271321436731853 ) ) ;
#11002=CARTESIAN_POINT ( 'NONE',  ( 37.25202387243752611, -25.21368208888610241, 70.00779233799262613 ) ) ;
#11007=CARTESIAN_POINT ( 'NONE',  ( 37.60469502381300089, 0.7863179111138978161, 70.49320253461759478 ) ) ;
#11014=ORIENTED_EDGE ( 'NONE', *, *, #10532, .T. ) ;
#11016=CARTESIAN_POINT ( 'NONE',  ( 39.29254315202757653, -6.803840866421915656, 72.81632618279323310 ) ) ;
#11024=CARTESIAN_POINT ( 'NONE',  ( 39.98359781491296161, -0.4136820888861053591, 71.86517103874048473 ) ) ;
#11025=CARTESIAN_POINT ( 'NONE',  ( 37.69796330110505522, -26.50384086642191050, 73.09843995877328382 ) ) ;
#11042=CARTESIAN_POINT ( 'NONE',  ( 39.31564783533280405, -14.31368208888609850, 72.03616607671141026 ) ) ;
#11046=CARTESIAN_POINT ( 'NONE',  ( 38.93415946300897446, -4.113682088886107202, 73.09843995877331224 ) ) ;
#11047=CARTESIAN_POINT ( 'NONE',  ( 39.82603832034400426, -21.30384086642191122, 70.35351908239857721 ) ) ;
#11049=CARTESIAN_POINT ( 'NONE',  ( 37.50301148336529167, 0.8863179111139005695, 69.06206559358666652 ) ) ;
#11071=CARTESIAN_POINT ( 'NONE',  ( 39.64521430340305841, -14.80384086642191832, 73.30173637941818754 ) ) ;
#11075=CARTESIAN_POINT ( 'NONE',  ( 40.14115730948191185, -18.51368208888610667, 71.32335560751960202 ) ) ;
#11082=CARTESIAN_POINT ( 'NONE',  ( 38.37017380507020192, -28.01368208888610667, 73.71602215082113219 ) ) ;
#11087=CARTESIAN_POINT ( 'NONE',  ( 37.80618814713140097, 0.08631791111389161553, 73.13360434286904876 ) ) ;
#11089=CARTESIAN_POINT ( 'NONE',  ( 37.33957961208646736, -11.81368208888610916, 72.81632618279321889 ) ) ;
#11093=CARTESIAN_POINT ( 'NONE',  ( 38.26194895904384197, -20.60384086642191193, 72.51602215082118619 ) ) ;
#11094=CARTESIAN_POINT ( 'NONE',  ( 38.82593461698262871, -2.913682088886099919, 69.62690120949091011 ) ) ;
#11099=CARTESIAN_POINT ( 'NONE',  ( 36.87297107704149823, -3.903840866421907752, 70.26145752964255564 ) ) ;
#11102=CARTESIAN_POINT ( 'NONE',  ( 38.26194895904383486, -1.013682088886101784, 69.64448340153879258 ) ) ;
#11104=CARTESIAN_POINT ( 'NONE',  ( 40.55423172469004811, -10.41368208888610347, 72.05058123536544201 ) ) ;
#11108=CARTESIAN_POINT ( 'NONE',  ( 37.21915885897815457, -14.20384086642191335, 71.67976084211552745 ) ) ;
#11114=CARTESIAN_POINT ( 'NONE',  ( 40.26954217208372455, -14.90384086642191797, 72.86986841596734621 ) ) ;
#11117=CARTESIAN_POINT ( 'NONE',  ( 37.69796330110504101, -19.11368208888610098, 69.66206559358661821 ) ) ;
#11127=CARTESIAN_POINT ( 'NONE',  ( 36.87297107704151244, -7.903840866421909084, 70.26145752964255564 ) ) ;
#11129=CARTESIAN_POINT ( 'NONE',  ( 37.33957961208646736, -27.81368208888611093, 72.81632618279320468 ) ) ;
#11131=CARTESIAN_POINT ( 'NONE',  ( 36.87297107704149823, -25.90384086642190908, 70.26145752964251301 ) ) ;
#11135=CARTESIAN_POINT ( 'NONE',  ( 39.82603832034400426, -18.31368208888610738, 72.40698646996133903 ) ) ;
#11137=CARTESIAN_POINT ( 'NONE',  ( 40.77203464402485622, -28.51368208888610667, 71.32335560751960202 ) ) ;
#11142=CARTESIAN_POINT ( 'NONE',  ( 38.63098279924288647, -0.9136820888861024725, 70.22690120949091863 ) ) ;
#11148=CARTESIAN_POINT ( 'NONE',  ( 36.87297107704149823, -5.903840866421907307, 70.26145752964255564 ) ) ;
#11157=CARTESIAN_POINT ( 'NONE',  ( 38.93415946300898867, -4.113682088886107202, 73.09843995877331224 ) ) ;
#11178=CARTESIAN_POINT ( 'NONE',  ( 38.63098279924288647, -16.91368208888609814, 70.22690120949090442 ) ) ;
#11184=CARTESIAN_POINT ( 'NONE',  ( 39.29254315202757653, -26.80384086642191477, 72.81632618279320468 ) ) ;
#11188=CARTESIAN_POINT ( 'NONE',  ( 36.29569395875879678, -3.313682088886101607, 69.98269868914869107 ) ) ;
#11205=CARTESIAN_POINT ( 'NONE',  ( 39.02088643472237806, -12.70384086642191690, 73.73360434286898624 ) ) ;
#11207=CARTESIAN_POINT ( 'NONE',  ( 36.80608444377001121, -21.31368208888610027, 70.35351908239857721 ) ) ;
#11212=PRODUCT_DEFINITION ( 'UNKNOWN', '', #997, #18020 ) ;
#11214=CARTESIAN_POINT ( 'NONE',  ( 40.33642880535524000, -18.31368208888610383, 72.77780686321126780 ) ) ;
#11218=CARTESIAN_POINT ( 'NONE',  ( 38.93415946300897446, -2.113682088886109423, 73.09843995877331224 ) ) ;
#11221=CARTESIAN_POINT ( 'NONE',  ( 40.14115730948191185, -16.51368208888610667, 71.32335560751960202 ) ) ;
#11222=CARTESIAN_POINT ( 'NONE',  ( 39.66066260159681889, -29.10876147764981781, 69.85357445396793707 ) ) ;
#11225=CARTESIAN_POINT ( 'NONE',  ( 37.60469502381300799, -18.40384086642190908, 72.26730301774234988 ) ) ;
#11226=CARTESIAN_POINT ( 'NONE',  ( 36.68196826583682935, -7.613682088886103649, 71.96809898377890136 ) ) ;
#11233=CARTESIAN_POINT ( 'NONE',  ( 37.25202387243754032, -6.403840866421914413, 72.75271321436733274 ) ) ;
#11236=CARTESIAN_POINT ( 'NONE',  ( 38.63098279924288647, -28.91368208888610170, 70.22690120949089021 ) ) ;
#11238=CARTESIAN_POINT ( 'NONE',  ( 36.11133435605973574, -7.613682088886103649, 72.15350918040385864 ) ) ;
#11242=CARTESIAN_POINT ( 'NONE',  ( 37.38336156205273397, -3.903840866421911748, 70.63227792289248441 ) ) ;
#11243=EDGE_CURVE ( 'NONE', #3300, #25416, #11910, .T. ) ;
#11249=CARTESIAN_POINT ( 'NONE',  ( 35.86008812008917346, -8.103840866421913702, 71.32335560751961623 ) ) ;
#11252=CARTESIAN_POINT ( 'NONE',  ( 36.68196826583682935, -23.61368208888610454, 71.96809898377887293 ) ) ;
#11260=CARTESIAN_POINT ( 'NONE',  ( 36.49096545463212493, -6.103840866421912814, 71.32335560751963044 ) ) ;
#11263=CARTESIAN_POINT ( 'NONE',  ( 39.38009889167650357, -26.21368208888610951, 72.75271321436730432 ) ) ;
#11266=CARTESIAN_POINT ( 'NONE',  ( 38.26194895904384907, -22.60384086642191548, 73.11602215082116629 ) ) ;
#11271=CARTESIAN_POINT ( 'NONE',  ( 39.38009889167650357, -16.21368208888610596, 72.75271321436731853 ) ) ;
#11273=CARTESIAN_POINT ( 'NONE',  ( 40.52078840805428683, -28.61368208888610454, 70.60699637195608602 ) ) ;
#11278=CARTESIAN_POINT ( 'NONE',  ( 39.31564783533279694, -25.30384086642191477, 70.72433947564850598 ) ) ;
#11286=CARTESIAN_POINT ( 'NONE',  ( 38.26194895904384907, -4.603840866421914590, 73.11602215082118050 ) ) ;
#11294=CARTESIAN_POINT ( 'NONE',  ( 39.29254315202756231, -0.8136820888860994971, 69.94417936956673998 ) ) ;
#11296=CARTESIAN_POINT ( 'NONE',  ( 38.82593461698264292, -24.70384086642191335, 73.13360434286902034 ) ) ;
#11312=CARTESIAN_POINT ( 'NONE',  ( 38.37017380507020192, -10.01368208888610312, 72.51602215082118619 ) ) ;
#11317=CARTESIAN_POINT ( 'NONE',  ( 38.93415946300896024, -23.50384086642189985, 69.66206559358661821 ) ) ;
#11337=CARTESIAN_POINT ( 'NONE',  ( 38.37017380507018771, -9.603840866421911926, 69.04448340153881247 ) ) ;
#11339=CARTESIAN_POINT ( 'NONE',  ( 39.29254315202756231, -14.81368208888610205, 69.94417936956672577 ) ) ;
#11344=CARTESIAN_POINT ( 'NONE',  ( 40.52078840805428683, -22.61368208888610454, 70.60699637195608602 ) ) ;
#11352=CARTESIAN_POINT ( 'NONE',  ( 38.37017380507018771, -11.60384086642191015, 70.24448340153877268 ) ) ;
#11353=CARTESIAN_POINT ( 'NONE',  ( 37.25202387243752611, -1.213682088886100630, 70.00779233799264034 ) ) ;
#11360=CARTESIAN_POINT ( 'NONE',  ( 40.14115730948191185, -1.103840866421911260, 71.43714994484034264 ) ) ;
#11361=CARTESIAN_POINT ( 'NONE',  ( 37.69796330110504101, -1.113682088886101207, 69.66206559358663242 ) ) ;
#11363=CARTESIAN_POINT ( 'NONE',  ( 36.07789103942398867, -5.413682088886107024, 70.70992431699450265 ) ) ;
#11366=CARTESIAN_POINT ( 'NONE',  ( 37.21915885897815457, -6.203840866421912459, 71.67976084211552745 ) ) ;
#11371=CARTESIAN_POINT ( 'NONE',  ( 39.02088643472237806, -10.70384086642192045, 73.73360434286902887 ) ) ;
#11374=CARTESIAN_POINT ( 'NONE',  ( 38.82593461698262871, -14.91368208888609637, 69.62690120949091011 ) ) ;
#11379=CARTESIAN_POINT ( 'NONE',  ( 37.80618814713138676, -5.703840866421908018, 69.62690120949091011 ) ) ;
#11383=CARTESIAN_POINT ( 'NONE',  ( 38.37017380507020192, -16.01368208888610667, 73.11602215082116629 ) ) ;
#11387=CARTESIAN_POINT ( 'NONE',  ( 37.33957961208645315, -15.80384086642190589, 69.94417936956672577 ) ) ;
#11389=CARTESIAN_POINT ( 'NONE',  ( 36.68196826583682935, -19.61368208888610809, 71.96809898377888715 ) ) ;
#11391=CARTESIAN_POINT ( 'NONE',  ( 36.36258059203031934, -27.71368208888610596, 72.86986841596734621 ) ) ;
#11395=CARTESIAN_POINT ( 'NONE',  ( 37.12184278917507640, -22.10384086642191193, 71.32335560751961623 ) ) ;
#11403=CARTESIAN_POINT ( 'NONE',  ( 36.89935272106205133, -26.40384086642191974, 73.23812341099225875 ) ) ;
#11412=CARTESIAN_POINT ( 'NONE',  ( 39.95015449827720744, -25.00384086642191406, 71.96809898377885872 ) ) ;
#11419=CARTESIAN_POINT ( 'NONE',  ( 37.89291511884479036, -4.503840866421912281, 72.49843995877331793 ) ) ;
#11426=CARTESIAN_POINT ( 'NONE',  ( 37.21915885897815457, -13.41368208888610170, 71.08074471024443142 ) ) ;
#11429=CARTESIAN_POINT ( 'NONE',  ( 39.51027997493896748, -12.51368208888610134, 71.32335560751960202 ) ) ;
#11436=CARTESIAN_POINT ( 'NONE',  ( 38.82593461698265003, -14.70384086642191512, 73.13360434286903455 ) ) ;
#11438=CARTESIAN_POINT ( 'NONE',  ( 39.51027997493896748, -18.51368208888610312, 71.32335560751960202 ) ) ;
#11459=CARTESIAN_POINT ( 'NONE',  ( 40.26954217208372455, -8.903840866421921518, 72.86986841596736042 ) ) ;
#11462=CARTESIAN_POINT ( 'NONE',  ( 38.26194895904383486, -15.01368208888610134, 69.64448340153877837 ) ) ;
#11468=CARTESIAN_POINT ( 'NONE',  ( 39.73277004305198545, -24.21368208888610951, 73.23812341099225875 ) ) ;
#11479=CARTESIAN_POINT ( 'NONE',  ( 39.24876120206129571, -14.90384086642191264, 72.12822762946747446 ) ) ;
#11480=CARTESIAN_POINT ( 'NONE',  ( 39.75915168707250302, -0.7136820888860997414, 70.26145752964252722 ) ) ;
#11488=CARTESIAN_POINT ( 'NONE',  ( 38.93415946300896024, 0.4961591335780925482, 69.66206559358664663 ) ) ;
#11490=CARTESIAN_POINT ( 'NONE',  ( 39.41296390513587511, -28.41368208888610525, 71.67976084211548482 ) ) ;
#11491=CARTESIAN_POINT ( 'NONE',  ( 36.98690846071097837, -5.813682088886107380, 73.30173637941818754 ) ) ;
#11494=CARTESIAN_POINT ( 'NONE',  ( 37.89291511884479036, -2.503840866421910505, 72.49843995877331793 ) ) ;
#11500=CARTESIAN_POINT ( 'NONE',  ( 40.26954217208372455, -8.903840866421921518, 72.86986841596736042 ) ) ;
#11503=CARTESIAN_POINT ( 'NONE',  ( 37.69796330110504101, -17.11368208888610098, 69.66206559358661821 ) ) ;
#11510=CARTESIAN_POINT ( 'NONE',  ( 39.29254315202757653, -10.80384086642191477, 72.81632618279323310 ) ) ;
#11514=CARTESIAN_POINT ( 'NONE',  ( 36.68196826583682935, -19.61368208888610809, 71.96809898377888715 ) ) ;
#11517=CARTESIAN_POINT ( 'NONE',  ( 38.93415946300896024, -19.50384086642191050, 69.66206559358661821 ) ) ;
#11520=CARTESIAN_POINT ( 'NONE',  ( 38.26194895904383486, -21.01368208888610312, 69.64448340153877837 ) ) ;
#11522=CARTESIAN_POINT ( 'NONE',  ( 36.29569395875879678, -25.31368208888610027, 69.98269868914866265 ) ) ;
#11526=CARTESIAN_POINT ( 'NONE',  ( 38.73920764526923932, -27.50384086642191406, 70.26206559358661252 ) ) ;
#11534=CARTESIAN_POINT ( 'NONE',  ( 38.37017380507018771, -29.60384086642191193, 69.04448340153878405 ) ) ;
#11543=CARTESIAN_POINT ( 'NONE',  ( 36.64852494920107517, -28.20384086642191335, 71.86517103874047052 ) ) ;
#11553=CARTESIAN_POINT ( 'NONE',  ( 37.60469502381300799, -4.403840866421911748, 72.26730301774236409 ) ) ;
#11559=CARTESIAN_POINT ( 'NONE',  ( 37.25260217561390874, -13.61368208888610098, 71.78268878715392987 ) ) ;
#11560=CARTESIAN_POINT ( 'NONE',  ( 39.24876120206128860, -10.71368208888610063, 70.63227792289247020 ) ) ;
#11567=CARTESIAN_POINT ( 'NONE',  ( 39.75915168707251723, -16.90384086642191619, 72.49904802271738902 ) ) ;
#11572=CARTESIAN_POINT ( 'NONE',  ( 39.24876120206128860, -20.71368208888610596, 70.63227792289245599 ) ) ;
#11588=CARTESIAN_POINT ( 'NONE',  ( 36.29569395875881099, -12.30384086642192010, 72.77780686321128201 ) ) ;
#11590=CARTESIAN_POINT ( 'NONE',  ( 37.80618814713140097, -17.91368208888609814, 73.13360434286903455 ) ) ;
#11594=CARTESIAN_POINT ( 'NONE',  ( 36.29569395875879678, -23.31368208888610383, 69.98269868914866265 ) ) ;
#11603=CARTESIAN_POINT ( 'NONE',  ( 38.73920764526923932, -9.503840866421912281, 70.26206559358664094 ) ) ;
#11604=CARTESIAN_POINT ( 'NONE',  ( 37.12184278917507640, -27.51368208888609956, 71.43714994484032843 ) ) ;
#11610=CARTESIAN_POINT ( 'NONE',  ( 36.87297107704149823, 0.09615913357809147133, 70.26145752964255564 ) ) ;
#11611=CARTESIAN_POINT ( 'NONE',  ( 38.00113996487114321, -27.91368208888610170, 72.53360434286901182 ) ) ;
#11612=CARTESIAN_POINT ( 'NONE',  ( 39.64521430340304420, -4.813682088886099386, 69.45876917294177133 ) ) ;
#11617=CARTESIAN_POINT ( 'NONE',  ( 37.38336156205273397, -7.903840866421910860, 70.63227792289248441 ) ) ;
#11625=CARTESIAN_POINT ( 'NONE',  ( 37.61123632939164452, -7.703840866421914235, 69.02690120949094421 ) ) ;
#11630=CARTESIAN_POINT ( 'NONE',  ( 36.64852494920107517, -11.41368208888610525, 70.89533451361947414 ) ) ;
#11636=CARTESIAN_POINT ( 'NONE',  ( 36.80608444377002542, -4.303840866421916544, 72.40698646996135324 ) ) ;
#11641=CARTESIAN_POINT ( 'NONE',  ( 36.68196826583682935, -21.61368208888610454, 71.96809898377888715 ) ) ;
#11644=CARTESIAN_POINT ( 'NONE',  ( 38.93415946300896024, -17.50384086642190695, 69.66206559358661821 ) ) ;
#11648=CARTESIAN_POINT ( 'NONE',  ( 40.14115730948191185, -16.51368208888610667, 71.32335560751960202 ) ) ;
#11650=CARTESIAN_POINT ( 'NONE',  ( 38.26194895904383486, -21.01368208888610312, 69.04448340153878405 ) ) ;
#11655=CARTESIAN_POINT ( 'NONE',  ( 37.12184278917507640, -24.10384086642191193, 71.32335560751960202 ) ) ;
#11662=CARTESIAN_POINT ( 'NONE',  ( 38.93415946300896024, 0.4961591335780925482, 69.66206559358664663 ) ) ;
#11665=CARTESIAN_POINT ( 'NONE',  ( 40.52078840805428683, -4.613682088886104538, 70.60699637195608602 ) ) ;
#11673=CARTESIAN_POINT ( 'NONE',  ( 36.80608444377002542, -22.30384086642191477, 72.40698646996133903 ) ) ;
#11681=CARTESIAN_POINT ( 'NONE',  ( 37.60469502381300799, -6.403840866421910860, 72.26730301774236409 ) ) ;
#11690=CARTESIAN_POINT ( 'NONE',  ( 37.89291511884476904, -9.113682088886102761, 70.26206559358664094 ) ) ;
#11691=CARTESIAN_POINT ( 'NONE',  ( 38.63098279924288647, -10.91368208888610170, 70.22690120949091863 ) ) ;
#11698=CARTESIAN_POINT ( 'NONE',  ( 38.37017380507020192, 1.986317911113890444, 73.11602215082119471 ) ) ;
#11699=CARTESIAN_POINT ( 'NONE',  ( 39.29254315202757653, -16.80384086642191477, 72.81632618279321889 ) ) ;
#11701=CARTESIAN_POINT ( 'NONE',  ( 38.73920764526925353, -18.11368208888610098, 72.49843995877330372 ) ) ;
#11706=CARTESIAN_POINT ( 'NONE',  ( 36.68196826583682935, -15.61368208888610454, 71.96809898377888715 ) ) ;
#11721=CARTESIAN_POINT ( 'NONE',  ( 40.77203464402485622, -11.10384086642191193, 71.43714994484034264 ) ) ;
#11724=CARTESIAN_POINT ( 'NONE',  ( 39.82603832034400426, -16.31368208888610738, 72.40698646996133903 ) ) ;
#11730=CARTESIAN_POINT ( 'NONE',  ( 38.37017380507020192, -20.01368208888611022, 73.71602215082113219 ) ) ;
#11740=CARTESIAN_POINT ( 'NONE',  ( 39.51027997493896748, -13.10384086642191015, 71.43714994484032843 ) ) ;
#11741=CARTESIAN_POINT ( 'NONE',  ( 36.87297107704152666, 0.2863179111138939303, 72.49904802271743165 ) ) ;
#11746=EDGE_LOOP ( 'NONE', ( #23543, #23975, #7456 ) ) ;
#11747=CARTESIAN_POINT ( 'NONE',  ( 36.11133435605973574, -28.00384086642191761, 70.60699637195608602 ) ) ;
#11748=CARTESIAN_POINT ( 'NONE',  ( 38.26194895904383486, -23.01368208888610312, 70.24448340153875847 ) ) ;
#11749=CARTESIAN_POINT ( 'NONE',  ( 40.26954217208371034, -4.713682088886099741, 69.89063713639259845 ) ) ;
#11753=CARTESIAN_POINT ( 'NONE',  ( 38.93987200065210175, -2.803840866421911660, 72.33091598616827866 ) ) ;
#11759=CARTESIAN_POINT ( 'NONE',  ( 36.07789103942399578, -10.20384086642191690, 72.05058123536544201 ) ) ;
#11762=CARTESIAN_POINT ( 'NONE',  ( 37.25202387243752611, -13.21368208888610063, 70.00779233799262613 ) ) ;
#11766=CARTESIAN_POINT ( 'NONE',  ( 36.64852494920107517, -2.203840866421912015, 71.86517103874049894 ) ) ;
#11769=CARTESIAN_POINT ( 'NONE',  ( 38.26194895904383486, -21.01368208888610312, 69.64448340153877837 ) ) ;
#11773=CARTESIAN_POINT ( 'NONE',  ( 39.95015449827720744, -19.00384086642191406, 71.96809898377887293 ) ) ;
#11776=CARTESIAN_POINT ( 'NONE',  ( 39.75915168707250302, -12.71368208888610063, 70.26145752964251301 ) ) ;
#11778=CARTESIAN_POINT ( 'NONE',  ( 39.73277004305198545, -24.21368208888610951, 73.23812341099225875 ) ) ;
#11782=CARTESIAN_POINT ( 'NONE',  ( 37.89291511884479036, -26.50384086642191406, 72.49843995877328950 ) ) ;
#11789=CARTESIAN_POINT ( 'NONE',  ( 39.38009889167648936, 0.5961591335780919154, 70.00779233799265455 ) ) ;
#11791=CARTESIAN_POINT ( 'NONE',  ( 40.52078840805428683, -2.613682088886105870, 70.60699637195608602 ) ) ;
#11798=CARTESIAN_POINT ( 'NONE',  ( 37.33957961208645315, -23.80384086642191122, 69.94417936956671156 ) ) ;
#11805=CARTESIAN_POINT ( 'NONE',  ( 37.69225076346193504, -3.803840866421912992, 70.42958956619168021 ) ) ;
#11812=CARTESIAN_POINT ( 'NONE',  ( 37.69225076346193504, -11.81368208888610205, 72.33091598616826445 ) ) ;
#11813=CARTESIAN_POINT ( 'NONE',  ( 37.25260217561390874, -9.613682088886102761, 71.78268878715394408 ) ) ;
#11821=CARTESIAN_POINT ( 'NONE',  ( 39.75915168707251723, -14.90384086642191086, 72.49904802271738902 ) ) ;
#11826=CARTESIAN_POINT ( 'NONE',  ( 38.63098279924288647, -16.91368208888609814, 70.22690120949090442 ) ) ;
#11830=CARTESIAN_POINT ( 'NONE',  ( 36.64852494920107517, -15.41368208888610525, 70.89533451361947414 ) ) ;
#11834=CARTESIAN_POINT ( 'NONE',  ( 40.14115730948191185, -28.51368208888610667, 71.32335560751958781 ) ) ;
#11844=CARTESIAN_POINT ( 'NONE',  ( 36.07789103942399578, -6.203840866421916900, 72.05058123536544201 ) ) ;
#11847=CARTESIAN_POINT ( 'NONE',  ( 37.80618814713140097, -13.91368208888610347, 73.13360434286903455 ) ) ;
#11851=CARTESIAN_POINT ( 'NONE',  ( 40.55423172469004811, -12.41368208888610525, 72.05058123536544201 ) ) ;
#11864=CARTESIAN_POINT ( 'NONE',  ( 37.31647492878124694, -10.30384086642191122, 72.03616607671141026 ) ) ;
#11865=CARTESIAN_POINT ( 'NONE',  ( 38.26194895904383486, -29.01368208888610312, 70.24448340153875847 ) ) ;
#11873=CARTESIAN_POINT ( 'NONE',  ( 40.33642880535521869, -23.30384086642191477, 69.98269868914866265 ) ) ;
#11875=CARTESIAN_POINT ( 'NONE',  ( 38.37017380507020192, -22.01368208888610312, 72.51602215082118619 ) ) ;
#11876=CARTESIAN_POINT ( 'NONE',  ( 36.07789103942398867, -3.413682088886104804, 70.70992431699450265 ) ) ;
#11879=CARTESIAN_POINT ( 'NONE',  ( 37.60469502381300799, -0.4038408664219124145, 72.26730301774236409 ) ) ;
#11883=CARTESIAN_POINT ( 'NONE',  ( 36.98690846071097127, -5.803840866421911215, 69.45876917294177133 ) ) ;
#11887=CARTESIAN_POINT ( 'NONE',  ( 36.80608444377001121, -13.31368208888609672, 70.35351908239857721 ) ) ;
#11889=CARTESIAN_POINT ( 'NONE',  ( 37.33957961208646736, -23.81368208888611093, 72.81632618279320468 ) ) ;
#11891=CARTESIAN_POINT ( 'NONE',  ( 38.26194895904384907, -4.603840866421914590, 73.11602215082118050 ) ) ;
#11893=CARTESIAN_POINT ( 'NONE',  ( 37.33957961208646736, -17.81368208888611093, 72.81632618279321889 ) ) ;
#11897=CARTESIAN_POINT ( 'NONE',  ( 36.64852494920107517, -18.20384086642191335, 71.86517103874048473 ) ) ;
#11899=CARTESIAN_POINT ( 'NONE',  ( 39.29254315202756231, -14.81368208888610205, 69.94417936956672577 ) ) ;
#11901=CARTESIAN_POINT ( 'NONE',  ( 40.33642880535524000, -20.31368208888610738, 72.77780686321126780 ) ) ;
#11905=CARTESIAN_POINT ( 'NONE',  ( 39.02742774030101458, -21.40384086642191619, 70.49320253461759478 ) ) ;
#11909=CARTESIAN_POINT ( 'NONE',  ( 39.62003278564551323, -28.88720382805528430, 70.76953470883664465 ) ) ;
#11910=B_SPLINE_CURVE_WITH_KNOTS ( 'NONE', 3,
 ( #20342, #2673, #2542, #10044, #12117, #10426, #5259, #20461 ),
 .UNSPECIFIED., .F., .F.,
 ( 4, 2, 2, 4 ),
 ( 0.0001628760028480823424, 0.0003078672859939987996, 0.0004528585691399152568, 0.0007428411354317482253 ),
 .UNSPECIFIED. ) ;
#11913=CARTESIAN_POINT ( 'NONE',  ( 39.75915168707251723, -0.9038408664219161892, 72.49904802271740323 ) ) ;
#11916=CARTESIAN_POINT ( 'NONE',  ( 36.98690846071097837, 0.1863179111138910382, 73.30173637941818754 ) ) ;
#11923=CARTESIAN_POINT ( 'NONE',  ( 36.64852494920107517, -20.20384086642191335, 71.86517103874048473 ) ) ;
#11932=CARTESIAN_POINT ( 'NONE',  ( 38.26194895904384197, -8.603840866421911926, 72.51602215082118619 ) ) ;
#11942=CARTESIAN_POINT ( 'NONE',  ( 38.73920764526925353, -10.11368208888610276, 72.49843995877331793 ) ) ;
#11943=CARTESIAN_POINT ( 'NONE',  ( 37.60469502381300089, -5.213682088886100630, 70.49320253461759478 ) ) ;
#11951=CARTESIAN_POINT ( 'NONE',  ( 36.68196826583682935, -16.00384086642191050, 70.79240656858107172 ) ) ;
#11956=CARTESIAN_POINT ( 'NONE',  ( 37.25260217561390874, -19.61368208888610098, 71.78268878715392987 ) ) ;
#11963=CARTESIAN_POINT ( 'NONE',  ( 38.82593461698262871, -12.91368208888610170, 69.62690120949091011 ) ) ;
#11968=CARTESIAN_POINT ( 'NONE',  ( 40.02576592390014554, -29.10876147765401001, 70.31011966505063526 ) ) ;
#11977=CARTESIAN_POINT ( 'NONE',  ( 40.52078840805429394, -5.003840866421915834, 72.15350918040385864 ) ) ;
#11982=CARTESIAN_POINT ( 'NONE',  ( 39.29254315202756231, -8.813682088886100274, 69.94417936956673998 ) ) ;
#11986=CARTESIAN_POINT ( 'NONE',  ( 36.98690846071097837, -15.81368208888610916, 73.30173637941818754 ) ) ;
#11996=CARTESIAN_POINT ( 'NONE',  ( 38.26194895904383486, -27.01368208888609956, 70.24448340153875847 ) ) ;
#12002=CARTESIAN_POINT ( 'NONE',  ( 39.12911128074872380, -21.50384086642191406, 69.06206559358665231 ) ) ;
#12003=CARTESIAN_POINT ( 'NONE',  ( 37.12184278917507640, -21.51368208888609956, 71.43714994484034264 ) ) ;
#12005=CARTESIAN_POINT ( 'NONE',  ( 39.98359781491296161, -28.41368208888610525, 71.86517103874045631 ) ) ;
#12007=CARTESIAN_POINT ( 'NONE',  ( 37.38336156205273397, 0.09615913357808798800, 70.63227792289248441 ) ) ;
#12012=CARTESIAN_POINT ( 'NONE',  ( 39.64521430340305841, -2.803840866421918765, 73.30173637941818754 ) ) ;
#12016=CARTESIAN_POINT ( 'NONE',  ( 39.29254315202756231, -4.813682088886099386, 69.94417936956673998 ) ) ;
#12019=CARTESIAN_POINT ( 'NONE',  ( 39.82603832034401847, -26.31368208888610738, 72.40698646996131060 ) ) ;
#12021=CARTESIAN_POINT ( 'NONE',  ( 37.80618814713138676, 0.2961591335780937584, 69.62690120949092432 ) ) ;
#12023=CARTESIAN_POINT ( 'NONE',  ( 38.93987200065210175, -24.80384086642191477, 72.33091598616823603 ) ) ;
#12024=CARTESIAN_POINT ( 'NONE',  ( 39.95015449827720744, -10.61368208888610631, 70.79240656858107172 ) ) ;
#12028=CARTESIAN_POINT ( 'NONE',  ( 39.98359781491296161, -13.20384086642191157, 70.89533451361945993 ) ) ;
#12031=CARTESIAN_POINT ( 'NONE',  ( 36.87297107704152666, -9.713682088886107735, 72.49904802271743165 ) ) ;
#12033=CARTESIAN_POINT ( 'NONE',  ( 39.02088643472237095, -24.91368208888610170, 69.02690120949091579 ) ) ;
#12036=CARTESIAN_POINT ( 'NONE',  ( 38.93987200065210175, -18.80384086642191122, 72.33091598616826445 ) ) ;
#12039=CARTESIAN_POINT ( 'NONE',  ( 39.60564227155354189, -28.80873119892454071, 70.65162531128912349 ) ) ;
#12041=CARTESIAN_POINT ( 'NONE',  ( 36.11133435605973574, -22.00384086642191761, 70.60699637195608602 ) ) ;
#12043=CARTESIAN_POINT ( 'NONE',  ( 36.80608444377001121, -27.31368208888610383, 70.35351908239857721 ) ) ;
#12052=CARTESIAN_POINT ( 'NONE',  ( 37.33957961208645315, -21.80384086642190766, 69.94417936956672577 ) ) ;
#12059=CARTESIAN_POINT ( 'NONE',  ( 37.31647492878124694, -2.303840866421911215, 72.03616607671141026 ) ) ;
#12067=CARTESIAN_POINT ( 'NONE',  ( 38.93987200065208754, -8.813682088886096722, 70.42958956619168021 ) ) ;
#12068=CARTESIAN_POINT ( 'NONE',  ( 37.38336156205274818, -7.713682088886103294, 72.12822762946751709 ) ) ;
#12075=CARTESIAN_POINT ( 'NONE',  ( 37.69796330110505522, -8.503840866421915834, 73.09843995877331224 ) ) ;
#12083=CARTESIAN_POINT ( 'NONE',  ( 37.80618814713140097, -9.913682088886107024, 73.13360434286904876 ) ) ;
#12102=CARTESIAN_POINT ( 'NONE',  ( 36.29569395875881099, -6.303840866421917433, 72.77780686321129622 ) ) ;
#12107=CARTESIAN_POINT ( 'NONE',  ( 38.82593461698262871, -10.91368208888609992, 69.62690120949091011 ) ) ;
#12113=CARTESIAN_POINT ( 'NONE',  ( 39.02088643472237095, -14.91368208888609992, 69.02690120949091579 ) ) ;
#12117=CARTESIAN_POINT ( 'NONE',  ( 39.61922982725797482, -28.88282523147813663, 69.90442756104691568 ) ) ;
#12124=CARTESIAN_POINT ( 'NONE',  ( 38.63098279924288647, -22.91368208888609814, 70.22690120949090442 ) ) ;
#12131=CARTESIAN_POINT ( 'NONE',  ( 38.37017380507018771, -25.60384086642191548, 69.04448340153878405 ) ) ;
#12134=CARTESIAN_POINT ( 'NONE',  ( 36.87297107704152666, -25.71368208888609885, 72.49904802271738902 ) ) ;
#12142=CARTESIAN_POINT ( 'NONE',  ( 39.02088643472237806, -0.7038408664219175659, 73.73360434286902887 ) ) ;
#12146=CARTESIAN_POINT ( 'NONE',  ( 37.25202387243752611, -7.213682088886102406, 70.00779233799264034 ) ) ;
#12148=CARTESIAN_POINT ( 'NONE',  ( 39.98359781491296161, -24.41368208888610525, 71.86517103874045631 ) ) ;
#12152=CARTESIAN_POINT ( 'NONE',  ( 39.98359781491296161, 0.7961591335780872081, 70.89533451361948835 ) ) ;
#12154=CARTESIAN_POINT ( 'NONE',  ( 38.26194895904384197, -26.60384086642191193, 72.51602215082114355 ) ) ;
#12155=CARTESIAN_POINT ( 'NONE',  ( 40.14115730948191185, -10.51368208888609956, 71.32335560751961623 ) ) ;
#12158=CARTESIAN_POINT ( 'NONE',  ( 36.49096545463212493, -12.10384086642191193, 71.32335560751961623 ) ) ;
#12160=CARTESIAN_POINT ( 'NONE',  ( 37.69796330110504101, -9.113682088886100985, 69.66206559358663242 ) ) ;
#12162=CARTESIAN_POINT ( 'NONE',  ( 36.36258059203031934, -15.71368208888610773, 72.86986841596736042 ) ) ;
#12166=CARTESIAN_POINT ( 'NONE',  ( 39.31564783533279694, -17.30384086642191477, 70.72433947564853440 ) ) ;
#12171=CARTESIAN_POINT ( 'NONE',  ( 36.98690846071097127, -23.80384086642191477, 69.45876917294174291 ) ) ;
#12173=CARTESIAN_POINT ( 'NONE',  ( 39.73277004305198545, 1.786317911113892043, 73.23812341099230139 ) ) ;
#12181=CARTESIAN_POINT ( 'NONE',  ( 39.95015449827720744, -23.00384086642191050, 71.96809898377887293 ) ) ;
#12186=CARTESIAN_POINT ( 'NONE',  ( 37.89291511884479036, -2.503840866421910505, 72.49843995877331793 ) ) ;
#12190=CARTESIAN_POINT ( 'NONE',  ( 38.93415946300897446, -28.11368208888610098, 73.09843995877328382 ) ) ;
#12195=CARTESIAN_POINT ( 'NONE',  ( 39.24876120206128860, -8.713682088886100630, 70.63227792289247020 ) ) ;
#12196=CARTESIAN_POINT ( 'NONE',  ( 38.37017380507020192, -2.013682088886102228, 72.51602215082118619 ) ) ;
#12202=CARTESIAN_POINT ( 'NONE',  ( 36.49096545463212493, -14.10384086642191015, 71.32335560751961623 ) ) ;
#12209=CARTESIAN_POINT ( 'NONE',  ( 40.14115730948191185, -4.513682088886104005, 71.32335560751961623 ) ) ;
#12213=CARTESIAN_POINT ( 'NONE',  ( 40.12624830571841983, -29.10876147765395672, 71.35553700530282129 ) ) ;
#12222=CARTESIAN_POINT ( 'NONE',  ( 36.36258059203030513, -5.903840866421909972, 69.89063713639259845 ) ) ;
#12225=CARTESIAN_POINT ( 'NONE',  ( 36.68196826583682935, -5.613682088886105426, 71.96809898377890136 ) ) ;
#12227=CARTESIAN_POINT ( 'NONE',  ( 36.29569395875879678, -17.31368208888610383, 69.98269868914867686 ) ) ;
#12241=CARTESIAN_POINT ( 'NONE',  ( 39.31564783533280405, -26.31368208888610027, 72.03616607671136762 ) ) ;
#12248=CARTESIAN_POINT ( 'NONE',  ( 39.12911128074872380, -23.50384086642191050, 69.06206559358665231 ) ) ;
#12249=CARTESIAN_POINT ( 'NONE',  ( 40.52078840805428683, 1.386317911113894130, 70.60699637195612866 ) ) ;
#12258=CARTESIAN_POINT ( 'NONE',  ( 40.33642880535521869, -5.303840866421911215, 69.98269868914867686 ) ) ;
#12262=CARTESIAN_POINT ( 'NONE',  ( 37.69796330110504101, -9.113682088886100985, 69.66206559358663242 ) ) ;
#12274=CARTESIAN_POINT ( 'NONE',  ( 39.02742774030101458, -27.40384086642191619, 70.49320253461758057 ) ) ;
#12275=CARTESIAN_POINT ( 'NONE',  ( 37.25202387243752611, -13.21368208888610063, 70.00779233799262613 ) ) ;
#12278=CARTESIAN_POINT ( 'NONE',  ( 36.64852494920107517, -14.20384086642191157, 71.86517103874048473 ) ) ;
#12281=CARTESIAN_POINT ( 'NONE',  ( 36.80608444377001121, -11.31368208888609672, 70.35351908239857721 ) ) ;
#12283=CARTESIAN_POINT ( 'NONE',  ( 39.12911128074873801, -14.11368208888610987, 73.69843995877327814 ) ) ;
#12287=CARTESIAN_POINT ( 'NONE',  ( 37.31647492878124694, -18.30384086642191122, 72.03616607671141026 ) ) ;
#12293=CARTESIAN_POINT ( 'NONE',  ( 35.86008812008917346, -22.10384086642191548, 71.32335560751961623 ) ) ;
#12296=CARTESIAN_POINT ( 'NONE',  ( 39.29254315202756231, -28.81368208888610383, 69.94417936956671156 ) ) ;
#12303=CARTESIAN_POINT ( 'NONE',  ( 36.80608444377002542, -14.30384086642191299, 72.40698646996133903 ) ) ;
#12309=CARTESIAN_POINT ( 'NONE',  ( 37.38336156205273397, 0.09615913357808798800, 70.63227792289248441 ) ) ;
#12313=CARTESIAN_POINT ( 'NONE',  ( 40.14115730948191185, -28.51368208888610667, 71.32335560751958781 ) ) ;
#12319=CARTESIAN_POINT ( 'NONE',  ( 37.31647492878122563, -5.313682088886097610, 70.72433947564853440 ) ) ;
#12322=CARTESIAN_POINT ( 'NONE',  ( 39.24876120206128860, -2.713682088886101962, 70.63227792289247020 ) ) ;
#12330=CARTESIAN_POINT ( 'NONE',  ( 36.80608444377001831, -10.30384086642191654, 72.40698646996136745 ) ) ;
#12338=CARTESIAN_POINT ( 'NONE',  ( 36.64852494920107517, -9.413682088886107024, 70.89533451361948835 ) ) ;
#12343=CARTESIAN_POINT ( 'NONE',  ( 36.64852494920107517, -23.41368208888610525, 70.89533451361945993 ) ) ;
#12344=CARTESIAN_POINT ( 'NONE',  ( 40.20492003450708296, -29.10876147765143074, 70.86866654954431510 ) ) ;
#12354=CARTESIAN_POINT ( 'NONE',  ( 36.89935272106205133, -2.403840866421917521, 73.23812341099225875 ) ) ;
#12360=CARTESIAN_POINT ( 'NONE',  ( 37.25202387243752611, -11.21368208888610241, 70.00779233799262613 ) ) ;
#12363=CARTESIAN_POINT ( 'NONE',  ( 37.61123632939165873, -17.91368208888610525, 73.73360434286898624 ) ) ;
#12374=CARTESIAN_POINT ( 'NONE',  ( 37.25260217561390874, -23.61368208888610098, 71.78268878715390144 ) ) ;
#12381=CARTESIAN_POINT ( 'NONE',  ( 36.98690846071097127, -25.80384086642191477, 69.45876917294174291 ) ) ;
#12382=CARTESIAN_POINT ( 'NONE',  ( 40.55423172469004811, 1.586317911113896306, 72.05058123536544201 ) ) ;
#12389=CARTESIAN_POINT ( 'NONE',  ( 35.86008812008917346, -2.103840866421915923, 71.32335560751961623 ) ) ;
#12392=CARTESIAN_POINT ( 'NONE',  ( 36.87297107704152666, -9.713682088886107735, 72.49904802271743165 ) ) ;
#12396=CARTESIAN_POINT ( 'NONE',  ( 36.68196826583682935, -27.61368208888610809, 71.96809898377887293 ) ) ;
#12400=CARTESIAN_POINT ( 'NONE',  ( 37.25260217561390874, -26.00384086642191406, 70.97781676520601479 ) ) ;
#12401=CARTESIAN_POINT ( 'NONE',  ( 36.80608444377001121, -13.31368208888609672, 70.35351908239857721 ) ) ;
#12404=CARTESIAN_POINT ( 'NONE',  ( 39.38009889167648936, -9.403840866421907307, 70.00779233799264034 ) ) ;
#12408=CARTESIAN_POINT ( 'NONE',  ( 38.26194895904383486, -5.013682088886102228, 69.64448340153879258 ) ) ;
#12410=CARTESIAN_POINT ( 'NONE',  ( 39.73277004305198545, -18.21368208888610596, 73.23812341099225875 ) ) ;
#12416=CARTESIAN_POINT ( 'NONE',  ( 38.00113996487112189, -15.70384086642191157, 70.22690120949090442 ) ) ;
#12423=CARTESIAN_POINT ( 'NONE',  ( 37.61123632939164452, -21.70384086642190979, 69.02690120949091579 ) ) ;
#12425=CARTESIAN_POINT ( 'NONE',  ( 39.64521430340304420, 1.186317911113898838, 69.45876917294178554 ) ) ;
#12434=CARTESIAN_POINT ( 'NONE',  ( 37.80618814713138676, -11.70384086642190802, 69.62690120949091011 ) ) ;
#12442=CARTESIAN_POINT ( 'NONE',  ( 39.98359781491296161, -29.20384086642191335, 70.89533451361944572 ) ) ;
#12445=CARTESIAN_POINT ( 'NONE',  ( 39.82603832034400426, -28.31368208888610027, 72.40698646996131060 ) ) ;
#12450=CARTESIAN_POINT ( 'NONE',  ( 37.60469502381300089, -5.213682088886100630, 70.49320253461759478 ) ) ;
#12451=CARTESIAN_POINT ( 'NONE',  ( 37.12184278917507640, -1.513682088886101784, 71.43714994484035685 ) ) ;
#12459=CARTESIAN_POINT ( 'NONE',  ( 39.38009889167648936, -9.403840866421907307, 70.00779233799264034 ) ) ;
#12468=CARTESIAN_POINT ( 'NONE',  ( 38.37017380507020192, -10.01368208888611022, 73.11602215082118050 ) ) ;
#12470=CARTESIAN_POINT ( 'NONE',  ( 39.72979056325730340, -29.10876147765396738, 70.86673335466467449 ) ) ;
#12483=CARTESIAN_POINT ( 'NONE',  ( 39.64521430340304420, -28.81368208888610383, 69.45876917294174291 ) ) ;
#12484=CARTESIAN_POINT ( 'NONE',  ( 39.37952058850012804, -26.61368208888610809, 70.97781676520600058 ) ) ;
#12489=CARTESIAN_POINT ( 'NONE',  ( 39.38009889167650357, -10.21368208888610773, 72.75271321436733274 ) ) ;
#12490=CARTESIAN_POINT ( 'NONE',  ( 37.21915885897815457, -2.203840866421911571, 71.67976084211552745 ) ) ;
#12493=CARTESIAN_POINT ( 'NONE',  ( 38.26194895904383486, -7.013682088886100452, 69.04448340153881247 ) ) ;
#12513=CARTESIAN_POINT ( 'NONE',  ( 37.61123632939164452, -19.70384086642190979, 69.02690120949091579 ) ) ;
#12515=CARTESIAN_POINT ( 'NONE',  ( 39.29254315202756231, -26.81368208888610027, 69.94417936956671156 ) ) ;
#12523=CARTESIAN_POINT ( 'NONE',  ( 37.61123632939165873, -25.91368208888610880, 73.73360434286898624 ) ) ;
#12527=CARTESIAN_POINT ( 'NONE',  ( 39.29254315202756231, -10.81368208888610205, 69.94417936956673998 ) ) ;
#12529=CARTESIAN_POINT ( 'NONE',  ( 39.82603832034401847, -18.31368208888610738, 72.40698646996131060 ) ) ;
#12534=CARTESIAN_POINT ( 'NONE',  ( 37.89291511884479036, -22.50384086642191050, 72.49843995877330372 ) ) ;
#12535=CARTESIAN_POINT ( 'NONE',  ( 38.26194895904383486, -13.01368208888610134, 69.64448340153877837 ) ) ;
#12538=CARTESIAN_POINT ( 'NONE',  ( 38.93415946300896024, -11.50384086642190340, 69.66206559358663242 ) ) ;
#12542=CARTESIAN_POINT ( 'NONE',  ( 39.29254315202756231, -2.813682088886101162, 69.94417936956673998 ) ) ;
#12544=CARTESIAN_POINT ( 'NONE',  ( 36.36258059203031934, -13.71368208888610773, 72.86986841596736042 ) ) ;
#12548=CARTESIAN_POINT ( 'NONE',  ( 39.31564783533279694, -9.303840866421909439, 70.72433947564853440 ) ) ;
#12554=CARTESIAN_POINT ( 'NONE',  ( 36.98690846071097127, -25.80384086642191477, 69.45876917294174291 ) ) ;
#12556=CARTESIAN_POINT ( 'NONE',  ( 37.25202387243752611, -27.21368208888610241, 70.00779233799262613 ) ) ;
#12565=CARTESIAN_POINT ( 'NONE',  ( 39.82603832034401137, -17.30384086642190411, 70.35351908239857721 ) ) ;
#12571=CARTESIAN_POINT ( 'NONE',  ( 36.68196826583682935, -28.00384086642191050, 70.79240656858105751 ) ) ;
#12575=CARTESIAN_POINT ( 'NONE',  ( 39.82603832034400426, -24.31368208888611093, 72.40698646996131060 ) ) ;
#12581=CARTESIAN_POINT ( 'NONE',  ( 39.02742774030102879, -4.213682088886099741, 72.26730301774236409 ) ) ;
#12582=CARTESIAN_POINT ( 'NONE',  ( 39.37952058850012804, 1.386317911113897683, 70.97781676520604321 ) ) ;
#12588=CARTESIAN_POINT ( 'NONE',  ( 36.68196826583682935, -12.00384086642191228, 70.79240656858107172 ) ) ;
#12595=CARTESIAN_POINT ( 'NONE',  ( 39.82603832034401847, -10.31368208888610560, 72.40698646996133903 ) ) ;
#12608=CARTESIAN_POINT ( 'NONE',  ( 40.77203464402485622, -1.103840866421915035, 71.43714994484034264 ) ) ;
#12609=CARTESIAN_POINT ( 'NONE',  ( 38.26194895904383486, -27.01368208888609956, 70.24448340153875847 ) ) ;
#12613=CARTESIAN_POINT ( 'NONE',  ( 36.49096545463212493, -3.513682088886103116, 71.43714994484035685 ) ) ;
#12614=CARTESIAN_POINT ( 'NONE',  ( 39.24876120206129571, 1.096159133578088696, 72.12822762946751709 ) ) ;
#12617=CARTESIAN_POINT ( 'NONE',  ( 38.26194895904383486, -11.01368208888609956, 69.04448340153881247 ) ) ;
#12630=CARTESIAN_POINT ( 'NONE',  ( 39.12911128074872380, -19.50384086642191406, 69.06206559358665231 ) ) ;
#12631=CARTESIAN_POINT ( 'NONE',  ( 37.80618814713140097, -21.91368208888610880, 73.13360434286903455 ) ) ;
#12639=CARTESIAN_POINT ( 'NONE',  ( 38.26194895904384907, 1.396159133578083633, 73.11602215082119471 ) ) ;
#12640=CARTESIAN_POINT ( 'NONE',  ( 36.29569395875881099, -0.3038408664219164890, 72.77780686321129622 ) ) ;
#12647=CARTESIAN_POINT ( 'NONE',  ( 36.64852494920107517, -1.413682088886102806, 70.89533451361948835 ) ) ;
#12649=CARTESIAN_POINT ( 'NONE',  ( 38.82593461698262871, -18.91368208888609814, 69.62690120949091011 ) ) ;
#12653=CARTESIAN_POINT ( 'NONE',  ( 39.02742774030101458, -21.40384086642191619, 70.49320253461759478 ) ) ;
#12654=CARTESIAN_POINT ( 'NONE',  ( 38.26194895904383486, -5.013682088886102228, 69.64448340153879258 ) ) ;
#12657=CARTESIAN_POINT ( 'NONE',  ( 37.69796330110505522, -6.503840866421914058, 73.09843995877331224 ) ) ;
#12661=CARTESIAN_POINT ( 'NONE',  ( 36.49096545463212493, -7.513682088886102228, 71.43714994484035685 ) ) ;
#12663=CARTESIAN_POINT ( 'NONE',  ( 39.02088643472237095, -10.91368208888610170, 69.02690120949094421 ) ) ;
#12667=CARTESIAN_POINT ( 'NONE',  ( 38.26194895904384197, -12.60384086642191015, 72.51602215082118619 ) ) ;
#12672=CARTESIAN_POINT ( 'NONE',  ( 38.37017380507018771, -17.60384086642191193, 69.04448340153878405 ) ) ;
#12675=CARTESIAN_POINT ( 'NONE',  ( 39.95015449827720744, -20.61368208888610454, 70.79240656858105751 ) ) ;
#12684=CARTESIAN_POINT ( 'NONE',  ( 39.98359781491296161, -17.20384086642190979, 70.89533451361945993 ) ) ;
#12690=CARTESIAN_POINT ( 'NONE',  ( 37.25202387243754032, -26.40384086642191619, 72.75271321436730432 ) ) ;
#12693=CARTESIAN_POINT ( 'NONE',  ( 39.98359781491296161, -26.41368208888610525, 71.86517103874045631 ) ) ;
#12699=CARTESIAN_POINT ( 'NONE',  ( 37.25260217561390874, -28.00384086642191406, 70.97781676520601479 ) ) ;
#12701=CARTESIAN_POINT ( 'NONE',  ( 37.60469502381300089, 0.7863179111138978161, 70.49320253461759478 ) ) ;
#12707=CARTESIAN_POINT ( 'NONE',  ( 39.75915168707251723, -4.903840866421914413, 72.49904802271740323 ) ) ;
#12713=CARTESIAN_POINT ( 'NONE',  ( 36.68196826583682935, -1.613682088886104982, 71.96809898377890136 ) ) ;
#12731=CARTESIAN_POINT ( 'NONE',  ( 39.31564783533280405, -20.31368208888610027, 72.03616607671141026 ) ) ;
#12735=CARTESIAN_POINT ( 'NONE',  ( 39.75915168707250302, -4.713682088886100630, 70.26145752964252722 ) ) ;
#12736=CARTESIAN_POINT ( 'NONE',  ( 36.64852494920107517, -28.20384086642191335, 71.86517103874047052 ) ) ;
#12742=CARTESIAN_POINT ( 'NONE',  ( 40.77203464402485622, -6.513682088886103116, 71.32335560751961623 ) ) ;
#12760=CARTESIAN_POINT ( 'NONE',  ( 36.29569395875881099, -18.30384086642191477, 72.77780686321128201 ) ) ;
#12762=CARTESIAN_POINT ( 'NONE',  ( 37.33957961208646736, -19.81368208888611093, 72.81632618279321889 ) ) ;
#12766=DIRECTION ( 'NONE',  ( 0.000000000000000000, 0.000000000000000000, 1.000000000000000000 ) ) ;
#12770=CARTESIAN_POINT ( 'NONE',  ( 36.98690846071097837, -27.81368208888610738, 73.30173637941817333 ) ) ;
#12774=CARTESIAN_POINT ( 'NONE',  ( 37.33957961208646736, -3.813682088886109156, 72.81632618279323310 ) ) ;
#12776=CARTESIAN_POINT ( 'NONE',  ( 36.49096545463212493, -17.51368208888610667, 71.43714994484034264 ) ) ;
#12781=CARTESIAN_POINT ( 'NONE',  ( 38.73920764526923932, -17.50384086642191406, 70.26206559358661252 ) ) ;
#12782=CARTESIAN_POINT ( 'NONE',  ( 40.14115730948191185, -6.513682088886103116, 71.32335560751961623 ) ) ;
#12785=CARTESIAN_POINT ( 'NONE',  ( 39.29254315202757653, -2.803840866421915212, 72.81632618279323310 ) ) ;
#12787=CARTESIAN_POINT ( 'NONE',  ( 38.82593461698262871, -6.913682088886100807, 69.62690120949091011 ) ) ;
#12789=CARTESIAN_POINT ( 'NONE',  ( 36.29569395875879678, -9.313682088886098498, 69.98269868914869107 ) ) ;
#12792=CARTESIAN_POINT ( 'NONE',  ( 39.24876120206129571, -10.90384086642191264, 72.12822762946750288 ) ) ;
#12798=CARTESIAN_POINT ( 'NONE',  ( 40.33642880535521869, -17.30384086642191477, 69.98269868914866265 ) ) ;
#12800=CARTESIAN_POINT ( 'NONE',  ( 40.14115730948191185, -22.51368208888609956, 71.32335560751960202 ) ) ;
#12806=CARTESIAN_POINT ( 'NONE',  ( 38.82593461698264292, -12.70384086642191512, 73.13360434286903455 ) ) ;
#12810=CARTESIAN_POINT ( 'NONE',  ( 39.82603832034400426, -26.31368208888611093, 72.40698646996131060 ) ) ;
#12815=CARTESIAN_POINT ( 'NONE',  ( 37.69796330110505522, -24.50384086642190695, 73.09843995877328382 ) ) ;
#12817=CARTESIAN_POINT ( 'NONE',  ( 37.33957961208646736, -21.81368208888610738, 72.81632618279321889 ) ) ;
#12822=CARTESIAN_POINT ( 'NONE',  ( 37.21915885897815457, 0.5863179111138989708, 71.08074471024443142 ) ) ;
#12823=CARTESIAN_POINT ( 'NONE',  ( 38.00113996487114321, 0.08631791111389855442, 72.53360434286905445 ) ) ;
#12831=CARTESIAN_POINT ( 'NONE',  ( 36.64852494920107517, -6.203840866421912459, 71.86517103874049894 ) ) ;
#12838=CARTESIAN_POINT ( 'NONE',  ( 36.64852494920107517, 0.5863179111138955291, 70.89533451361948835 ) ) ;
#12851=CARTESIAN_POINT ( 'NONE',  ( 37.21915885897815457, -15.41368208888610347, 71.08074471024443142 ) ) ;
#12857=CARTESIAN_POINT ( 'NONE',  ( 39.29254315202756231, -4.813682088886099386, 69.94417936956673998 ) ) ;
#12858=CARTESIAN_POINT ( 'NONE',  ( 38.82593461698265003, -22.70384086642191690, 73.13360434286903455 ) ) ;
#12860=CARTESIAN_POINT ( 'NONE',  ( 38.37017380507020192, -10.01368208888611022, 73.71602215082116061 ) ) ;
#12882=CARTESIAN_POINT ( 'NONE',  ( 36.07789103942399578, -16.20384086642191690, 72.05058123536544201 ) ) ;
#12885=CARTESIAN_POINT ( 'NONE',  ( 38.37017380507020192, -22.01368208888611022, 73.11602215082116629 ) ) ;
#12893=CARTESIAN_POINT ( 'NONE',  ( 39.64521430340304420, -26.81368208888610738, 69.45876917294174291 ) ) ;
#12897=CARTESIAN_POINT ( 'NONE',  ( 36.49096545463212493, 0.4863179111138959954, 71.43714994484035685 ) ) ;
#12900=CARTESIAN_POINT ( 'NONE',  ( 36.49096545463212493, -23.51368208888609956, 71.43714994484031422 ) ) ;
#12904=CARTESIAN_POINT ( 'NONE',  ( 37.12184278917507640, -22.10384086642191193, 71.32335560751961623 ) ) ;
#12905=CARTESIAN_POINT ( 'NONE',  ( 36.80608444377001121, -5.313682088886100274, 70.35351908239860563 ) ) ;
#12911=CARTESIAN_POINT ( 'NONE',  ( 36.49096545463212493, -6.103840866421912814, 71.32335560751963044 ) ) ;
#12914=CARTESIAN_POINT ( 'NONE',  ( 39.75915168707250302, -4.713682088886100630, 70.26145752964252722 ) ) ;
#12916=CARTESIAN_POINT ( 'NONE',  ( 36.11133435605973574, -11.61368208888610454, 72.15350918040385864 ) ) ;
#12919=CARTESIAN_POINT ( 'NONE',  ( 37.25260217561390874, -12.00384086642191228, 70.97781676520601479 ) ) ;
#12924=CARTESIAN_POINT ( 'NONE',  ( 40.33642880535521869, -13.30384086642190944, 69.98269868914866265 ) ) ;
#12927=CARTESIAN_POINT ( 'NONE',  ( 36.80608444377001121, -21.31368208888610027, 70.35351908239857721 ) ) ;
#12935=CARTESIAN_POINT ( 'NONE',  ( 38.26194895904384907, -8.603840866421915479, 73.11602215082118050 ) ) ;
#12938=CARTESIAN_POINT ( 'NONE',  ( 39.75915168707250302, -24.71368208888610241, 70.26145752964249880 ) ) ;
#12942=CARTESIAN_POINT ( 'NONE',  ( 36.80608444377001831, -24.30384086642191832, 72.40698646996133903 ) ) ;
#12945=CARTESIAN_POINT ( 'NONE',  ( 36.87297107704152666, -27.71368208888610241, 72.49904802271738902 ) ) ;
#12950=CARTESIAN_POINT ( 'NONE',  ( 37.69225076346193504, 0.1863179111138979493, 72.33091598616827866 ) ) ;
#12951=CARTESIAN_POINT ( 'NONE',  ( 37.89291511884476904, -1.113682088886101207, 70.26206559358664094 ) ) ;
#12953=VERTEX_POINT ( 'NONE', #17017 ) ;
#12958=CARTESIAN_POINT ( 'NONE',  ( 39.98359781491296161, -3.203840866421912903, 70.89533451361947414 ) ) ;
#12968=CARTESIAN_POINT ( 'NONE',  ( 36.49096545463212493, -1.513682088886105559, 71.43714994484035685 ) ) ;
#12985=CARTESIAN_POINT ( 'NONE',  ( 38.37017380507020192, -18.01368208888610312, 72.51602215082118619 ) ) ;
#12989=CARTESIAN_POINT ( 'NONE',  ( 36.80608444377001121, 0.6863179111138983934, 70.35351908239860563 ) ) ;
#12990=CARTESIAN_POINT ( 'NONE',  ( 39.75915168707251723, -22.90384086642190908, 72.49904802271738902 ) ) ;
#12992=CARTESIAN_POINT ( 'NONE',  ( 36.07789103942398867, -7.413682088886105248, 70.70992431699450265 ) ) ;
#13007=CARTESIAN_POINT ( 'NONE',  ( 40.55423172469004101, -17.20384086642191335, 70.70992431699450265 ) ) ;
#13008=CARTESIAN_POINT ( 'NONE',  ( 36.87297107704152666, -19.71368208888610951, 72.49904802271740323 ) ) ;
#13014=CARTESIAN_POINT ( 'NONE',  ( 39.64521430340304420, -28.81368208888610383, 69.45876917294174291 ) ) ;
#13018=CARTESIAN_POINT ( 'NONE',  ( 39.38009889167650357, -4.213682088886106847, 72.75271321436733274 ) ) ;
#13021=CARTESIAN_POINT ( 'NONE',  ( 36.49096545463212493, -19.51368208888610312, 71.43714994484034264 ) ) ;
#13025=CARTESIAN_POINT ( 'NONE',  ( 37.25260217561390874, -20.00384086642191406, 70.97781676520601479 ) ) ;
#13026=CARTESIAN_POINT ( 'NONE',  ( 38.26194895904383486, -3.013682088886100008, 69.64448340153879258 ) ) ;
#13030=CARTESIAN_POINT ( 'NONE',  ( 39.38009889167648936, -5.403840866421906419, 70.00779233799264034 ) ) ;
#13032=CARTESIAN_POINT ( 'NONE',  ( 36.64852494920107517, 0.5863179111138955291, 70.89533451361948835 ) ) ;
#13034=CARTESIAN_POINT ( 'NONE',  ( 40.55423172469004811, -8.413682088886105248, 72.05058123536544201 ) ) ;
#13037=CARTESIAN_POINT ( 'NONE',  ( 38.37017380507018771, -11.60384086642191015, 70.24448340153877268 ) ) ;
#13044=CARTESIAN_POINT ( 'NONE',  ( 37.50301148336529877, -18.50384086642192116, 73.69843995877327814 ) ) ;
#13049=( NAMED_UNIT ( * ) PLANE_ANGLE_UNIT ( ) SI_UNIT ( $, .RADIAN. ) );
#13050=CARTESIAN_POINT ( 'NONE',  ( 36.49096545463212493, -21.51368208888609956, 71.43714994484034264 ) ) ;
#13057=CARTESIAN_POINT ( 'NONE',  ( 37.69796330110505522, -8.503840866421915834, 73.09843995877331224 ) ) ;
#13062=CARTESIAN_POINT ( 'NONE',  ( 36.80608444377001121, -27.31368208888610383, 70.35351908239857721 ) ) ;
#13064=AXIS2_PLACEMENT_3D ( 'NONE', #16927, #18857, #20404 ) ;
#13066=CARTESIAN_POINT ( 'NONE',  ( 36.87297107704149823, -21.90384086642189843, 70.26145752964252722 ) ) ;
#13068=CARTESIAN_POINT ( 'NONE',  ( 36.87297107704152666, -25.71368208888609885, 72.49904802271738902 ) ) ;
#13070=CARTESIAN_POINT ( 'NONE',  ( 38.26194895904384197, 1.396159133578080080, 73.71602215082117482 ) ) ;
#13074=CARTESIAN_POINT ( 'NONE',  ( 38.73920764526925353, -2.113682088886101873, 72.49843995877331793 ) ) ;
#13080=CARTESIAN_POINT ( 'NONE',  ( 38.26194895904384907, -6.603840866421916367, 73.11602215082118050 ) ) ;
#13089=CARTESIAN_POINT ( 'NONE',  ( 40.14115730948191185, -2.513682088886103116, 71.32335560751961623 ) ) ;
#13090=CARTESIAN_POINT ( 'NONE',  ( 39.29254315202757653, -26.80384086642191477, 72.81632618279320468 ) ) ;
#13111=CARTESIAN_POINT ( 'NONE',  ( 38.00113996487114321, -19.91368208888610170, 72.53360434286904024 ) ) ;
#13116=CARTESIAN_POINT ( 'NONE',  ( 38.82593461698265003, -24.70384086642191690, 73.13360434286902034 ) ) ;
#13118=CARTESIAN_POINT ( 'NONE',  ( 40.55423172469004811, -4.413682088886105248, 72.05058123536544201 ) ) ;
#13127=( GEOMETRIC_REPRESENTATION_CONTEXT ( 3 ) GLOBAL_UNCERTAINTY_ASSIGNED_CONTEXT ( ( #8446 ) ) GLOBAL_UNIT_ASSIGNED_CONTEXT ( ( #22278, #2687, #18549 ) ) REPRESENTATION_CONTEXT ( 'NONE', 'WORKASPACE' ) );
#13135=CARTESIAN_POINT ( 'NONE',  ( 39.64521430340305841, -12.80384086642191832, 73.30173637941818754 ) ) ;
#13138=CARTESIAN_POINT ( 'NONE',  ( 38.26194895904383486, -21.01368208888610312, 69.64448340153877837 ) ) ;
#13144=CARTESIAN_POINT ( 'NONE',  ( 40.26954217208371034, -20.71368208888610596, 69.89063713639258424 ) ) ;
#13148=CARTESIAN_POINT ( 'NONE',  ( 40.14115730948191185, -0.5136820888861047818, 71.32335560751961623 ) ) ;
#13150=CARTESIAN_POINT ( 'NONE',  ( 39.75915168707250302, -14.71368208888610063, 70.26145752964252722 ) ) ;
#13155=CARTESIAN_POINT ( 'NONE',  ( 39.24876120206129571, -16.90384086642190553, 72.12822762946747446 ) ) ;
#13156=CARTESIAN_POINT ( 'NONE',  ( 39.38009889167650357, -8.213682088886105959, 72.75271321436733274 ) ) ;
#13162=CARTESIAN_POINT ( 'NONE',  ( 39.29254315202757653, -4.803840866421913880, 72.81632618279323310 ) ) ;
#13164=CARTESIAN_POINT ( 'NONE',  ( 38.37017380507020192, -2.013682088886109334, 73.11602215082118050 ) ) ;
#13166=CARTESIAN_POINT ( 'NONE',  ( 37.50301148336529167, -7.113682088886103649, 69.06206559358666652 ) ) ;
#13169=CARTESIAN_POINT ( 'NONE',  ( 37.12184278917507640, -8.103840866421910150, 71.32335560751961623 ) ) ;
#13176=CARTESIAN_POINT ( 'NONE',  ( 38.26194895904384197, -16.60384086642191548, 73.71602215082113219 ) ) ;
#13179=CARTESIAN_POINT ( 'NONE',  ( 39.98359781491296161, -22.41368208888610525, 71.86517103874047052 ) ) ;
#13187=CARTESIAN_POINT ( 'NONE',  ( 36.80608444377002542, -6.303840866421914768, 72.40698646996135324 ) ) ;
#13190=CARTESIAN_POINT ( 'NONE',  ( 36.49096545463212493, -23.51368208888609601, 71.43714994484030001 ) ) ;
#13195=CARTESIAN_POINT ( 'NONE',  ( 39.38009889167648936, -23.40384086642190908, 70.00779233799262613 ) ) ;
#13198=CARTESIAN_POINT ( 'NONE',  ( 37.69796330110504101, -17.11368208888610098, 69.66206559358661821 ) ) ;
#13200=CARTESIAN_POINT ( 'NONE',  ( 40.55423172469004101, 0.7961591335780838774, 70.70992431699450265 ) ) ;
#13205=CARTESIAN_POINT ( 'NONE',  ( 37.60469502381300799, -24.40384086642190908, 72.26730301774232146 ) ) ;
#13213=CARTESIAN_POINT ( 'NONE',  ( 38.26194895904384907, -2.603840866421916367, 73.11602215082118050 ) ) ;
#13222=CARTESIAN_POINT ( 'NONE',  ( 39.82603832034401847, -0.3136820888861094336, 72.40698646996133903 ) ) ;
#13224=CARTESIAN_POINT ( 'NONE',  ( 39.95015449827720744, -27.00384086642191050, 71.96809898377885872 ) ) ;
#13239=CARTESIAN_POINT ( 'NONE',  ( 38.93987200065208754, -16.81368208888610383, 70.42958956619168021 ) ) ;
#13244=CARTESIAN_POINT ( 'NONE',  ( 40.14115730948191185, 1.486317911113896884, 71.32335560751963044 ) ) ;
#13245=CARTESIAN_POINT ( 'NONE',  ( 39.38009889167648936, -23.40384086642190908, 70.00779233799262613 ) ) ;
#13263=CARTESIAN_POINT ( 'NONE',  ( 36.89935272106205133, -10.40384086642191797, 73.23812341099225875 ) ) ;
#13265=CARTESIAN_POINT ( 'NONE',  ( 39.29254315202756231, -12.81368208888610383, 69.94417936956672577 ) ) ;
#13269=CARTESIAN_POINT ( 'NONE',  ( 36.11133435605973574, -23.61368208888610098, 72.15350918040381600 ) ) ;
#13283=CARTESIAN_POINT ( 'NONE',  ( 39.02742774030101458, -15.40384086642191441, 70.49320253461759478 ) ) ;
#13284=CARTESIAN_POINT ( 'NONE',  ( 36.68196826583682935, 0.3863179111138967392, 71.96809898377890136 ) ) ;
#13292=CARTESIAN_POINT ( 'NONE',  ( 40.52078840805429394, -29.00384086642191406, 72.15350918040381600 ) ) ;
#13294=CARTESIAN_POINT ( 'NONE',  ( 37.38336156205274818, -27.71368208888610241, 72.12822762946747446 ) ) ;
#13295=CARTESIAN_POINT ( 'NONE',  ( 36.29569395875879678, -3.313682088886101607, 69.98269868914869107 ) ) ;
#13298=CARTESIAN_POINT ( 'NONE',  ( 39.41296390513587511, -5.203840866421910683, 71.08074471024443142 ) ) ;
#13304=CARTESIAN_POINT ( 'NONE',  ( 36.29569395875881099, -8.303840866421920097, 72.77780686321129622 ) ) ;
#13307=CARTESIAN_POINT ( 'NONE',  ( 39.75915168707250302, -14.71368208888610063, 70.26145752964251301 ) ) ;
#13314=CARTESIAN_POINT ( 'NONE',  ( 39.75915168707251723, -6.903840866421914413, 72.49904802271740323 ) ) ;
#13317=CARTESIAN_POINT ( 'NONE',  ( 39.75915168707250302, -16.71368208888609885, 70.26145752964251301 ) ) ;
#13321=CARTESIAN_POINT ( 'NONE',  ( 37.80618814713138676, -19.70384086642190624, 69.62690120949091011 ) ) ;
#13324=CARTESIAN_POINT ( 'NONE',  ( 37.69796330110504101, -21.11368208888610454, 69.66206559358661821 ) ) ;
#13326=CARTESIAN_POINT ( 'NONE',  ( 39.12911128074873801, -28.11368208888610809, 73.69843995877326392 ) ) ;
#13331=CARTESIAN_POINT ( 'NONE',  ( 38.73920764526923932, -25.50384086642191406, 70.26206559358661252 ) ) ;
#13338=CARTESIAN_POINT ( 'NONE',  ( 39.73277004305197124, -27.40384086642191619, 69.52238214136765748 ) ) ;
#13363=CARTESIAN_POINT ( 'NONE',  ( 37.31647492878122563, -9.313682088886098498, 70.72433947564853440 ) ) ;
#13365=CARTESIAN_POINT ( 'NONE',  ( 37.21915885897815457, -9.413682088886103472, 71.08074471024443142 ) ) ;
#13371=CARTESIAN_POINT ( 'NONE',  ( 37.33957961208645315, -25.80384086642190766, 69.94417936956671156 ) ) ;
#13375=CARTESIAN_POINT ( 'NONE',  ( 37.31647492878122563, -19.31368208888610027, 70.72433947564853440 ) ) ;
#13392=CARTESIAN_POINT ( 'NONE',  ( 40.77203464402485622, -9.103840866421915479, 71.43714994484034264 ) ) ;
#13395=CARTESIAN_POINT ( 'NONE',  ( 38.37017380507020192, -16.01368208888610667, 73.11602215082116629 ) ) ;
#13399=CARTESIAN_POINT ( 'NONE',  ( 39.02088643472237095, -20.91368208888609814, 69.02690120949091579 ) ) ;
#13405=CARTESIAN_POINT ( 'NONE',  ( 39.31564783533279694, -13.30384086642190944, 70.72433947564853440 ) ) ;
#13406=CARTESIAN_POINT ( 'NONE',  ( 37.33957961208646736, -1.813682088886107380, 72.81632618279323310 ) ) ;
#13413=CARTESIAN_POINT ( 'NONE',  ( 40.77203464402485622, -29.10384086642191193, 71.43714994484031422 ) ) ;
#13414=CARTESIAN_POINT ( 'NONE',  ( 36.87297107704152666, -1.713682088886108179, 72.49904802271743165 ) ) ;
#13416=CARTESIAN_POINT ( 'NONE',  ( 39.12911128074873801, -2.113682088886108534, 73.69843995877330656 ) ) ;
#13419=CARTESIAN_POINT ( 'NONE',  ( 37.12184278917507640, -4.103840866421911038, 71.32335560751961623 ) ) ;
#13424=CARTESIAN_POINT ( 'NONE',  ( 40.33642880535521869, -9.303840866421909439, 69.98269868914867686 ) ) ;
#13427=CARTESIAN_POINT ( 'NONE',  ( 36.64852494920107517, -13.41368208888610525, 70.89533451361947414 ) ) ;
#13433=CARTESIAN_POINT ( 'NONE',  ( 37.69796330110505522, -10.50384086642191228, 73.09843995877331224 ) ) ;
#13436=CARTESIAN_POINT ( 'NONE',  ( 38.26194895904383486, -19.01368208888610312, 69.64448340153877837 ) ) ;
#13438=CARTESIAN_POINT ( 'NONE',  ( 38.37017380507018771, -15.60384086642190837, 69.64448340153877837 ) ) ;
#13441=CARTESIAN_POINT ( 'NONE',  ( 36.64852494920107517, -15.41368208888610525, 70.89533451361947414 ) ) ;
#13443=CARTESIAN_POINT ( 'NONE',  ( 36.89935272106204422, -25.21368208888610241, 69.52238214136765748 ) ) ;
#13447=CARTESIAN_POINT ( 'NONE',  ( 37.31647492878124694, -26.30384086642190766, 72.03616607671141026 ) ) ;
#13453=CARTESIAN_POINT ( 'NONE',  ( 39.98359781491296161, 0.7961591335780872081, 70.89533451361948835 ) ) ;
#13464=CARTESIAN_POINT ( 'NONE',  ( 40.05245289102395390, -29.10876147765230115, 71.40796565871902146 ) ) ;
#13471=CARTESIAN_POINT ( 'NONE',  ( 38.63098279924290068, -8.703840866421911571, 72.53360434286905445 ) ) ;
#13478=CARTESIAN_POINT ( 'NONE',  ( 39.41296390513587511, -14.41368208888610347, 71.67976084211551324 ) ) ;
#13481=CARTESIAN_POINT ( 'NONE',  ( 37.60469502381300089, -11.21368208888610241, 70.49320253461759478 ) ) ;
#13488=CARTESIAN_POINT ( 'NONE',  ( 39.75915168707251723, -18.90384086642190553, 72.49904802271738902 ) ) ;
#13491=CARTESIAN_POINT ( 'NONE',  ( 37.38336156205274818, -19.71368208888610596, 72.12822762946750288 ) ) ;
#13509=CARTESIAN_POINT ( 'NONE',  ( 40.55423172469004101, -9.203840866421915123, 70.70992431699450265 ) ) ;
#13513=CARTESIAN_POINT ( 'NONE',  ( 39.38009889167650357, -14.21368208888610773, 72.75271321436731853 ) ) ;
#13520=CARTESIAN_POINT ( 'NONE',  ( 38.37017380507020192, -24.01368208888611022, 73.71602215082113219 ) ) ;
#13528=CARTESIAN_POINT ( 'NONE',  ( 37.69225076346193504, -9.803840866421911215, 70.42958956619168021 ) ) ;
#13529=CARTESIAN_POINT ( 'NONE',  ( 39.02742774030102879, -28.21368208888610596, 72.26730301774232146 ) ) ;
#13536=CARTESIAN_POINT ( 'NONE',  ( 40.52078840805429394, -27.00384086642191761, 72.15350918040381600 ) ) ;
#13538=CARTESIAN_POINT ( 'NONE',  ( 39.51027997493896748, -28.51368208888610667, 71.32335560751960202 ) ) ;
#13539=CARTESIAN_POINT ( 'NONE',  ( 40.26954217208371034, -0.7136820888861000745, 69.89063713639259845 ) ) ;
#13542=CARTESIAN_POINT ( 'NONE',  ( 38.26194895904384197, -6.603840866421913702, 72.51602215082118619 ) ) ;
#13548=CARTESIAN_POINT ( 'NONE',  ( 40.77203464402485622, -13.10384086642191548, 71.43714994484032843 ) ) ;
#13552=CARTESIAN_POINT ( 'NONE',  ( 38.93415946300897446, -16.11368208888611164, 73.09843995877329803 ) ) ;
#13558=CARTESIAN_POINT ( 'NONE',  ( 38.26194895904384907, -0.6038408664219147015, 73.11602215082118050 ) ) ;
#13563=CARTESIAN_POINT ( 'NONE',  ( 37.25202387243752611, -17.21368208888610241, 70.00779233799262613 ) ) ;
#13566=CARTESIAN_POINT ( 'NONE',  ( 36.87297107704149823, -19.90384086642190198, 70.26145752964252722 ) ) ;
#13569=CARTESIAN_POINT ( 'NONE',  ( 38.93415946300897446, -18.11368208888611164, 73.09843995877329803 ) ) ;
#13570=ORIENTED_EDGE ( 'NONE', *, *, #11243, .T. ) ;
#13571=CARTESIAN_POINT ( 'NONE',  ( 37.61123632939165873, -19.91368208888610880, 73.73360434286898624 ) ) ;
#13575=CARTESIAN_POINT ( 'NONE',  ( 37.25260217561390874, -26.00384086642191406, 70.97781676520601479 ) ) ;
#13579=CARTESIAN_POINT ( 'NONE',  ( 39.63762123564960405, -28.98311505855621206, 70.81515399290854873 ) ) ;
#13582=CARTESIAN_POINT ( 'NONE',  ( 39.64521430340305841, -28.80384086642192187, 73.30173637941817333 ) ) ;
#13585=CARTESIAN_POINT ( 'NONE',  ( 37.61123632939165873, -3.913682088886108357, 73.73360434286902887 ) ) ;
#13596=CARTESIAN_POINT ( 'NONE',  ( 39.38009889167648936, -23.40384086642190908, 70.00779233799262613 ) ) ;
#13604=CARTESIAN_POINT ( 'NONE',  ( 39.24876120206129571, -8.903840866421910860, 72.12822762946750288 ) ) ;
#13611=CARTESIAN_POINT ( 'NONE',  ( 38.73920764526925353, -12.11368208888610098, 72.49843995877330372 ) ) ;
#13612=CARTESIAN_POINT ( 'NONE',  ( 37.38336156205274818, -13.71368208888610241, 72.12822762946750288 ) ) ;
#13618=CARTESIAN_POINT ( 'NONE',  ( 38.37017380507018771, -19.60384086642191193, 69.64448340153877837 ) ) ;
#13621=CARTESIAN_POINT ( 'NONE',  ( 37.12184278917507640, -17.51368208888609956, 71.43714994484034264 ) ) ;
#13625=CARTESIAN_POINT ( 'NONE',  ( 39.38009889167650357, -16.21368208888610596, 72.75271321436731853 ) ) ;
#13638=CARTESIAN_POINT ( 'NONE',  ( 40.52078840805429394, -11.00384086642191406, 72.15350918040385864 ) ) ;
#13641=CARTESIAN_POINT ( 'NONE',  ( 36.49096545463212493, -17.51368208888610667, 71.43714994484034264 ) ) ;
#13645=CARTESIAN_POINT ( 'NONE',  ( 39.02088643472237095, -18.91368208888609814, 69.02690120949091579 ) ) ;
#13658=CARTESIAN_POINT ( 'NONE',  ( 38.37017380507018771, -13.60384086642191193, 70.24448340153875847 ) ) ;
#13659=CARTESIAN_POINT ( 'NONE',  ( 38.73920764526925353, -28.11368208888610454, 72.49843995877328950 ) ) ;
#13665=CARTESIAN_POINT ( 'NONE',  ( 39.98359781491296161, -1.203840866421911127, 70.89533451361947414 ) ) ;
#13666=CARTESIAN_POINT ( 'NONE',  ( 38.37017380507020192, -24.01368208888609956, 72.51602215082114355 ) ) ;
#13667=CARTESIAN_POINT ( 'NONE',  ( 39.12911128074873801, -6.113682088886108978, 73.69843995877330656 ) ) ;
#13671=CARTESIAN_POINT ( 'NONE',  ( 38.37017380507018771, -7.603840866421910150, 70.24448340153877268 ) ) ;
#13677=CARTESIAN_POINT ( 'NONE',  ( 36.89935272106205133, -10.40384086642191797, 73.23812341099225875 ) ) ;
#13680=CARTESIAN_POINT ( 'NONE',  ( 36.68196826583682935, -15.61368208888610454, 71.96809898377888715 ) ) ;
#13687=CARTESIAN_POINT ( 'NONE',  ( 36.49096545463212493, -0.1038408664219107880, 71.32335560751963044 ) ) ;
#13689=CARTESIAN_POINT ( 'NONE',  ( 38.93415946300897446, -16.11368208888611164, 73.09843995877329803 ) ) ;
#13693=CARTESIAN_POINT ( 'NONE',  ( 39.75915168707251723, -20.90384086642190553, 72.49904802271738902 ) ) ;
#13696=CARTESIAN_POINT ( 'NONE',  ( 37.33957961208646736, -11.81368208888610916, 72.81632618279321889 ) ) ;
#13698=CARTESIAN_POINT ( 'NONE',  ( 40.55423172469004811, -24.41368208888610880, 72.05058123536539938 ) ) ;
#13702=CARTESIAN_POINT ( 'NONE',  ( 38.26194895904384197, -22.60384086642191548, 72.51602215082118619 ) ) ;
#13710=CARTESIAN_POINT ( 'NONE',  ( 38.82593461698265003, 1.296159133578084210, 73.13360434286906298 ) ) ;
#13713=CARTESIAN_POINT ( 'NONE',  ( 35.86008812008917346, 0.4863179111138961064, 71.43714994484035685 ) ) ;
#13721=CARTESIAN_POINT ( 'NONE',  ( 36.80608444377002542, -18.30384086642191122, 72.40698646996133903 ) ) ;
#13728=CARTESIAN_POINT ( 'NONE',  ( 38.00113996487112189, -5.703840866421911571, 70.22690120949091863 ) ) ;
#13736=CARTESIAN_POINT ( 'NONE',  ( 39.24876120206128860, -12.71368208888610241, 70.63227792289245599 ) ) ;
#13738=CARTESIAN_POINT ( 'NONE',  ( 39.31564783533280405, -12.31368208888610027, 72.03616607671141026 ) ) ;
#13747=CARTESIAN_POINT ( 'NONE',  ( 37.69796330110505522, -18.50384086642191406, 73.09843995877329803 ) ) ;
#13750=CARTESIAN_POINT ( 'NONE',  ( 37.38336156205274818, -17.71368208888609885, 72.12822762946750288 ) ) ;
#13755=CARTESIAN_POINT ( 'NONE',  ( 37.25202387243752611, -17.21368208888610241, 70.00779233799262613 ) ) ;
#13760=CARTESIAN_POINT ( 'NONE',  ( 39.29254315202756231, -28.81368208888610383, 69.94417936956671156 ) ) ;
#13769=CARTESIAN_POINT ( 'NONE',  ( 36.98690846071097127, -5.803840866421911215, 69.45876917294177133 ) ) ;
#13772=CARTESIAN_POINT ( 'NONE',  ( 39.98359781491296161, -14.41368208888610525, 71.86517103874047052 ) ) ;
#13776=CARTESIAN_POINT ( 'NONE',  ( 38.37017380507020192, -12.01368208888611022, 73.71602215082113219 ) ) ;
#13784=CARTESIAN_POINT ( 'NONE',  ( 37.89291511884479036, -10.50384086642191050, 72.49843995877331793 ) ) ;
#13785=CARTESIAN_POINT ( 'NONE',  ( 39.41296390513587511, -28.41368208888610525, 71.67976084211548482 ) ) ;
#13791=CARTESIAN_POINT ( 'NONE',  ( 36.89935272106205133, -28.40384086642191619, 73.23812341099225875 ) ) ;
#13792=CARTESIAN_POINT ( 'NONE',  ( 39.24876120206128860, -22.71368208888610241, 70.63227792289245599 ) ) ;
#13793=CARTESIAN_POINT ( 'NONE',  ( 39.73277004305198545, -0.2136820888861065970, 73.23812341099225875 ) ) ;
#13796=CARTESIAN_POINT ( 'NONE',  ( 38.93987200065210175, 1.196159133578088118, 72.33091598616827866 ) ) ;
#13801=CARTESIAN_POINT ( 'NONE',  ( 36.89935272106205133, -8.403840866421919742, 73.23812341099225875 ) ) ;
#13804=CARTESIAN_POINT ( 'NONE',  ( 38.37017380507020192, -14.01368208888610845, 73.11602215082116629 ) ) ;
#13807=CARTESIAN_POINT ( 'NONE',  ( 39.95015449827720744, -24.61368208888610454, 70.79240656858104330 ) ) ;
#13809=CARTESIAN_POINT ( 'NONE',  ( 37.33957961208645315, 0.1961591335780908663, 69.94417936956673998 ) ) ;
#13811=CARTESIAN_POINT ( 'NONE',  ( 40.14115730948191185, -18.51368208888610667, 71.32335560751960202 ) ) ;
#13813=CARTESIAN_POINT ( 'NONE',  ( 36.87297107704149823, -17.90384086642190908, 70.26145752964252722 ) ) ;
#13817=CARTESIAN_POINT ( 'NONE',  ( 38.37017380507020192, -10.01368208888611022, 73.11602215082118050 ) ) ;
#13819=CARTESIAN_POINT ( 'NONE',  ( 36.29569395875879678, -21.31368208888610027, 69.98269868914867686 ) ) ;
#13824=CARTESIAN_POINT ( 'NONE',  ( 37.31647492878124694, -20.30384086642190766, 72.03616607671141026 ) ) ;
#13832=CARTESIAN_POINT ( 'NONE',  ( 40.55423172469004101, -29.20384086642191335, 70.70992431699446001 ) ) ;
#13834=CARTESIAN_POINT ( 'NONE',  ( 39.02088643472237095, -2.913682088886100363, 69.02690120949094421 ) ) ;
#13843=CARTESIAN_POINT ( 'NONE',  ( 36.80608444377002542, -20.30384086642191832, 72.40698646996133903 ) ) ;
#13851=CARTESIAN_POINT ( 'NONE',  ( 37.25260217561390874, -6.003840866421913169, 70.97781676520604321 ) ) ;
#13858=CARTESIAN_POINT ( 'NONE',  ( 37.69225076346193504, -13.81368208888610383, 72.33091598616826445 ) ) ;
#13859=CARTESIAN_POINT ( 'NONE',  ( 39.41296390513587511, -8.413682088886101695, 71.67976084211552745 ) ) ;
#13866=CARTESIAN_POINT ( 'NONE',  ( 37.80618814713138676, -17.70384086642190979, 69.62690120949091011 ) ) ;
#13872=CARTESIAN_POINT ( 'NONE',  ( 39.37952058850012804, -16.61368208888610098, 70.97781676520601479 ) ) ;
#13877=CARTESIAN_POINT ( 'NONE',  ( 38.37017380507020192, -14.01368208888610845, 73.11602215082116629 ) ) ;
#13882=CARTESIAN_POINT ( 'NONE',  ( 40.08847615259004016, -29.10876147765399224, 71.39729523596237470 ) ) ;
#13891=CARTESIAN_POINT ( 'NONE',  ( 40.77203464402485622, -3.103840866421913258, 71.43714994484034264 ) ) ;
#13894=CARTESIAN_POINT ( 'NONE',  ( 39.75915168707250302, -8.713682088886097077, 70.26145752964252722 ) ) ;
#13897=CARTESIAN_POINT ( 'NONE',  ( 40.26954217208371034, -14.71368208888610241, 69.89063713639258424 ) ) ;
#13910=CARTESIAN_POINT ( 'NONE',  ( 39.24876120206128860, -26.71368208888610596, 70.63227792289242757 ) ) ;
#13917=CARTESIAN_POINT ( 'NONE',  ( 35.86008812008917346, -24.10384086642191193, 71.32335560751960202 ) ) ;
#13921=CARTESIAN_POINT ( 'NONE',  ( 39.51027997493896748, -26.51368208888610667, 71.32335560751960202 ) ) ;
#13922=CARTESIAN_POINT ( 'NONE',  ( 35.86008812008917346, 0.4863179111138961064, 71.43714994484035685 ) ) ;
#13925=CARTESIAN_POINT ( 'NONE',  ( 39.37952058850012804, -1.003840866421912281, 71.78268878715392987 ) ) ;
#13930=CARTESIAN_POINT ( 'NONE',  ( 40.52078840805429394, -3.003840866421914502, 72.15350918040385864 ) ) ;
#13934=CARTESIAN_POINT ( 'NONE',  ( 37.69796330110504101, -5.113682088886101873, 69.66206559358663242 ) ) ;
#13936=CARTESIAN_POINT ( 'NONE',  ( 38.93415946300898867, -26.11368208888610454, 73.09843995877328382 ) ) ;
#13939=CARTESIAN_POINT ( 'NONE',  ( 39.82603832034401137, -3.303840866421908551, 70.35351908239860563 ) ) ;
#13942=CARTESIAN_POINT ( 'NONE',  ( 38.37017380507020192, -10.01368208888611022, 73.11602215082118050 ) ) ;
#13944=CARTESIAN_POINT ( 'NONE',  ( 38.26194895904384907, -12.60384086642191548, 73.11602215082116629 ) ) ;
#13946=CARTESIAN_POINT ( 'NONE',  ( 38.93415946300897446, -14.11368208888610631, 73.09843995877329803 ) ) ;
#13948=CARTESIAN_POINT ( 'NONE',  ( 37.50301148336529167, -23.11368208888610454, 69.06206559358663810 ) ) ;
#13952=CARTESIAN_POINT ( 'NONE',  ( 39.51027997493896748, -15.10384086642191370, 71.43714994484032843 ) ) ;
#13958=CARTESIAN_POINT ( 'NONE',  ( 36.89935272106205133, -20.40384086642192329, 73.23812341099225875 ) ) ;
#13961=CARTESIAN_POINT ( 'NONE',  ( 39.73277004305198545, -0.2136820888861065970, 73.23812341099225875 ) ) ;
#13970=CARTESIAN_POINT ( 'NONE',  ( 39.98359781491296161, -19.20384086642191335, 70.89533451361945993 ) ) ;
#13980=CARTESIAN_POINT ( 'NONE',  ( 39.02742774030101458, -5.403840866421909972, 70.49320253461759478 ) ) ;
#13991=CARTESIAN_POINT ( 'NONE',  ( 37.25260217561390874, -7.613682088886100985, 71.78268878715394408 ) ) ;
#13992=CARTESIAN_POINT ( 'NONE',  ( 37.31647492878122563, -5.313682088886097610, 70.72433947564853440 ) ) ;
#13999=CARTESIAN_POINT ( 'NONE',  ( 37.33957961208645315, -11.80384086642190944, 69.94417936956672577 ) ) ;
#14001=B_SPLINE_CURVE_WITH_KNOTS ( 'NONE', 3,
 ( #24038, #8469, #10400, #11968, #83, #9900, #12344, #19935, #23911, #19805, #21614, #12213, #6526, #13882, #6025, #21992 ),
 .UNSPECIFIED., .F., .F.,
 ( 4, 2, 2, 2, 2, 2, 2, 4 ),
 ( 0.001207831664637873956, 0.001646106639017851266, 0.002084381613397828792, 0.002522656587777805885, 0.002741794074967794648, 0.002851362818562789246, 0.002906147190360304326, 0.002960931562157818973 ),
 .UNSPECIFIED. ) ;
#14008=CARTESIAN_POINT ( 'NONE',  ( 38.93415946300898867, -16.11368208888611164, 73.09843995877329803 ) ) ;
#14021=CARTESIAN_POINT ( 'NONE',  ( 35.86008812008917346, -4.103840866421913702, 71.32335560751961623 ) ) ;
#14025=CARTESIAN_POINT ( 'NONE',  ( 39.95015449827720744, -6.613682088886106314, 70.79240656858107172 ) ) ;
#14030=CARTESIAN_POINT ( 'NONE',  ( 37.50301148336529167, -13.11368208888610454, 69.06206559358665231 ) ) ;
#14039=CARTESIAN_POINT ( 'NONE',  ( 39.41296390513587511, -26.41368208888610170, 71.67976084211548482 ) ) ;
#14045=CARTESIAN_POINT ( 'NONE',  ( 38.26194895904384197, -24.60384086642191903, 73.71602215082113219 ) ) ;
#14047=CARTESIAN_POINT ( 'NONE',  ( 38.93415946300897446, -26.11368208888610098, 73.09843995877328382 ) ) ;
#14056=CARTESIAN_POINT ( 'NONE',  ( 36.11133435605973574, -4.003840866421914946, 70.60699637195612866 ) ) ;
#14059=CARTESIAN_POINT ( 'NONE',  ( 36.87297107704152666, -7.713682088886109511, 72.49904802271743165 ) ) ;
#14062=CARTESIAN_POINT ( 'NONE',  ( 39.98359781491296161, -26.41368208888610525, 71.86517103874045631 ) ) ;
#14065=CARTESIAN_POINT ( 'NONE',  ( 38.93415946300897446, 0.4961591335780924927, 69.66206559358666084 ) ) ;
#14068=CARTESIAN_POINT ( 'NONE',  ( 39.37952058850012804, -25.00384086642191406, 71.78268878715390144 ) ) ;
#14069=CARTESIAN_POINT ( 'NONE',  ( 37.80618814713140097, -11.91368208888611058, 73.13360434286903455 ) ) ;
#14073=CARTESIAN_POINT ( 'NONE',  ( 37.33957961208645315, -13.80384086642190766, 69.94417936956672577 ) ) ;
#14076=CARTESIAN_POINT ( 'NONE',  ( 38.37017380507020192, -12.01368208888610845, 73.11602215082116629 ) ) ;
#14078=CARTESIAN_POINT ( 'NONE',  ( 36.89935272106204422, -15.21368208888610063, 69.52238214136768590 ) ) ;
#14082=CARTESIAN_POINT ( 'NONE',  ( 39.37952058850012804, -21.00384086642191050, 71.78268878715390144 ) ) ;
#14087=CARTESIAN_POINT ( 'NONE',  ( 40.52078840805429394, -21.00384086642191761, 72.15350918040381600 ) ) ;
#14089=CARTESIAN_POINT ( 'NONE',  ( 37.33957961208646736, -23.81368208888611093, 72.81632618279320468 ) ) ;
#14097=CARTESIAN_POINT ( 'NONE',  ( 37.69796330110505522, -22.50384086642191406, 73.09843995877329803 ) ) ;
#14105=CARTESIAN_POINT ( 'NONE',  ( 39.38009889167648936, -29.40384086642190908, 70.00779233799262613 ) ) ;
#14114=CARTESIAN_POINT ( 'NONE',  ( 39.02742774030102879, -8.213682088886098853, 72.26730301774236409 ) ) ;
#14117=CARTESIAN_POINT ( 'NONE',  ( 38.37017380507020192, -4.013682088886100452, 72.51602215082118619 ) ) ;
#14125=CARTESIAN_POINT ( 'NONE',  ( 37.80618814713138676, -9.703840866421904465, 69.62690120949091011 ) ) ;
#14134=CARTESIAN_POINT ( 'NONE',  ( 38.37017380507020192, -8.013682088886108446, 73.11602215082118050 ) ) ;
#14149=CARTESIAN_POINT ( 'NONE',  ( 40.77203464402485622, -5.103840866421915479, 71.43714994484034264 ) ) ;
#14155=CARTESIAN_POINT ( 'NONE',  ( 37.80618814713140097, -5.913682088886107024, 73.13360434286904876 ) ) ;
#14162=CARTESIAN_POINT ( 'NONE',  ( 40.26954217208371034, -16.71368208888610241, 69.89063713639258424 ) ) ;
#14173=CARTESIAN_POINT ( 'NONE',  ( 37.60469502381300089, -23.21368208888610241, 70.49320253461758057 ) ) ;
#14182=CARTESIAN_POINT ( 'NONE',  ( 40.77203464402485622, -25.10384086642191903, 71.43714994484031422 ) ) ;
#14183=CARTESIAN_POINT ( 'NONE',  ( 38.26194895904383486, -25.01368208888610312, 69.64448340153876416 ) ) ;
#14189=CARTESIAN_POINT ( 'NONE',  ( 36.36258059203030513, -5.903840866421909972, 69.89063713639259845 ) ) ;
#14193=CARTESIAN_POINT ( 'NONE',  ( 36.64852494920107517, -9.413682088886107024, 70.89533451361948835 ) ) ;
#14195=CARTESIAN_POINT ( 'NONE',  ( 36.87297107704153376, -23.71368208888610596, 72.49904802271738902 ) ) ;
#14198=CARTESIAN_POINT ( 'NONE',  ( 39.29254315202757653, 1.196159133578084788, 72.81632618279324731 ) ) ;
#14202=CARTESIAN_POINT ( 'NONE',  ( 39.41296390513587511, -25.20384086642191335, 71.08074471024438878 ) ) ;
#14203=CARTESIAN_POINT ( 'NONE',  ( 38.82593461698262871, -12.91368208888610347, 69.62690120949091011 ) ) ;
#14207=CARTESIAN_POINT ( 'NONE',  ( 38.82593461698265003, -14.70384086642191512, 73.13360434286903455 ) ) ;
#14210=CARTESIAN_POINT ( 'NONE',  ( 39.82603832034400426, -14.31368208888610916, 72.40698646996133903 ) ) ;
#14212=CARTESIAN_POINT ( 'NONE',  ( 40.33642880535524000, -16.31368208888611093, 72.77780686321126780 ) ) ;
#14216=CARTESIAN_POINT ( 'NONE',  ( 39.24876120206129571, -18.90384086642191264, 72.12822762946747446 ) ) ;
#14222=CARTESIAN_POINT ( 'NONE',  ( 39.64521430340305841, -22.80384086642191832, 73.30173637941818754 ) ) ;
#14224=CARTESIAN_POINT ( 'NONE',  ( 36.68196826583682935, -27.61368208888610809, 71.96809898377887293 ) ) ;
#14229=CARTESIAN_POINT ( 'NONE',  ( 39.29254315202757653, -14.80384086642191477, 72.81632618279321889 ) ) ;
#14235=CARTESIAN_POINT ( 'NONE',  ( 37.60469502381300799, -0.4038408664219124145, 72.26730301774236409 ) ) ;
#14243=CARTESIAN_POINT ( 'NONE',  ( 37.12184278917507640, -3.513682088886100452, 71.43714994484035685 ) ) ;
#14244=CARTESIAN_POINT ( 'NONE',  ( 37.21915885897815457, -7.413682088886101695, 71.08074471024443142 ) ) ;
#14252=CARTESIAN_POINT ( 'NONE',  ( 37.80618814713138676, -11.70384086642190624, 69.62690120949091011 ) ) ;
#14259=CARTESIAN_POINT ( 'NONE',  ( 39.38009889167650357, -8.213682088886105959, 72.75271321436733274 ) ) ;
#14270=CARTESIAN_POINT ( 'NONE',  ( 36.07789103942399578, -2.203840866421915123, 72.05058123536544201 ) ) ;
#14274=CARTESIAN_POINT ( 'NONE',  ( 38.93415946300897446, -6.113682088886107202, 73.09843995877331224 ) ) ;
#14276=CARTESIAN_POINT ( 'NONE',  ( 38.37017380507020192, -14.01368208888610845, 73.71602215082113219 ) ) ;
#14289=CARTESIAN_POINT ( 'NONE',  ( 38.00113996487114321, -23.91368208888610170, 72.53360434286901182 ) ) ;
#14296=CARTESIAN_POINT ( 'NONE',  ( 40.55423172469004101, -25.20384086642191690, 70.70992431699446001 ) ) ;
#14298=CARTESIAN_POINT ( 'NONE',  ( 39.12911128074873801, 1.886317911113891244, 73.69843995877330656 ) ) ;
#14308=CARTESIAN_POINT ( 'NONE',  ( 39.73277004305197124, -5.403840866421909972, 69.52238214136768590 ) ) ;
#14311=CARTESIAN_POINT ( 'NONE',  ( 39.29254315202756231, -8.813682088886100274, 69.94417936956673998 ) ) ;
#14314=CARTESIAN_POINT ( 'NONE',  ( 39.29254315202756231, -26.81368208888610027, 69.94417936956671156 ) ) ;
#14318=CARTESIAN_POINT ( 'NONE',  ( 38.37017380507018771, -23.60384086642191903, 70.24448340153875847 ) ) ;
#14319=CARTESIAN_POINT ( 'NONE',  ( 39.75915168707250302, -14.71368208888610063, 70.26145752964251301 ) ) ;
#14324=CARTESIAN_POINT ( 'NONE',  ( 39.75915168707251723, -10.90384086642191619, 72.49904802271740323 ) ) ;
#14326=CARTESIAN_POINT ( 'NONE',  ( 39.38009889167650357, -8.213682088886105959, 72.75271321436733274 ) ) ;
#14328=CARTESIAN_POINT ( 'NONE',  ( 38.37017380507020192, -16.01368208888610667, 73.71602215082113219 ) ) ;
#14332=CARTESIAN_POINT ( 'NONE',  ( 37.38336156205273397, -15.90384086642191264, 70.63227792289247020 ) ) ;
#14337=CARTESIAN_POINT ( 'NONE',  ( 39.02088643472237806, -24.70384086642192401, 73.73360434286898624 ) ) ;
#14339=CARTESIAN_POINT ( 'NONE',  ( 39.38009889167650357, -28.21368208888610951, 72.75271321436730432 ) ) ;
#14348=CARTESIAN_POINT ( 'NONE',  ( 38.93415946300897446, -13.50384086642190518, 69.66206559358663242 ) ) ;
#14355=CARTESIAN_POINT ( 'NONE',  ( 37.89291511884479036, -0.5038408664219118371, 72.49843995877331793 ) ) ;
#14363=CARTESIAN_POINT ( 'NONE',  ( 39.37952058850012804, -8.613682088886100985, 70.97781676520601479 ) ) ;
#14365=CARTESIAN_POINT ( 'NONE',  ( 37.69225076346193504, -1.813682088886100274, 72.33091598616827866 ) ) ;
#14371=CARTESIAN_POINT ( 'NONE',  ( 38.37017380507018771, -13.60384086642190837, 69.64448340153877837 ) ) ;
#14381=CARTESIAN_POINT ( 'NONE',  ( 40.14115730948191185, -10.51368208888610134, 71.32335560751961623 ) ) ;
#14394=CARTESIAN_POINT ( 'NONE',  ( 37.61123632939164452, 0.2961591335780902612, 69.02690120949095842 ) ) ;
#14396=CARTESIAN_POINT ( 'NONE',  ( 38.63098279924288647, -20.91368208888609814, 70.22690120949090442 ) ) ;
#14400=CARTESIAN_POINT ( 'NONE',  ( 36.68196826583682935, -9.613682088886104538, 71.96809898377890136 ) ) ;
#14401=CARTESIAN_POINT ( 'NONE',  ( 37.69796330110505522, -28.50384086642191406, 73.09843995877328382 ) ) ;
#14405=CARTESIAN_POINT ( 'NONE',  ( 36.29569395875879678, -11.31368208888609850, 69.98269868914867686 ) ) ;
#14423=CARTESIAN_POINT ( 'NONE',  ( 37.50301148336529877, -24.50384086642192116, 73.69843995877326392 ) ) ;
#14424=CARTESIAN_POINT ( 'NONE',  ( 39.75915168707250302, -26.71368208888609530, 70.26145752964249880 ) ) ;
#14432=CARTESIAN_POINT ( 'NONE',  ( 40.26954217208371034, -24.71368208888610241, 69.89063713639254161 ) ) ;
#14437=CARTESIAN_POINT ( 'NONE',  ( 38.26194895904383486, -7.013682088886100452, 69.64448340153879258 ) ) ;
#14440=CARTESIAN_POINT ( 'NONE',  ( 39.98359781491296161, -18.41368208888610880, 71.86517103874047052 ) ) ;
#14445=CARTESIAN_POINT ( 'NONE',  ( 39.02742774030101458, -25.40384086642191264, 70.49320253461758057 ) ) ;
#14446=CARTESIAN_POINT ( 'NONE',  ( 37.33957961208646736, -11.81368208888610916, 72.81632618279321889 ) ) ;
#14449=CARTESIAN_POINT ( 'NONE',  ( 40.14115730948191185, -11.10384086642191015, 71.43714994484034264 ) ) ;
#14451=CARTESIAN_POINT ( 'NONE',  ( 38.37017380507020192, -8.013682088886108446, 73.11602215082118050 ) ) ;
#14453=CARTESIAN_POINT ( 'NONE',  ( 36.98690846071097837, -17.81368208888610738, 73.30173637941818754 ) ) ;
#14458=CARTESIAN_POINT ( 'NONE',  ( 38.26194895904384197, -10.60384086642191370, 72.51602215082118619 ) ) ;
#14463=CARTESIAN_POINT ( 'NONE',  ( 40.77203464402485622, -21.10384086642191548, 71.43714994484032843 ) ) ;
#14467=CARTESIAN_POINT ( 'NONE',  ( 39.38009889167650357, -24.21368208888610596, 72.75271321436730432 ) ) ;
#14474=CARTESIAN_POINT ( 'NONE',  ( 39.38009889167648936, -13.40384086642191086, 70.00779233799262613 ) ) ;
#14480=CARTESIAN_POINT ( 'NONE',  ( 36.80608444377001831, -28.30384086642191122, 72.40698646996133903 ) ) ;
#14484=CARTESIAN_POINT ( 'NONE',  ( 36.80608444377001121, -27.31368208888610383, 70.35351908239857721 ) ) ;
#14489=CARTESIAN_POINT ( 'NONE',  ( 39.24876120206128860, -2.713682088886101962, 70.63227792289247020 ) ) ;
#14490=CARTESIAN_POINT ( 'NONE',  ( 39.37952058850012804, -0.6136820888861006518, 70.97781676520601479 ) ) ;
#14497=CARTESIAN_POINT ( 'NONE',  ( 36.64852494920107517, -8.203840866421909794, 71.86517103874049894 ) ) ;
#14506=CARTESIAN_POINT ( 'NONE',  ( 39.29254315202756231, -4.813682088886099386, 69.94417936956673998 ) ) ;
#14521=CARTESIAN_POINT ( 'NONE',  ( 36.29569395875879678, -27.31368208888610027, 69.98269868914866265 ) ) ;
#14522=CARTESIAN_POINT ( 'NONE',  ( 38.73920764526925353, -22.11368208888610098, 72.49843995877330372 ) ) ;
#14527=CARTESIAN_POINT ( 'NONE',  ( 38.93415946300897446, -2.113682088886109423, 73.09843995877331224 ) ) ;
#14528=CARTESIAN_POINT ( 'NONE',  ( 38.63098279924290068, 1.296159133578087763, 72.53360434286905445 ) ) ;
#14532=CARTESIAN_POINT ( 'NONE',  ( 39.64521430340304420, -8.813682088886096722, 69.45876917294177133 ) ) ;
#14546=CARTESIAN_POINT ( 'NONE',  ( 39.64521430340305841, -18.80384086642191477, 73.30173637941818754 ) ) ;
#14548=CARTESIAN_POINT ( 'NONE',  ( 38.93415946300897446, -22.11368208888610454, 73.09843995877329803 ) ) ;
#14556=CARTESIAN_POINT ( 'NONE',  ( 37.50301148336529167, -27.11368208888610454, 69.06206559358663810 ) ) ;
#14560=CARTESIAN_POINT ( 'NONE',  ( 39.82603832034400426, 1.686317911113891732, 72.40698646996136745 ) ) ;
#14562=CARTESIAN_POINT ( 'NONE',  ( 40.14115730948191185, -18.51368208888610312, 71.32335560751960202 ) ) ;
#14566=CARTESIAN_POINT ( 'NONE',  ( 38.26194895904384197, -24.60384086642190837, 72.51602215082114355 ) ) ;
#14567=CARTESIAN_POINT ( 'NONE',  ( 38.82593461698262871, -8.913682088886101695, 69.62690120949091011 ) ) ;
#14571=CARTESIAN_POINT ( 'NONE',  ( 36.80608444377001831, -4.303840866421916544, 72.40698646996136745 ) ) ;
#14574=CARTESIAN_POINT ( 'NONE',  ( 39.38009889167650357, -6.213682088886108623, 72.75271321436733274 ) ) ;
#14576=CARTESIAN_POINT ( 'NONE',  ( 40.52078840805428683, -14.61368208888610276, 70.60699637195608602 ) ) ;
#14580=CARTESIAN_POINT ( 'NONE',  ( 38.93987200065210175, -10.80384086642191299, 72.33091598616827866 ) ) ;
#14586=CARTESIAN_POINT ( 'NONE',  ( 40.77203464402485622, -17.10384086642191193, 71.43714994484032843 ) ) ;
#14590=CARTESIAN_POINT ( 'NONE',  ( 36.87297107704152666, -25.71368208888609885, 72.49904802271738902 ) ) ;
#14596=CARTESIAN_POINT ( 'NONE',  ( 36.49096545463212493, -14.10384086642191193, 71.32335560751961623 ) ) ;
#14605=CARTESIAN_POINT ( 'NONE',  ( 39.82603832034400426, -29.30384086642190766, 70.35351908239857721 ) ) ;
#14609=CARTESIAN_POINT ( 'NONE',  ( 37.69796330110504101, -23.11368208888609743, 69.66206559358660400 ) ) ;
#14614=CARTESIAN_POINT ( 'NONE',  ( 39.31564783533280405, 1.686317911113899282, 72.03616607671141026 ) ) ;
#14615=CARTESIAN_POINT ( 'NONE',  ( 39.51027997493896748, -0.5136820888861012291, 71.32335560751961623 ) ) ;
#14623=CARTESIAN_POINT ( 'NONE',  ( 37.80618814713138676, -7.703840866421907130, 69.62690120949091011 ) ) ;
#14631=CARTESIAN_POINT ( 'NONE',  ( 39.82603832034401847, -6.313682088886107380, 72.40698646996133903 ) ) ;
#14642=CARTESIAN_POINT ( 'NONE',  ( 40.26954217208372455, 1.096159133578081812, 72.86986841596736042 ) ) ;
#14644=CARTESIAN_POINT ( 'NONE',  ( 37.69225076346193504, -19.81368208888610383, 72.33091598616826445 ) ) ;
#14648=CARTESIAN_POINT ( 'NONE',  ( 37.69796330110504101, -5.113682088886101873, 69.66206559358663242 ) ) ;
#14649=CARTESIAN_POINT ( 'NONE',  ( 39.29254315202757653, -28.80384086642191832, 72.81632618279320468 ) ) ;
#14651=CARTESIAN_POINT ( 'NONE',  ( 35.86008812008917346, -5.513682088886105781, 71.43714994484035685 ) ) ;
#14665=CARTESIAN_POINT ( 'NONE',  ( 40.77203464402485622, -17.10384086642191193, 71.43714994484032843 ) ) ;
#14666=CARTESIAN_POINT ( 'NONE',  ( 36.68196826583682935, -19.61368208888610809, 71.96809898377888715 ) ) ;
#14672=CARTESIAN_POINT ( 'NONE',  ( 39.02088643472237806, 1.296159133578080658, 73.73360434286904308 ) ) ;
#14681=CARTESIAN_POINT ( 'NONE',  ( 39.75915168707250302, -2.713682088886101962, 70.26145752964252722 ) ) ;
#14683=CARTESIAN_POINT ( 'NONE',  ( 38.26194895904383486, -21.01368208888610312, 69.64448340153877837 ) ) ;
#14687=CARTESIAN_POINT ( 'NONE',  ( 37.38336156205273397, -15.90384086642191264, 70.63227792289247020 ) ) ;
#14688=CARTESIAN_POINT ( 'NONE',  ( 38.82593461698262871, -4.913682088886100807, 69.62690120949091011 ) ) ;
#14694=CARTESIAN_POINT ( 'NONE',  ( 38.37017380507018771, -7.603840866421906597, 69.64448340153879258 ) ) ;
#14698=CARTESIAN_POINT ( 'NONE',  ( 39.75915168707250302, -2.713682088886101962, 70.26145752964252722 ) ) ;
#14700=CARTESIAN_POINT ( 'NONE',  ( 40.77203464402485622, -8.513682088886104893, 71.32335560751961623 ) ) ;
#14703=CARTESIAN_POINT ( 'NONE',  ( 39.02742774030101458, -11.40384086642191086, 70.49320253461759478 ) ) ;
#14708=CARTESIAN_POINT ( 'NONE',  ( 40.33642880535521869, -15.30384086642191477, 69.98269868914866265 ) ) ;
#14710=FILL_AREA_STYLE_COLOUR ( '', #25131 ) ;
#14711=CARTESIAN_POINT ( 'NONE',  ( 40.14115730948191185, -18.51368208888610667, 71.32335560751960202 ) ) ;
#14720=CARTESIAN_POINT ( 'NONE',  ( 39.82603832034401137, -13.30384086642190589, 70.35351908239857721 ) ) ;
#14723=CARTESIAN_POINT ( 'NONE',  ( 38.37017380507020192, -28.01368208888610667, 73.11602215082115208 ) ) ;
#14728=CARTESIAN_POINT ( 'NONE',  ( 37.69796330110505522, -26.50384086642190695, 73.09843995877328382 ) ) ;
#14730=CARTESIAN_POINT ( 'NONE',  ( 38.37017380507020192, -22.01368208888611022, 73.11602215082116629 ) ) ;
#14736=CARTESIAN_POINT ( 'NONE',  ( 38.93987200065208754, 1.186317911113898838, 70.42958956619170863 ) ) ;
#14738=CARTESIAN_POINT ( 'NONE',  ( 38.93987200065210175, -28.80384086642191477, 72.33091598616823603 ) ) ;
#14744=CARTESIAN_POINT ( 'NONE',  ( 37.69796330110505522, -4.503840866421913169, 73.09843995877331224 ) ) ;
#14757=CARTESIAN_POINT ( 'NONE',  ( 39.95015449827720744, 1.386317911113894130, 70.79240656858108593 ) ) ;
#14773=CARTESIAN_POINT ( 'NONE',  ( 37.69225076346193504, -17.81368208888610383, 72.33091598616826445 ) ) ;
#14777=CARTESIAN_POINT ( 'NONE',  ( 38.26194895904383486, -5.013682088886102228, 69.64448340153879258 ) ) ;
#14778=CARTESIAN_POINT ( 'NONE',  ( 40.14115730948191185, -25.10384086642190482, 71.43714994484028580 ) ) ;
#14781=CARTESIAN_POINT ( 'NONE',  ( 36.89935272106204422, -9.213682088886100630, 69.52238214136768590 ) ) ;
#14799=CARTESIAN_POINT ( 'NONE',  ( 37.50301148336529877, -18.50384086642192116, 73.69843995877327814 ) ) ;
#14802=CARTESIAN_POINT ( 'NONE',  ( 38.37017380507020192, -20.01368208888610667, 73.11602215082116629 ) ) ;
#14808=CARTESIAN_POINT ( 'NONE',  ( 39.12911128074872380, 0.4961591335780889955, 69.06206559358666652 ) ) ;
#14812=CARTESIAN_POINT ( 'NONE',  ( 36.87297107704152666, -1.713682088886108179, 72.49904802271743165 ) ) ;
#14814=CARTESIAN_POINT ( 'NONE',  ( 37.25202387243752611, -21.21368208888610241, 70.00779233799262613 ) ) ;
#14819=CARTESIAN_POINT ( 'NONE',  ( 39.24876120206129571, -20.90384086642191264, 72.12822762946747446 ) ) ;
#14820=CARTESIAN_POINT ( 'NONE',  ( 37.33957961208646736, -5.813682088886107380, 72.81632618279323310 ) ) ;
#14824=CARTESIAN_POINT ( 'NONE',  ( 36.64852494920107517, -2.203840866421912015, 71.86517103874049894 ) ) ;
#14827=CARTESIAN_POINT ( 'NONE',  ( 38.82593461698262871, -2.913682088886099919, 69.62690120949091011 ) ) ;
#14829=CARTESIAN_POINT ( 'NONE',  ( 37.61123632939165873, -7.913682088886107913, 73.73360434286902887 ) ) ;
#14832=CARTESIAN_POINT ( 'NONE',  ( 38.63098279924290068, -14.70384086642191157, 72.53360434286904024 ) ) ;
#14838=CARTESIAN_POINT ( 'NONE',  ( 37.61123632939164452, -13.70384086642191157, 69.02690120949091579 ) ) ;
#14841=CARTESIAN_POINT ( 'NONE',  ( 36.68196826583682935, -21.61368208888610454, 71.96809898377888715 ) ) ;
#14844=EDGE_LOOP ( 'NONE', ( #3427, #16407, #17410 ) ) ;
#14847=CARTESIAN_POINT ( 'NONE',  ( 39.82603832034401137, -7.303840866421907663, 70.35351908239860563 ) ) ;
#14850=CARTESIAN_POINT ( 'NONE',  ( 38.93415946300897446, -24.11368208888610454, 73.09843995877328382 ) ) ;
#14853=CARTESIAN_POINT ( 'NONE',  ( 39.98359781491296161, -25.20384086642191335, 70.89533451361944572 ) ) ;
#14855=CARTESIAN_POINT ( 'NONE',  ( 36.68196826583682935, -21.61368208888610454, 71.96809898377888715 ) ) ;
#14860=CARTESIAN_POINT ( 'NONE',  ( 38.63098279924290068, -28.70384086642190979, 72.53360434286901182 ) ) ;
#14861=CARTESIAN_POINT ( 'NONE',  ( 39.41296390513587511, 1.586317911113900081, 71.67976084211552745 ) ) ;
#14868=CARTESIAN_POINT ( 'NONE',  ( 38.93415946300896024, -5.503840866421906952, 69.66206559358663242 ) ) ;
#14876=CARTESIAN_POINT ( 'NONE',  ( 37.33957961208646736, -3.813682088886109156, 72.81632618279323310 ) ) ;
#14896=CARTESIAN_POINT ( 'NONE',  ( 39.31564783533280405, -16.31368208888610383, 72.03616607671141026 ) ) ;
#14901=CARTESIAN_POINT ( 'NONE',  ( 36.68196826583682935, -3.613682088886103205, 71.96809898377890136 ) ) ;
#14902=CARTESIAN_POINT ( 'NONE',  ( 37.69796330110505522, -24.50384086642190695, 73.09843995877328382 ) ) ;
#14905=CARTESIAN_POINT ( 'NONE',  ( 36.36258059203031934, -9.713682088886105959, 72.86986841596736042 ) ) ;
#14913=DIRECTION ( 'NONE',  ( -2.994052579541399595E-16, 1.632680918566405413E-15, -1.000000000000000000 ) ) ;
#14926=CARTESIAN_POINT ( 'NONE',  ( 36.89935272106205133, -16.40384086642191974, 73.23812341099225875 ) ) ;
#14930=CARTESIAN_POINT ( 'NONE',  ( 36.64852494920107517, -23.41368208888610525, 70.89533451361945993 ) ) ;
#14938=CARTESIAN_POINT ( 'NONE',  ( 35.86008812008917346, -25.51368208888610667, 71.43714994484032843 ) ) ;
#14943=CARTESIAN_POINT ( 'NONE',  ( 37.33957961208646736, -1.813682088886107380, 72.81632618279323310 ) ) ;
#14946=CARTESIAN_POINT ( 'NONE',  ( 38.93415946300898867, -20.11368208888610809, 73.09843995877329803 ) ) ;
#14951=CARTESIAN_POINT ( 'NONE',  ( 39.37952058850012804, -19.00384086642191406, 71.78268878715390144 ) ) ;
#14952=CARTESIAN_POINT ( 'NONE',  ( 37.69796330110504101, -7.113682088886100985, 69.66206559358663242 ) ) ;
#14957=CARTESIAN_POINT ( 'NONE',  ( 37.33957961208645315, -5.803840866421907663, 69.94417936956673998 ) ) ;
#14959=CARTESIAN_POINT ( 'NONE',  ( 36.68196826583682935, -1.613682088886104982, 71.96809898377890136 ) ) ;
#14961=CARTESIAN_POINT ( 'NONE',  ( 40.52078840805428683, -8.613682088886102761, 70.60699637195608602 ) ) ;
#14964=CARTESIAN_POINT ( 'NONE',  ( 37.60469502381300799, -14.40384086642191441, 72.26730301774234988 ) ) ;
#14970=CARTESIAN_POINT ( 'NONE',  ( 39.64521430340305841, -18.80384086642191477, 73.30173637941818754 ) ) ;
#14974=CARTESIAN_POINT ( 'NONE',  ( 37.25202387243752611, -23.21368208888610241, 70.00779233799262613 ) ) ;
#14983=CARTESIAN_POINT ( 'NONE',  ( 37.25202387243754032, -10.40384086642191441, 72.75271321436733274 ) ) ;
#14985=CARTESIAN_POINT ( 'NONE',  ( 37.33957961208646736, -21.81368208888610738, 72.81632618279321889 ) ) ;
#14989=CARTESIAN_POINT ( 'NONE',  ( 39.82603832034400426, -25.30384086642190766, 70.35351908239857721 ) ) ;
#14992=CARTESIAN_POINT ( 'NONE',  ( 37.69796330110504101, -25.11368208888609388, 69.66206559358660400 ) ) ;
#14997=CARTESIAN_POINT ( 'NONE',  ( 38.00113996487114321, 0.08631791111389855442, 72.53360434286905445 ) ) ;
#15004=CARTESIAN_POINT ( 'NONE',  ( 40.14115730948191185, -5.103840866421909261, 71.43714994484034264 ) ) ;
#15013=CARTESIAN_POINT ( 'NONE',  ( 39.98359781491296161, -2.413682088886103472, 71.86517103874048473 ) ) ;
#15028=CARTESIAN_POINT ( 'NONE',  ( 38.00113996487114321, -17.91368208888609459, 72.53360434286904024 ) ) ;
#15032=CARTESIAN_POINT ( 'NONE',  ( 39.75915168707250302, -0.7136820888860997414, 70.26145752964252722 ) ) ;
#15033=CARTESIAN_POINT ( 'NONE',  ( 39.29254315202757653, -20.80384086642191832, 72.81632618279321889 ) ) ;
#15035=CARTESIAN_POINT ( 'NONE',  ( 39.64521430340304420, -2.813682088886101162, 69.45876917294177133 ) ) ;
#15050=CARTESIAN_POINT ( 'NONE',  ( 37.61123632939164452, -15.70384086642191157, 69.02690120949091579 ) ) ;
#15052=CARTESIAN_POINT ( 'NONE',  ( 39.95015449827720744, -20.61368208888610454, 70.79240656858105751 ) ) ;
#15058=CARTESIAN_POINT ( 'NONE',  ( 36.98690846071097837, -21.81368208888610738, 73.30173637941818754 ) ) ;
#15062=CARTESIAN_POINT ( 'NONE',  ( 37.69796330110504101, 0.8863179111139003474, 69.66206559358664663 ) ) ;
#15065=CARTESIAN_POINT ( 'NONE',  ( 37.80618814713140097, -13.91368208888610702, 73.13360434286903455 ) ) ;
#15071=CARTESIAN_POINT ( 'NONE',  ( 39.31564783533279694, -17.30384086642191477, 70.72433947564853440 ) ) ;
#15072=CARTESIAN_POINT ( 'NONE',  ( 39.98359781491296161, -8.413682088886105248, 71.86517103874048473 ) ) ;
#15079=CARTESIAN_POINT ( 'NONE',  ( 39.95015449827720744, -3.003840866421910505, 71.96809898377888715 ) ) ;
#15081=CARTESIAN_POINT ( 'NONE',  ( 37.69796330110504101, 0.8863179111139003474, 69.66206559358664663 ) ) ;
#15083=CARTESIAN_POINT ( 'NONE',  ( 40.52078840805428683, -6.613682088886105426, 70.60699637195608602 ) ) ;
#15086=CARTESIAN_POINT ( 'NONE',  ( 37.69225076346193504, -5.803840866421911215, 70.42958956619168021 ) ) ;
#15093=CARTESIAN_POINT ( 'NONE',  ( 40.52078840805429394, -19.00384086642191406, 72.15350918040381600 ) ) ;
#15095=CARTESIAN_POINT ( 'NONE',  ( 38.93415946300897446, -18.11368208888611164, 73.09843995877329803 ) ) ;
#15102=CARTESIAN_POINT ( 'NONE',  ( 39.29254315202757653, -8.803840866421912992, 72.81632618279323310 ) ) ;
#15105=CARTESIAN_POINT ( 'NONE',  ( 36.68196826583682935, -27.61368208888610809, 71.96809898377887293 ) ) ;
#15110=CARTESIAN_POINT ( 'NONE',  ( 39.95015449827720744, -25.00384086642191406, 71.96809898377885872 ) ) ;
#15112=CARTESIAN_POINT ( 'NONE',  ( 36.49096545463212493, -17.51368208888610667, 71.43714994484034264 ) ) ;
#15113=ORIENTED_EDGE ( 'NONE', *, *, #18953, .T. ) ;
#15114=CARTESIAN_POINT ( 'NONE',  ( 35.86008812008917346, -25.51368208888610667, 71.43714994484032843 ) ) ;
#15118=CARTESIAN_POINT ( 'NONE',  ( 39.24876120206128860, 1.286317911113898260, 70.63227792289248441 ) ) ;
#15126=CARTESIAN_POINT ( 'NONE',  ( 39.38009889167648936, -5.403840866421906419, 70.00779233799264034 ) ) ;
#15135=CARTESIAN_POINT ( 'NONE',  ( 37.69796330110504101, 0.8863179111139005695, 69.66206559358666084 ) ) ;
#15136=CARTESIAN_POINT ( 'NONE',  ( 37.25202387243754032, -26.40384086642191619, 72.75271321436730432 ) ) ;
#15154=CARTESIAN_POINT ( 'NONE',  ( 37.31647492878122563, -15.31368208888610205, 70.72433947564853440 ) ) ;
#15160=CARTESIAN_POINT ( 'NONE',  ( 39.95015449827720744, -25.00384086642191406, 71.96809898377885872 ) ) ;
#15177=CARTESIAN_POINT ( 'NONE',  ( 40.26954217208372455, -12.90384086642192152, 72.86986841596734621 ) ) ;
#15180=CARTESIAN_POINT ( 'NONE',  ( 39.95015449827720744, -14.61368208888610454, 70.79240656858105751 ) ) ;
#15184=CARTESIAN_POINT ( 'NONE',  ( 37.61123632939165873, -19.91368208888610880, 73.73360434286898624 ) ) ;
#15195=CARTESIAN_POINT ( 'NONE',  ( 38.73920764526923932, -19.50384086642191406, 70.26206559358661252 ) ) ;
#15196=CARTESIAN_POINT ( 'NONE',  ( 37.69225076346193504, -27.81368208888610383, 72.33091598616823603 ) ) ;
#15204=CARTESIAN_POINT ( 'NONE',  ( 39.82603832034400426, -1.303840866421906997, 70.35351908239857721 ) ) ;
#15207=CARTESIAN_POINT ( 'NONE',  ( 38.93415946300897446, -2.113682088886109423, 73.09843995877331224 ) ) ;
#15208=CARTESIAN_POINT ( 'NONE',  ( 40.33642880535524000, -8.313682088886110932, 72.77780686321128201 ) ) ;
#15212=CARTESIAN_POINT ( 'NONE',  ( 38.00113996487112189, -7.703840866421914235, 70.22690120949091863 ) ) ;
#15218=CARTESIAN_POINT ( 'NONE',  ( 40.77203464402485622, -7.103840866421913702, 71.43714994484034264 ) ) ;
#15220=CARTESIAN_POINT ( 'NONE',  ( 37.25202387243752611, -11.21368208888610241, 70.00779233799262613 ) ) ;
#15229=CARTESIAN_POINT ( 'NONE',  ( 38.37017380507018771, -9.603840866421908373, 69.64448340153879258 ) ) ;
#15232=CARTESIAN_POINT ( 'NONE',  ( 38.82593461698262871, -24.91368208888610170, 69.62690120949091011 ) ) ;
#15233=APPLICATION_CONTEXT ( 'automotive_design' ) ;
#15236=CARTESIAN_POINT ( 'NONE',  ( 39.95015449827720744, -17.00384086642191406, 71.96809898377887293 ) ) ;
#15240=CARTESIAN_POINT ( 'NONE',  ( 40.14115730948191185, -18.51368208888610667, 71.32335560751960202 ) ) ;
#15242=CARTESIAN_POINT ( 'NONE',  ( 38.37017380507018771, 0.3961591335780896284, 69.04448340153882668 ) ) ;
#15247=CARTESIAN_POINT ( 'NONE',  ( 38.00113996487112189, -23.70384086642191335, 70.22690120949089021 ) ) ;
#15256=CARTESIAN_POINT ( 'NONE',  ( 40.77203464402485622, -29.10384086642191193, 71.43714994484031422 ) ) ;
#15279=CARTESIAN_POINT ( 'NONE',  ( 38.73920764526925353, -14.11368208888610098, 72.49843995877330372 ) ) ;
#15280=CARTESIAN_POINT ( 'NONE',  ( 38.73920764526925353, -14.11368208888610098, 72.49843995877330372 ) ) ;
#15284=CARTESIAN_POINT ( 'NONE',  ( 39.38009889167650357, 1.786317911113891821, 72.75271321436734695 ) ) ;
#15285=CARTESIAN_POINT ( 'NONE',  ( 36.64852494920107517, -24.20384086642190979, 71.86517103874047052 ) ) ;
#15288=CARTESIAN_POINT ( 'NONE',  ( 38.73920764526925353, -20.11368208888610098, 72.49843995877330372 ) ) ;
#15307=CARTESIAN_POINT ( 'NONE',  ( 38.37017380507018771, -11.60384086642191015, 69.04448340153881247 ) ) ;
#15310=CARTESIAN_POINT ( 'NONE',  ( 38.82593461698262871, -12.91368208888610347, 69.62690120949091011 ) ) ;
#15315=CARTESIAN_POINT ( 'NONE',  ( 39.02088643472237095, -22.91368208888609814, 69.02690120949091579 ) ) ;
#15326=CARTESIAN_POINT ( 'NONE',  ( 38.63098279924290068, -14.70384086642191157, 72.53360434286904024 ) ) ;
#15327=CARTESIAN_POINT ( 'NONE',  ( 38.93415946300897446, 1.886317911113891244, 73.09843995877332645 ) ) ;
#15335=CARTESIAN_POINT ( 'NONE',  ( 37.33957961208645315, 0.1961591335780908663, 69.94417936956673998 ) ) ;
#15338=CARTESIAN_POINT ( 'NONE',  ( 38.37017380507020192, 1.986317911113890444, 73.11602215082119471 ) ) ;
#15339=CARTESIAN_POINT ( 'NONE',  ( 37.50301148336529167, -1.113682088886101207, 69.06206559358666652 ) ) ;
#15342=CARTESIAN_POINT ( 'NONE',  ( 37.69225076346193504, -7.803840866421912104, 70.42958956619168021 ) ) ;
#15347=CARTESIAN_POINT ( 'NONE',  ( 40.26954217208372455, -12.90384086642192152, 72.86986841596734621 ) ) ;
#15350=CARTESIAN_POINT ( 'NONE',  ( 38.93415946300897446, -14.11368208888610631, 73.09843995877329803 ) ) ;
#15356=CARTESIAN_POINT ( 'NONE',  ( 36.49096545463212493, -10.10384086642191193, 71.32335560751963044 ) ) ;
#15359=CARTESIAN_POINT ( 'NONE',  ( 39.95015449827720744, -16.61368208888610454, 70.79240656858105751 ) ) ;
#15362=CARTESIAN_POINT ( 'NONE',  ( 37.80618814713138676, -15.70384086642191157, 69.62690120949091011 ) ) ;
#15366=CARTESIAN_POINT ( 'NONE',  ( 37.33957961208646736, -15.81368208888610916, 72.81632618279321889 ) ) ;
#15368=CARTESIAN_POINT ( 'NONE',  ( 36.36258059203031934, -21.71368208888610596, 72.86986841596736042 ) ) ;
#15373=CARTESIAN_POINT ( 'NONE',  ( 39.37952058850012804, -23.00384086642191050, 71.78268878715390144 ) ) ;
#15381=CARTESIAN_POINT ( 'NONE',  ( 39.12911128074872380, -29.50384086642191050, 69.06206559358663810 ) ) ;
#15391=CARTESIAN_POINT ( 'NONE',  ( 39.98359781491296161, -25.20384086642191335, 70.89533451361944572 ) ) ;
#15404=CARTESIAN_POINT ( 'NONE',  ( 37.21915885897815457, -6.203840866421912459, 71.67976084211552745 ) ) ;
#15412=CARTESIAN_POINT ( 'NONE',  ( 39.24876120206128860, -10.71368208888610063, 70.63227792289247020 ) ) ;
#15414=CARTESIAN_POINT ( 'NONE',  ( 39.51027997493896748, -8.513682088886101340, 71.32335560751961623 ) ) ;
#15420=CARTESIAN_POINT ( 'NONE',  ( 36.80608444377001831, -16.30384086642191477, 72.40698646996135324 ) ) ;
#15422=CARTESIAN_POINT ( 'NONE',  ( 38.00113996487114321, -19.91368208888610170, 72.53360434286904024 ) ) ;
#15436=CARTESIAN_POINT ( 'NONE',  ( 37.61123632939164452, -11.70384086642191335, 69.02690120949094421 ) ) ;
#15438=CARTESIAN_POINT ( 'NONE',  ( 39.95015449827720744, -16.61368208888610454, 70.79240656858105751 ) ) ;
#15443=CARTESIAN_POINT ( 'NONE',  ( 40.77203464402485622, -22.51368208888610667, 71.32335560751960202 ) ) ;
#15453=CARTESIAN_POINT ( 'NONE',  ( 39.51027997493896748, -11.10384086642191015, 71.43714994484034264 ) ) ;
#15454=CARTESIAN_POINT ( 'NONE',  ( 39.24876120206128860, -28.71368208888610241, 70.63227792289242757 ) ) ;
#15460=CARTESIAN_POINT ( 'NONE',  ( 40.33642880535521869, -29.30384086642190766, 69.98269868914864844 ) ) ;
#15461=CARTESIAN_POINT ( 'NONE',  ( 37.60469502381300089, -27.21368208888609885, 70.49320253461758057 ) ) ;
#15462=CARTESIAN_POINT ( 'NONE',  ( 37.61123632939165873, -1.913682088886106580, 73.73360434286902887 ) ) ;
#15466=CARTESIAN_POINT ( 'NONE',  ( 37.31647492878124694, -2.303840866421911215, 72.03616607671141026 ) ) ;
#15472=CARTESIAN_POINT ( 'NONE',  ( 38.37017380507018771, -9.603840866421911926, 69.04448340153881247 ) ) ;
#15475=CARTESIAN_POINT ( 'NONE',  ( 40.14115730948191185, -12.51368208888610489, 71.32335560751960202 ) ) ;
#15481=CARTESIAN_POINT ( 'NONE',  ( 39.29254315202757653, -2.803840866421915212, 72.81632618279323310 ) ) ;
#15484=CARTESIAN_POINT ( 'NONE',  ( 36.68196826583682935, -17.61368208888610454, 71.96809898377888715 ) ) ;
#15486=CARTESIAN_POINT ( 'NONE',  ( 36.68196826583682935, -20.00384086642191050, 70.79240656858107172 ) ) ;
#15488=CARTESIAN_POINT ( 'NONE',  ( 36.49096545463212493, -19.51368208888610312, 71.43714994484034264 ) ) ;
#15490=CARTESIAN_POINT ( 'NONE',  ( 40.55423172469004811, -20.41368208888610880, 72.05058123536544201 ) ) ;
#15494=CARTESIAN_POINT ( 'NONE',  ( 38.00113996487112189, -21.70384086642190979, 70.22690120949090442 ) ) ;
#15500=CARTESIAN_POINT ( 'NONE',  ( 40.33642880535521869, -29.30384086642190766, 69.98269868914864844 ) ) ;
#15502=CARTESIAN_POINT ( 'NONE',  ( 38.26194895904383486, -5.013682088886101340, 69.04448340153881247 ) ) ;
#15512=CARTESIAN_POINT ( 'NONE',  ( 36.68196826583682935, -26.00384086642191406, 70.79240656858105751 ) ) ;
#15519=CARTESIAN_POINT ( 'NONE',  ( 37.69225076346193504, -5.803840866421911215, 70.42958956619168021 ) ) ;
#15526=CARTESIAN_POINT ( 'NONE',  ( 39.41296390513587511, -12.41368208888609992, 71.67976084211551324 ) ) ;
#15531=CARTESIAN_POINT ( 'NONE',  ( 37.89291511884476904, -11.11368208888610276, 70.26206559358664094 ) ) ;
#15536=CARTESIAN_POINT ( 'NONE',  ( 38.26194895904384907, -18.60384086642191548, 73.11602215082116629 ) ) ;
#15540=CARTESIAN_POINT ( 'NONE',  ( 37.25260217561390874, -21.61368208888610098, 71.78268878715392987 ) ) ;
#15543=CARTESIAN_POINT ( 'NONE',  ( 39.82603832034401847, -16.31368208888610738, 72.40698646996131060 ) ) ;
#15556=CARTESIAN_POINT ( 'NONE',  ( 39.64521430340305841, -8.803840866421916544, 73.30173637941818754 ) ) ;
#15559=CARTESIAN_POINT ( 'NONE',  ( 37.33957961208646736, -11.81368208888610916, 72.81632618279321889 ) ) ;
#15566=CARTESIAN_POINT ( 'NONE',  ( 39.64521430340304420, -22.81368208888610383, 69.45876917294175712 ) ) ;
#15576=CARTESIAN_POINT ( 'NONE',  ( 39.37952058850012804, -13.00384086642191228, 71.78268878715390144 ) ) ;
#15577=CARTESIAN_POINT ( 'NONE',  ( 39.31564783533280405, -28.31368208888610383, 72.03616607671136762 ) ) ;
#15585=CARTESIAN_POINT ( 'NONE',  ( 40.26954217208372455, -26.90384086642191619, 72.86986841596730358 ) ) ;
#15587=CARTESIAN_POINT ( 'NONE',  ( 39.02742774030102879, -26.21368208888610241, 72.26730301774232146 ) ) ;
#15588=CARTESIAN_POINT ( 'NONE',  ( 37.50301148336529167, -5.113682088886100985, 69.06206559358666652 ) ) ;
#15591=CARTESIAN_POINT ( 'NONE',  ( 37.31647492878124694, -8.303840866421912992, 72.03616607671141026 ) ) ;
#15597=CARTESIAN_POINT ( 'NONE',  ( 36.11133435605973574, -12.00384086642191583, 70.60699637195608602 ) ) ;
#15601=CARTESIAN_POINT ( 'NONE',  ( 37.69796330110504101, -15.11368208888609743, 69.66206559358661821 ) ) ;
#15607=CARTESIAN_POINT ( 'NONE',  ( 40.14115730948191185, -5.103840866421911038, 71.43714994484034264 ) ) ;
#15611=CARTESIAN_POINT ( 'NONE',  ( 36.64852494920107517, -21.41368208888610525, 70.89533451361947414 ) ) ;
#15616=CARTESIAN_POINT ( 'NONE',  ( 39.95015449827720744, -15.00384086642191228, 71.96809898377887293 ) ) ;
#15619=CARTESIAN_POINT ( 'NONE',  ( 36.64852494920107517, -19.41368208888610525, 70.89533451361947414 ) ) ;
#15621=CARTESIAN_POINT ( 'NONE',  ( 36.07789103942398867, -19.41368208888610525, 70.70992431699450265 ) ) ;
#15625=CARTESIAN_POINT ( 'NONE',  ( 37.21915885897815457, -24.20384086642190979, 71.67976084211551324 ) ) ;
#15635=CARTESIAN_POINT ( 'NONE',  ( 40.77203464402485622, -27.10384086642191903, 71.43714994484031422 ) ) ;
#15638=CARTESIAN_POINT ( 'NONE',  ( 40.77203464402485622, -0.5136820888861047818, 71.32335560751961623 ) ) ;
#15644=CARTESIAN_POINT ( 'NONE',  ( 36.64852494920107517, -18.20384086642191335, 71.86517103874048473 ) ) ;
#15652=CARTESIAN_POINT ( 'NONE',  ( 39.02742774030101458, -7.403840866421910860, 70.49320253461759478 ) ) ;
#15658=CARTESIAN_POINT ( 'NONE',  ( 37.31647492878122563, -15.31368208888610205, 70.72433947564853440 ) ) ;
#15659=CARTESIAN_POINT ( 'NONE',  ( 38.37017380507020192, -14.01368208888610312, 72.51602215082118619 ) ) ;
#15666=CARTESIAN_POINT ( 'NONE',  ( 38.93415946300897446, 1.886317911113891244, 73.09843995877332645 ) ) ;
#15667=CARTESIAN_POINT ( 'NONE',  ( 40.14115730948191185, -15.10384086642190837, 71.43714994484030001 ) ) ;
#15671=CARTESIAN_POINT ( 'NONE',  ( 37.21915885897815457, -19.41368208888609814, 71.08074471024443142 ) ) ;
#15675=( BOUNDED_CURVE ( )  B_SPLINE_CURVE ( 2, ( #13464, #9240, #25290, #17086, #22991, #21316, #22868, #3658, #9110, #1717, #11543, #9360, #25030, #25156, #5227, #7546, #1476, #7669, #5480, #5729, #23241, #5604, #13224, #19255, #13090, #23114, #7288, #11025, #15136, #7418, #20819, #1593, #15512, #5357, #21073, #9483, #23364, #21197, #17331, #3153, #15391, #18883, #11412, #16950, #3417, #11296, #3536, #19139, #21698, #45, #15893, #19764, #174, #10113, #11798, #1974, #21952, #418, #13596, #5990, #2237, #16142, #12181, #21445, #6239, #3789, #7928, #14097, #15774, #11673, #9858, #19898, #5862, #9985, #12052, #16017, #17971, #21823, #19633, #8302, #17716, #23632, #8175, #17587, #296, #4315, #19513, #23996, #21577, #13843, #11923, #23867, #1851, #2104, #4049, #23493, #17848, #8052, #23750, #6111, #13970, #4183, #9733, #20019, #25414, #2357, #10234, #18100, #7797, #13721, #15644, #3927, #8935, #6863, #18467, #22201, #16521, #4802, #24370, #12565, #12684, #4437, #4687, #2610, #16271, #24241, #8558, #20397, #671, #6746, #8689, #20524, #10493, #18724, #10748, #6613, #20654, #2728, #16659, #4938, #22331, #1058, #10619, #16784, #14229, #929, #803, #6373, #18347, #12303, #16393, #14596, #22072, #20149, #24488, #20273, #10873, #14348, #14474, #14720, #8433, #8821, #24114, #22454, #2990, #12806, #6492, #18591, #2484, #2857, #10356, #18221, #22581, #550, #4567, #12434, #17050, #23079, #16920, #19109, #10992, #22837, #24876, #7128, #11510, #1561, #19351, #13433, #14983, #3123, #5070, #15356, #7255, #1446, #5198, #24615, #15229, #9577, #24750, #9076, #17173, #3381, #5444, #18978, #15102, #3246, #12935, #13057, #9329, #3626, #22962, #20912, #21282, #11127, #1318, #1684, #23206, #6998, #17301, #14847, #9205, #20788, #22706, #13314, #24998, #1186, #21166, #18846, #5324, #13187, #21039, #11260, #7385, #19221, #3506, #11379, #9452, #25122, #5574, #7503, #2324, #15607, #2205, #9827, #15863, #9704, #11891, #3756, #7638, #11636, #4017, #17426, #23714, #23837, #1817, #3892, #6080, #6209, #9953, #13939, #259, #25380, #25256, #8025, #15481, #17554, #7763, #17814, #19732, #12, #11766, #2074, #23595, #146, #21795, #23463, #5827, #8137, #4281, #23328, #17681, #19600, #19989, #15981, #5694, #10084, #13558, #1941, #17943, #7894, #21413, #13687, #4154, #21546, #13809, #12021, #19861, #14065, #21919, #15741, #12152, #19474, #5959, #21663, #14198, #24690, #3188 ),
 .UNSPECIFIED., .F., .T. ) 
 B_SPLINE_CURVE_WITH_KNOTS ( ( 3, 2, 2, 2, 2, 2, 2, 2, 2, 2, 2, 2, 2, 2, 2, 2, 2, 2, 2, 2, 2, 2, 2, 2, 2, 2, 2, 2, 2, 2, 2, 2, 2, 2, 2, 2, 2, 2, 2, 2, 2, 2, 2, 2, 2, 2, 2, 2, 2, 2, 2, 2, 2, 2, 2, 2, 2, 2, 2, 2, 2, 2, 2, 2, 2, 2, 2, 2, 2, 2, 2, 2, 2, 2, 2, 2, 2, 2, 2, 2, 2, 2, 2, 2, 2, 2, 2, 2, 2, 2, 2, 2, 2, 2, 2, 2, 2, 2, 2, 2, 2, 2, 2, 2, 2, 2, 2, 2, 2, 2, 2, 2, 2, 2, 2, 2, 2, 2, 2, 2, 2, 2, 2, 2, 2, 2, 2, 2, 2, 2, 2, 2, 2, 2, 2, 2, 2, 2, 2, 2, 2, 2, 2, 2, 2, 2, 2, 2, 2, 2, 2, 2, 2, 3 ),
 ( 0.01547498522512168184, 0.01874999999999999931, 0.02500000000000000139, 0.03125000000000000000, 0.03749999999999999861, 0.04374999999999999722, 0.05000000000000000278, 0.05625000000000000139, 0.06250000000000000000, 0.06875000000000000555, 0.07499999999999999722, 0.08125000000000000278, 0.08749999999999999445, 0.09375000000000000000, 0.1000000000000000056, 0.1062499999999999972, 0.1125000000000000028, 0.1187499999999999944, 0.1250000000000000000, 0.1312500000000000056, 0.1375000000000000111, 0.1437499999999999889, 0.1500000000000000222, 0.1562500000000000000, 0.1625000000000000333, 0.1687500000000000111, 0.1749999999999999889, 0.1812500000000000222, 0.1875000000000000000, 0.1937500000000000333, 0.2000000000000000111, 0.2062499999999999889, 0.2125000000000000222, 0.2187500000000000000, 0.2250000000000000333, 0.2312500000000000111, 0.2374999999999999889, 0.2437500000000000222, 0.2500000000000000000, 0.2562499999999999778, 0.2625000000000000111, 0.2687499999999999889, 0.2750000000000000222, 0.2812500000000000000, 0.2874999999999999778, 0.2937500000000000111, 0.2999999999999999889, 0.3062500000000000222, 0.3125000000000000000, 0.3187499999999999778, 0.3250000000000000111, 0.3312499999999999889, 0.3375000000000000222, 0.3437500000000000000, 0.3499999999999999778, 0.3562500000000000111, 0.3624999999999999889, 0.3687500000000000222, 0.3750000000000000000, 0.3812499999999999778, 0.3875000000000000111, 0.3937499999999999889, 0.4000000000000000222, 0.4062500000000000000, 0.4124999999999999778, 0.4187500000000000111, 0.4249999999999999889, 0.4312500000000000222, 0.4375000000000000000, 0.4437499999999999778, 0.4500000000000000111, 0.4562499999999999889, 0.4625000000000000222, 0.4687500000000000000, 0.4749999999999999778, 0.4812500000000000111, 0.4874999999999999889, 0.4937500000000000222, 0.5000000000000000000, 0.5062499999999999778, 0.5124999999999999556, 0.5187500000000000444, 0.5250000000000000222, 0.5312500000000000000, 0.5374999999999999778, 0.5437499999999999556, 0.5500000000000000444, 0.5562500000000000222, 0.5625000000000000000, 0.5687499999999999778, 0.5749999999999999556, 0.5812500000000000444, 0.5875000000000000222, 0.5937500000000000000, 0.5999999999999999778, 0.6062499999999999556, 0.6125000000000000444, 0.6187500000000000222, 0.6250000000000000000, 0.6312499999999999778, 0.6374999999999999556, 0.6437500000000000444, 0.6500000000000000222, 0.6562500000000000000, 0.6624999999999999778, 0.6687499999999999556, 0.6750000000000001554, 0.6812500000000000222, 0.6875000000000000000, 0.6937499999999999778, 0.6999999999999999556, 0.7062500000000000444, 0.7125000000000000222, 0.7187500000000000000, 0.7249999999999999778, 0.7312499999999999556, 0.7375000000000000444, 0.7437500000000000222, 0.7500000000000000000, 0.7562499999999999778, 0.7624999999999999556, 0.7687500000000000444, 0.7750000000000001332, 0.7812500000000000000, 0.7874999999999999778, 0.7937499999999999556, 0.8000000000000000444, 0.8062500000000000222, 0.8125000000000000000, 0.8187499999999999778, 0.8249999999999999556, 0.8312500000000000444, 0.8375000000000000222, 0.8437500000000000000, 0.8499999999999999778, 0.8562499999999999556, 0.8625000000000000444, 0.8687500000000000222, 0.8750000000000000000, 0.8812499999999999778, 0.8874999999999999556, 0.8937500000000000444, 0.9000000000000000222, 0.9062500000000000000, 0.9124999999999999778, 0.9187499999999999556, 0.9250000000000001554, 0.9312500000000000222, 0.9375000000000000000, 0.9437499999999999778, 0.9499999999999999556, 0.9562500000000000444, 0.9625000000000000222, 0.9687500000000000000 ),
 .UNSPECIFIED. ) 
 CURVE ( )  GEOMETRIC_REPRESENTATION_ITEM ( )  RATIONAL_B_SPLINE_CURVE ( ( 0.9755846521486901679, 0.9743534988372177796, 1.000000000000000000, 0.9510565162951535312, 1.000000000000000000, 0.9510565162951535312, 1.000000000000000000, 0.9510565162951535312, 1.000000000000000000, 0.9510565162951535312, 1.000000000000000000, 0.9510565162951535312, 1.000000000000000000, 0.9510565162951535312, 1.000000000000000000, 0.9510565162951535312, 1.000000000000000000, 0.9510565162951535312, 1.000000000000000000, 0.9510565162951535312, 1.000000000000000000, 0.9510565162951535312, 1.000000000000000000, 0.9510565162951535312, 1.000000000000000000, 0.9510565162951535312, 1.000000000000000000, 0.9510565162951535312, 1.000000000000000000, 0.9510565162951535312, 1.000000000000000000, 0.9510565162951535312, 1.000000000000000000, 0.9510565162951535312, 1.000000000000000000, 0.9510565162951535312, 1.000000000000000000, 0.9510565162951535312, 1.000000000000000000, 0.9510565162951535312, 1.000000000000000000, 0.9510565162951535312, 1.000000000000000000, 0.9510565162951535312, 1.000000000000000000, 0.9510565162951535312, 1.000000000000000000, 0.9510565162951535312, 1.000000000000000000, 0.9510565162951535312, 1.000000000000000000, 0.9510565162951535312, 1.000000000000000000, 0.9510565162951535312, 1.000000000000000000, 0.9510565162951535312, 1.000000000000000000, 0.9510565162951535312, 1.000000000000000000, 0.9510565162951535312, 1.000000000000000000, 0.9510565162951535312, 1.000000000000000000, 0.9510565162951535312, 1.000000000000000000, 0.9510565162951535312, 1.000000000000000000, 0.9510565162951535312, 1.000000000000000000, 0.9510565162951535312, 1.000000000000000000, 0.9510565162951535312, 1.000000000000000000, 0.9510565162951535312, 1.000000000000000000, 0.9510565162951535312, 1.000000000000000000, 0.9510565162951535312, 1.000000000000000000, 0.9510565162951535312, 1.000000000000000000, 0.9510565162951535312, 1.000000000000000000, 0.9510565162951535312, 1.000000000000000000, 0.9510565162951535312, 1.000000000000000000, 0.9510565162951535312, 1.000000000000000000, 0.9510565162951535312, 1.000000000000000000, 0.9510565162951535312, 1.000000000000000000, 0.9510565162951535312, 1.000000000000000000, 0.9510565162951535312, 1.000000000000000000, 0.9510565162951535312, 1.000000000000000000, 0.9510565162951535312, 1.000000000000000000, 0.9510565162951535312, 1.000000000000000000, 0.9510565162951535312, 1.000000000000000000, 0.9510565162951535312, 1.000000000000000000, 0.9510565162951535312, 1.000000000000000000, 0.9510565162951535312, 1.000000000000000000, 0.9510565162951535312, 1.000000000000000000, 0.9510565162951535312, 1.000000000000000000, 0.9510565162951535312, 1.000000000000000000, 0.9510565162951535312, 1.000000000000000000, 0.9510565162951535312, 1.000000000000000000, 0.9510565162951535312, 1.000000000000000000, 0.9510565162951535312, 1.000000000000000000, 0.9510565162951535312, 1.000000000000000000, 0.9510565162951535312, 1.000000000000000000, 0.9510565162951535312, 1.000000000000000000, 0.9510565162951535312, 1.000000000000000000, 0.9510565162951535312, 1.000000000000000000, 0.9510565162951535312, 1.000000000000000000, 0.9510565162951535312, 1.000000000000000000, 0.9510565162951535312, 1.000000000000000000, 0.9510565162951535312, 1.000000000000000000, 0.9510565162951535312, 1.000000000000000000, 0.9510565162951535312, 1.000000000000000000, 0.9510565162951535312, 1.000000000000000000, 0.9510565162951535312, 1.000000000000000000, 0.9510565162951535312, 1.000000000000000000, 0.9510565162951535312, 1.000000000000000000, 0.9510565162951535312, 1.000000000000000000, 0.9510565162951535312, 1.000000000000000000, 0.9510565162951535312, 1.000000000000000000, 0.9510565162951535312, 1.000000000000000000, 0.9510565162951535312, 1.000000000000000000, 0.9510565162951535312, 1.000000000000000000, 0.9510565162951535312, 1.000000000000000000, 0.9510565162951535312, 1.000000000000000000, 0.9510565162951535312, 1.000000000000000000, 0.9510565162951535312, 1.000000000000000000, 0.9510565162951535312, 1.000000000000000000, 0.9510565162951535312, 1.000000000000000000, 0.9510565162951535312, 1.000000000000000000, 0.9510565162951535312, 1.000000000000000000, 0.9510565162951535312, 1.000000000000000000, 0.9510565162951535312, 1.000000000000000000, 0.9510565162951535312, 1.000000000000000000, 0.9510565162951535312, 1.000000000000000000, 0.9510565162951535312, 1.000000000000000000, 0.9510565162951535312, 1.000000000000000000, 0.9510565162951535312, 1.000000000000000000, 0.9510565162951535312, 1.000000000000000000, 0.9510565162951535312, 1.000000000000000000, 0.9510565162951535312, 1.000000000000000000, 0.9510565162951535312, 1.000000000000000000, 0.9510565162951535312, 1.000000000000000000, 0.9510565162951535312, 1.000000000000000000, 0.9510565162951535312, 1.000000000000000000, 0.9510565162951535312, 1.000000000000000000, 0.9510565162951535312, 1.000000000000000000, 0.9510565162951535312, 1.000000000000000000, 0.9510565162951535312, 1.000000000000000000, 0.9510565162951535312, 1.000000000000000000, 0.9510565162951535312, 1.000000000000000000, 0.9510565162951535312, 1.000000000000000000, 0.9510565162951535312, 1.000000000000000000, 0.9510565162951535312, 1.000000000000000000, 0.9510565162951535312, 1.000000000000000000, 0.9510565162951535312, 1.000000000000000000, 0.9510565162951535312, 1.000000000000000000, 0.9510565162951535312, 1.000000000000000000, 0.9510565162951535312, 1.000000000000000000, 0.9510565162951535312, 1.000000000000000000, 0.9510565162951535312, 1.000000000000000000, 0.9510565162951535312, 1.000000000000000000, 0.9510565162951535312, 1.000000000000000000, 0.9510565162951535312, 1.000000000000000000, 0.9510565162951535312, 1.000000000000000000, 0.9510565162951535312, 1.000000000000000000, 0.9510565162951535312, 1.000000000000000000, 0.9510565162951535312, 1.000000000000000000, 0.9510565162951535312, 1.000000000000000000, 0.9510565162951535312, 1.000000000000000000, 0.9510565162951535312, 1.000000000000000000, 0.9510565162951535312, 1.000000000000000000, 0.9510565162951535312, 1.000000000000000000, 0.9510565162951535312, 1.000000000000000000, 0.9510565162951535312, 1.000000000000000000, 0.9510565162951535312, 1.000000000000000000, 0.9510565162951535312, 1.000000000000000000, 0.9510565162951535312, 1.000000000000000000, 0.9510565162951535312, 1.000000000000000000, 0.9510565162951535312, 1.000000000000000000, 0.9510565162951535312, 1.000000000000000000, 0.9510565162951535312, 1.000000000000000000, 0.9510565162951535312, 1.000000000000000000, 0.9510565162951535312, 1.000000000000000000, 0.9510565162951535312, 1.000000000000000000, 0.9510565162951535312, 1.000000000000000000, 0.9510565162951535312, 1.000000000000000000, 0.9510565162951535312, 1.000000000000000000, 0.9510565162951535312, 1.000000000000000000, 0.9510565162951535312, 1.000000000000000000, 0.9510565162951535312, 1.000000000000000000, 0.9510565162951535312, 1.000000000000000000, 0.9510565162951535312, 1.000000000000000000 ) ) 
 REPRESENTATION_ITEM ( '' )  );
#15677=CARTESIAN_POINT ( 'NONE',  ( 36.80608444377001121, -13.31368208888609850, 70.35351908239860563 ) ) ;
#15680=CARTESIAN_POINT ( 'NONE',  ( 38.26194895904383486, -29.01368208888610312, 69.64448340153876416 ) ) ;
#15689=CARTESIAN_POINT ( 'NONE',  ( 38.37017380507018771, -1.603840866421912148, 69.04448340153881247 ) ) ;
#15693=CARTESIAN_POINT ( 'NONE',  ( 40.14115730948191185, -14.51368208888610667, 71.32335560751960202 ) ) ;
#15698=CARTESIAN_POINT ( 'NONE',  ( 40.26954217208371034, -12.71368208888610241, 69.89063713639258424 ) ) ;
#15710=CARTESIAN_POINT ( 'NONE',  ( 38.73920764526923932, -15.50384086642191228, 70.26206559358661252 ) ) ;
#15711=CARTESIAN_POINT ( 'NONE',  ( 36.68196826583682935, -1.613682088886104982, 71.96809898377890136 ) ) ;
#15718=CARTESIAN_POINT ( 'NONE',  ( 39.75915168707251723, -0.9038408664219161892, 72.49904802271740323 ) ) ;
#15720=CARTESIAN_POINT ( 'NONE',  ( 38.93987200065208754, -22.81368208888610383, 70.42958956619168021 ) ) ;
#15721=CARTESIAN_POINT ( 'NONE',  ( 36.89935272106204422, -1.213682088886100630, 69.52238214136768590 ) ) ;
#15727=CARTESIAN_POINT ( 'NONE',  ( 40.14115730948191185, -27.10384086642190482, 71.43714994484028580 ) ) ;
#15734=CARTESIAN_POINT ( 'NONE',  ( 38.26194895904384197, -12.60384086642191903, 73.71602215082113219 ) ) ;
#15736=CARTESIAN_POINT ( 'NONE',  ( 39.82603832034400426, -14.31368208888610916, 72.40698646996133903 ) ) ;
#15739=CARTESIAN_POINT ( 'NONE',  ( 38.26194895904383486, -25.01368208888610312, 69.64448340153876416 ) ) ;
#15741=CARTESIAN_POINT ( 'NONE',  ( 39.82603832034401137, 0.6961591335780912271, 70.35351908239861984 ) ) ;
#15745=CARTESIAN_POINT ( 'NONE',  ( 37.25202387243752611, -19.21368208888610241, 70.00779233799262613 ) ) ;
#15747=CARTESIAN_POINT ( 'NONE',  ( 37.80618814713138676, -17.70384086642190979, 69.62690120949091011 ) ) ;
#15750=CARTESIAN_POINT ( 'NONE',  ( 39.95015449827720744, -12.61368208888610454, 70.79240656858105751 ) ) ;
#15752=CARTESIAN_POINT ( 'NONE',  ( 36.98690846071097837, -23.81368208888611093, 73.30173637941817333 ) ) ;
#15756=CARTESIAN_POINT ( 'NONE',  ( 38.63098279924290068, -24.70384086642190979, 72.53360434286901182 ) ) ;
#15763=CARTESIAN_POINT ( 'NONE',  ( 40.14115730948191185, -1.103840866421911260, 71.43714994484034264 ) ) ;
#15767=CARTESIAN_POINT ( 'NONE',  ( 40.26954217208371034, -0.7136820888861000745, 69.89063713639259845 ) ) ;
#15774=CARTESIAN_POINT ( 'NONE',  ( 37.25202387243754032, -22.40384086642191619, 72.75271321436731853 ) ) ;
#15782=CARTESIAN_POINT ( 'NONE',  ( 37.25260217561390874, -8.003840866421910505, 70.97781676520604321 ) ) ;
#15789=CARTESIAN_POINT ( 'NONE',  ( 38.26194895904383486, -11.01368208888609956, 70.24448340153877268 ) ) ;
#15790=CARTESIAN_POINT ( 'NONE',  ( 38.00113996487114321, -7.913682088886101695, 72.53360434286905445 ) ) ;
#15798=CARTESIAN_POINT ( 'NONE',  ( 36.80608444377001831, -20.30384086642191477, 72.40698646996135324 ) ) ;
#15803=CARTESIAN_POINT ( 'NONE',  ( 38.37017380507020192, -16.01368208888609956, 72.51602215082118619 ) ) ;
#15807=CARTESIAN_POINT ( 'NONE',  ( 39.29254315202756231, -12.81368208888610383, 69.94417936956672577 ) ) ;
#15820=CARTESIAN_POINT ( 'NONE',  ( 38.26194895904384197, -6.603840866421920808, 73.71602215082116061 ) ) ;
#15823=CARTESIAN_POINT ( 'NONE',  ( 37.80618814713140097, -7.913682088886107913, 73.13360434286904876 ) ) ;
#15826=CARTESIAN_POINT ( 'NONE',  ( 36.11133435605973574, -17.61368208888610454, 72.15350918040385864 ) ) ;
#15835=CARTESIAN_POINT ( 'NONE',  ( 39.31564783533280405, -22.31368208888609672, 72.03616607671141026 ) ) ;
#15841=CARTESIAN_POINT ( 'NONE',  ( 39.73277004305197124, -25.40384086642191264, 69.52238214136765748 ) ) ;
#15842=CARTESIAN_POINT ( 'NONE',  ( 38.00113996487114321, -21.91368208888610170, 72.53360434286904024 ) ) ;
#15843=CARTESIAN_POINT ( 'NONE',  ( 36.11133435605973574, -5.613682088886105426, 72.15350918040385864 ) ) ;
#15846=CARTESIAN_POINT ( 'NONE',  ( 39.75915168707251723, -28.90384086642191619, 72.49904802271737481 ) ) ;
#15853=CARTESIAN_POINT ( 'NONE',  ( 36.07789103942399578, -4.203840866421913347, 72.05058123536544201 ) ) ;
#15858=CARTESIAN_POINT ( 'NONE',  ( 36.64852494920107517, -5.413682088886106136, 70.89533451361948835 ) ) ;
#15860=CARTESIAN_POINT ( 'NONE',  ( 39.82603832034401847, -24.31368208888611093, 72.40698646996131060 ) ) ;
#15863=CARTESIAN_POINT ( 'NONE',  ( 39.29254315202757653, -4.803840866421913880, 72.81632618279323310 ) ) ;
#15867=CARTESIAN_POINT ( 'NONE',  ( 38.26194895904383486, -17.01368208888610312, 69.64448340153877837 ) ) ;
#15869=CARTESIAN_POINT ( 'NONE',  ( 39.38009889167648936, -11.40384086642190908, 70.00779233799264034 ) ) ;
#15872=CARTESIAN_POINT ( 'NONE',  ( 37.69796330110504101, -13.11368208888609743, 69.66206559358661821 ) ) ;
#15874=CARTESIAN_POINT ( 'NONE',  ( 39.12911128074873801, -20.11368208888610809, 73.69843995877327814 ) ) ;
#15878=CARTESIAN_POINT ( 'NONE',  ( 39.31564783533279694, -15.30384086642191477, 70.72433947564853440 ) ) ;
#15881=CARTESIAN_POINT ( 'NONE',  ( 39.63090472924900354, -28.94648940971289264, 70.80759201118661395 ) ) ;
#15883=CARTESIAN_POINT ( 'NONE',  ( 36.29569395875881099, -20.30384086642191122, 72.77780686321128201 ) ) ;
#15885=CARTESIAN_POINT ( 'NONE',  ( 39.64521430340304420, -0.8136820888860993861, 69.45876917294177133 ) ) ;
#15893=CARTESIAN_POINT ( 'NONE',  ( 36.64852494920107517, -24.20384086642190979, 71.86517103874047052 ) ) ;
#15900=CARTESIAN_POINT ( 'NONE',  ( 37.12184278917507640, -6.103840866421912814, 71.32335560751961623 ) ) ;
#15908=CARTESIAN_POINT ( 'NONE',  ( 39.37952058850012804, -6.613682088886101873, 70.97781676520601479 ) ) ;
#15909=CARTESIAN_POINT ( 'NONE',  ( 39.37952058850012804, -2.613682088886102761, 70.97781676520601479 ) ) ;
#15916=CARTESIAN_POINT ( 'NONE',  ( 39.29254315202757653, -14.80384086642191477, 72.81632618279321889 ) ) ;
#15925=CARTESIAN_POINT ( 'NONE',  ( 39.75915168707250302, -16.71368208888609885, 70.26145752964252722 ) ) ;
#15940=CARTESIAN_POINT ( 'NONE',  ( 36.07789103942399578, -4.203840866421913347, 72.05058123536544201 ) ) ;
#15943=CARTESIAN_POINT ( 'NONE',  ( 37.33957961208646736, -9.813682088886107380, 72.81632618279323310 ) ) ;
#15947=CARTESIAN_POINT ( 'NONE',  ( 36.98690846071097837, -13.81368208888610916, 73.30173637941818754 ) ) ;
#15956=CARTESIAN_POINT ( 'NONE',  ( 37.31647492878122563, -25.31368208888610027, 70.72433947564853440 ) ) ;
#15963=CARTESIAN_POINT ( 'NONE',  ( 40.52078840805429394, -23.00384086642191761, 72.15350918040381600 ) ) ;
#15965=CARTESIAN_POINT ( 'NONE',  ( 39.95015449827720744, -28.61368208888610454, 70.79240656858104330 ) ) ;
#15973=CARTESIAN_POINT ( 'NONE',  ( 37.61123632939164452, -5.703840866421911571, 69.02690120949094421 ) ) ;
#15975=CARTESIAN_POINT ( 'NONE',  ( 39.75915168707250302, -10.71368208888609885, 70.26145752964252722 ) ) ;
#15977=CARTESIAN_POINT ( 'NONE',  ( 39.75915168707250302, -26.71368208888609885, 70.26145752964251301 ) ) ;
#15981=CARTESIAN_POINT ( 'NONE',  ( 39.75915168707251723, -0.9038408664219163002, 72.49904802271740323 ) ) ;
#15986=CARTESIAN_POINT ( 'NONE',  ( 39.41296390513587511, -27.20384086642191690, 71.08074471024438878 ) ) ;
#15987=CARTESIAN_POINT ( 'NONE',  ( 37.25202387243752611, -9.213682088886100630, 70.00779233799264034 ) ) ;
#15991=CARTESIAN_POINT ( 'NONE',  ( 39.82603832034400426, -13.30384086642190233, 70.35351908239857721 ) ) ;
#15994=CARTESIAN_POINT ( 'NONE',  ( 36.68196826583682935, -13.61368208888610454, 71.96809898377888715 ) ) ;
#15996=CARTESIAN_POINT ( 'NONE',  ( 39.12911128074873801, -16.11368208888610809, 73.69843995877327814 ) ) ;
#16000=CARTESIAN_POINT ( 'NONE',  ( 37.38336156205273397, -17.90384086642190908, 70.63227792289247020 ) ) ;
#16007=CARTESIAN_POINT ( 'NONE',  ( 36.36258059203030513, -25.90384086642191264, 69.89063713639258424 ) ) ;
#16010=CARTESIAN_POINT ( 'NONE',  ( 36.49096545463212493, -25.51368208888609956, 71.43714994484030001 ) ) ;
#16017=CARTESIAN_POINT ( 'NONE',  ( 37.80618814713138676, -21.70384086642190979, 69.62690120949091011 ) ) ;
#16027=CARTESIAN_POINT ( 'NONE',  ( 38.93987200065210175, -2.803840866421911660, 72.33091598616827866 ) ) ;
#16031=CARTESIAN_POINT ( 'NONE',  ( 38.26194895904383486, -29.01368208888610312, 69.64448340153876416 ) ) ;
#16037=CARTESIAN_POINT ( 'NONE',  ( 37.89291511884476904, -7.113682088886103649, 70.26206559358664094 ) ) ;
#16038=CARTESIAN_POINT ( 'NONE',  ( 38.73920764526925353, -6.113682088886101873, 72.49843995877331793 ) ) ;
#16047=CARTESIAN_POINT ( 'NONE',  ( 39.29254315202757653, -10.80384086642191477, 72.81632618279323310 ) ) ;
#16054=CARTESIAN_POINT ( 'NONE',  ( 39.29254315202756231, -6.813682088886101162, 69.94417936956673998 ) ) ;
#16068=CARTESIAN_POINT ( 'NONE',  ( 37.61123632939164452, -1.703840866421911571, 69.02690120949094421 ) ) ;
#16072=CARTESIAN_POINT ( 'NONE',  ( 39.38009889167650357, -6.213682088886108623, 72.75271321436733274 ) ) ;
#16076=CARTESIAN_POINT ( 'NONE',  ( 39.64521430340304420, -16.81368208888610383, 69.45876917294175712 ) ) ;
#16087=CARTESIAN_POINT ( 'NONE',  ( 37.12184278917507640, -25.51368208888609956, 71.43714994484032843 ) ) ;
#16094=CARTESIAN_POINT ( 'NONE',  ( 36.89935272106205133, -26.40384086642191974, 73.23812341099225875 ) ) ;
#16096=CARTESIAN_POINT ( 'NONE',  ( 36.80608444377001121, -27.31368208888610383, 70.35351908239857721 ) ) ;
#16101=CARTESIAN_POINT ( 'NONE',  ( 38.26194895904384197, -0.6038408664219181432, 73.71602215082116061 ) ) ;
#16106=CARTESIAN_POINT ( 'NONE',  ( 38.93415946300897446, -6.113682088886107202, 73.09843995877331224 ) ) ;
#16109=CARTESIAN_POINT ( 'NONE',  ( 38.93415946300898867, -28.11368208888610454, 73.09843995877328382 ) ) ;
#16113=CARTESIAN_POINT ( 'NONE',  ( 39.31564783533279694, -27.30384086642191477, 70.72433947564850598 ) ) ;
#16114=CARTESIAN_POINT ( 'NONE',  ( 39.38009889167650357, -14.21368208888610773, 72.75271321436731853 ) ) ;
#16119=CARTESIAN_POINT ( 'NONE',  ( 39.82603832034400426, -9.303840866421907663, 70.35351908239857721 ) ) ;
#16122=CARTESIAN_POINT ( 'NONE',  ( 36.87297107704152666, -13.71368208888610773, 72.49904802271740323 ) ) ;
#16124=CARTESIAN_POINT ( 'NONE',  ( 39.12911128074873801, -18.11368208888610454, 73.69843995877327814 ) ) ;
#16128=CARTESIAN_POINT ( 'NONE',  ( 39.41296390513587511, -21.20384086642190979, 71.08074471024441721 ) ) ;
#16133=CARTESIAN_POINT ( 'NONE',  ( 38.26194895904384197, -24.60384086642191903, 73.71602215082113219 ) ) ;
#16135=CARTESIAN_POINT ( 'NONE',  ( 40.14115730948191185, -28.51368208888610667, 71.32335560751958781 ) ) ;
#16142=CARTESIAN_POINT ( 'NONE',  ( 40.14115730948191185, -23.10384086642191548, 71.43714994484031422 ) ) ;
#16149=CARTESIAN_POINT ( 'NONE',  ( 37.21915885897815457, -2.203840866421911571, 71.67976084211552745 ) ) ;
#16159=CARTESIAN_POINT ( 'NONE',  ( 37.69225076346193504, -3.813682088886102051, 72.33091598616827866 ) ) ;
#16160=CARTESIAN_POINT ( 'NONE',  ( 39.41296390513587511, -6.413682088886100807, 71.67976084211552745 ) ) ;
#16167=CARTESIAN_POINT ( 'NONE',  ( 38.82593461698265003, -12.70384086642191512, 73.13360434286903455 ) ) ;
#16181=CARTESIAN_POINT ( 'NONE',  ( 36.80608444377001121, -9.313682088886100274, 70.35351908239861984 ) ) ;
#16196=CARTESIAN_POINT ( 'NONE',  ( 40.55423172469004101, -3.203840866421916456, 70.70992431699450265 ) ) ;
#16199=CARTESIAN_POINT ( 'NONE',  ( 36.80608444377001121, -9.313682088886100274, 70.35351908239860563 ) ) ;
#16203=CARTESIAN_POINT ( 'NONE',  ( 40.77203464402485622, -16.51368208888610667, 71.32335560751960202 ) ) ;
#16205=FACE_OUTER_BOUND ( 'NONE', #11746, .T. ) ;
#16215=CARTESIAN_POINT ( 'NONE',  ( 39.31564783533280405, -24.31368208888610383, 72.03616607671136762 ) ) ;
#16223=CARTESIAN_POINT ( 'NONE',  ( 40.77203464402485622, -21.10384086642191548, 71.43714994484032843 ) ) ;
#16225=CARTESIAN_POINT ( 'NONE',  ( 37.50301148336529167, 0.8863179111139005695, 69.06206559358666652 ) ) ;
#16235=CARTESIAN_POINT ( 'NONE',  ( 39.64521430340305841, -6.803840866421918321, 73.30173637941818754 ) ) ;
#16238=CARTESIAN_POINT ( 'NONE',  ( 36.87297107704152666, -5.713682088886105959, 72.49904802271743165 ) ) ;
#16240=CARTESIAN_POINT ( 'NONE',  ( 37.33957961208646736, -27.81368208888611093, 72.81632618279320468 ) ) ;
#16243=CARTESIAN_POINT ( 'NONE',  ( 39.24876120206129571, -22.90384086642191264, 72.12822762946747446 ) ) ;
#16244=CARTESIAN_POINT ( 'NONE',  ( 39.95015449827720744, -12.61368208888610454, 70.79240656858105751 ) ) ;
#16248=CARTESIAN_POINT ( 'NONE',  ( 38.37017380507018771, -9.603840866421908373, 69.64448340153879258 ) ) ;
#16251=CARTESIAN_POINT ( 'NONE',  ( 38.26194895904383486, -13.01368208888610134, 69.64448340153877837 ) ) ;
#16253=CARTESIAN_POINT ( 'NONE',  ( 36.29569395875879678, -15.31368208888610205, 69.98269868914867686 ) ) ;
#16257=CARTESIAN_POINT ( 'NONE',  ( 37.25260217561390874, -16.00384086642191050, 70.97781676520601479 ) ) ;
#16262=CARTESIAN_POINT ( 'NONE',  ( 39.64521430340305841, -24.80384086642191832, 73.30173637941817333 ) ) ;
#16264=CARTESIAN_POINT ( 'NONE',  ( 37.69796330110504101, -25.11368208888609388, 69.66206559358660400 ) ) ;
#16271=CARTESIAN_POINT ( 'NONE',  ( 39.29254315202757653, -16.80384086642191477, 72.81632618279321889 ) ) ;
#16275=CARTESIAN_POINT ( 'NONE',  ( 38.63098279924290068, -2.703840866421912015, 72.53360434286905445 ) ) ;
#16283=CARTESIAN_POINT ( 'NONE',  ( 38.93987200065208754, -6.813682088886101162, 70.42958956619168021 ) ) ;
#16284=CARTESIAN_POINT ( 'NONE',  ( 37.21915885897815457, -5.413682088886103472, 71.08074471024443142 ) ) ;
#16291=CARTESIAN_POINT ( 'NONE',  ( 38.26194895904384907, -12.60384086642191548, 73.11602215082116629 ) ) ;
#16298=CARTESIAN_POINT ( 'NONE',  ( 38.37017380507020192, -6.013682088886109334, 73.11602215082118050 ) ) ;
#16299=CARTESIAN_POINT ( 'NONE',  ( 39.86921189136248955, -29.10876147765123179, 71.15716630587182578 ) ) ;
#16311=CARTESIAN_POINT ( 'NONE',  ( 38.26194895904383486, -27.01368208888609956, 69.04448340153878405 ) ) ;
#16314=CARTESIAN_POINT ( 'NONE',  ( 38.26194895904383486, -21.01368208888610312, 70.24448340153875847 ) ) ;
#16318=CARTESIAN_POINT ( 'NONE',  ( 39.75915168707250302, -6.713682088886099741, 70.26145752964252722 ) ) ;
#16319=CARTESIAN_POINT ( 'NONE',  ( 37.12184278917507640, -2.103840866421912370, 71.32335560751961623 ) ) ;
#16322=CARTESIAN_POINT ( 'NONE',  ( 40.26954217208371034, -6.713682088886101518, 69.89063713639259845 ) ) ;
#16337=CARTESIAN_POINT ( 'NONE',  ( 37.50301148336529877, -20.50384086642191761, 73.69843995877327814 ) ) ;
#16338=ADVANCED_FACE ( 'NONE', ( #24322 ), #876, .F. ) ;
#16340=CARTESIAN_POINT ( 'NONE',  ( 38.37017380507020192, -26.01368208888611022, 73.11602215082115208 ) ) ;
#16351=CARTESIAN_POINT ( 'NONE',  ( 39.73277004305197124, -1.403840866421909972, 69.52238214136768590 ) ) ;
#16354=CARTESIAN_POINT ( 'NONE',  ( 36.49096545463212493, -7.513682088886102228, 71.43714994484035685 ) ) ;
#16356=CARTESIAN_POINT ( 'NONE',  ( 38.26194895904383486, -19.01368208888610312, 69.64448340153877837 ) ) ;
#16361=CARTESIAN_POINT ( 'NONE',  ( 39.51027997493896748, -23.10384086642191548, 71.43714994484032843 ) ) ;
#16362=CARTESIAN_POINT ( 'NONE',  ( 36.80608444377001121, -11.31368208888609672, 70.35351908239857721 ) ) ;
#16367=CARTESIAN_POINT ( 'NONE',  ( 39.75915168707251723, -8.903840866421916189, 72.49904802271740323 ) ) ;
#16369=CARTESIAN_POINT ( 'NONE',  ( 36.80608444377001121, -7.313682088886100274, 70.35351908239860563 ) ) ;
#16371=CARTESIAN_POINT ( 'NONE',  ( 40.26954217208371034, -14.71368208888610241, 69.89063713639258424 ) ) ;
#16375=CARTESIAN_POINT ( 'NONE',  ( 37.60469502381300799, -18.40384086642190908, 72.26730301774234988 ) ) ;
#16380=CARTESIAN_POINT ( 'NONE',  ( 39.64521430340305841, -20.80384086642191832, 73.30173637941818754 ) ) ;
#16383=CARTESIAN_POINT ( 'NONE',  ( 38.26194895904383486, -29.01368208888610312, 69.64448340153876416 ) ) ;
#16393=CARTESIAN_POINT ( 'NONE',  ( 36.64852494920107517, -14.20384086642191157, 71.86517103874048473 ) ) ;
#16396=COLOUR_RGB ( '', 0.09019608, 0.27058824, 0.51372549) ;
#16400=CARTESIAN_POINT ( 'NONE',  ( 38.82593461698265003, -28.70384086642190624, 73.13360434286902034 ) ) ;
#16405=CARTESIAN_POINT ( 'NONE',  ( 37.80618814713140097, -23.91368208888610880, 73.13360434286902034 ) ) ;
#16407=ORIENTED_EDGE ( 'NONE', *, *, #6116, .F. ) ;
#16410=CARTESIAN_POINT ( 'NONE',  ( 38.63098279924288647, -2.913682088886100363, 70.22690120949091863 ) ) ;
#16412=CARTESIAN_POINT ( 'NONE',  ( 38.37017380507020192, -6.013682088886104005, 72.51602215082118619 ) ) ;
#16419=CARTESIAN_POINT ( 'NONE',  ( 38.93415946300896024, -9.503840866421908729, 69.66206559358663242 ) ) ;
#16428=CARTESIAN_POINT ( 'NONE',  ( 37.33957961208646736, -7.813682088886109156, 72.81632618279323310 ) ) ;
#16442=CARTESIAN_POINT ( 'NONE',  ( 36.07789103942399578, -0.2038408664219136524, 72.05058123536544201 ) ) ;
#16444=CARTESIAN_POINT ( 'NONE',  ( 39.02742774030102879, -24.21368208888609885, 72.26730301774232146 ) ) ;
#16448=CARTESIAN_POINT ( 'NONE',  ( 38.82593461698262871, -4.913682088886100807, 69.62690120949091011 ) ) ;
#16449=CARTESIAN_POINT ( 'NONE',  ( 36.80608444377001831, -28.30384086642191122, 72.40698646996133903 ) ) ;
#16452=CARTESIAN_POINT ( 'NONE',  ( 36.98690846071097837, -9.813682088886107380, 73.30173637941818754 ) ) ;
#16468=CARTESIAN_POINT ( 'NONE',  ( 38.26194895904384197, -18.60384086642191548, 73.71602215082113219 ) ) ;
#16469=CARTESIAN_POINT ( 'NONE',  ( 37.80618814713140097, -23.91368208888610880, 73.13360434286902034 ) ) ;
#16476=CARTESIAN_POINT ( 'NONE',  ( 39.12911128074873801, -28.11368208888610809, 73.69843995877326392 ) ) ;
#16481=CARTESIAN_POINT ( 'NONE',  ( 36.49096545463212493, -3.513682088886103116, 71.43714994484035685 ) ) ;
#16485=CARTESIAN_POINT ( 'NONE',  ( 39.75915168707250302, -18.71368208888610241, 70.26145752964252722 ) ) ;
#16492=CARTESIAN_POINT ( 'NONE',  ( 38.93987200065210175, -26.80384086642191122, 72.33091598616823603 ) ) ;
#16493=CARTESIAN_POINT ( 'NONE',  ( 36.80608444377001121, -7.313682088886100274, 70.35351908239860563 ) ) ;
#16497=CARTESIAN_POINT ( 'NONE',  ( 36.49096545463212493, -8.103840866421908373, 71.32335560751963044 ) ) ;
#16499=CARTESIAN_POINT ( 'NONE',  ( 40.14115730948191185, -2.513682088886103116, 71.32335560751961623 ) ) ;
#16501=CARTESIAN_POINT ( 'NONE',  ( 40.33642880535524000, -14.31368208888610738, 72.77780686321126780 ) ) ;
#16506=CARTESIAN_POINT ( 'NONE',  ( 37.60469502381300799, -10.40384086642191086, 72.26730301774236409 ) ) ;
#16513=CARTESIAN_POINT ( 'NONE',  ( 39.73277004305197124, -17.40384086642191264, 69.52238214136768590 ) ) ;
#16515=CARTESIAN_POINT ( 'NONE',  ( 38.93415946300897446, -28.11368208888610098, 73.09843995877328382 ) ) ;
#16521=CARTESIAN_POINT ( 'NONE',  ( 38.37017380507018771, -17.60384086642190837, 69.64448340153877837 ) ) ;
#16528=CARTESIAN_POINT ( 'NONE',  ( 37.25260217561390874, -0.003840866421911393481, 70.97781676520604321 ) ) ;
#16531=CARTESIAN_POINT ( 'NONE',  ( 36.80608444377001121, -25.31368208888610383, 70.35351908239857721 ) ) ;
#16536=CARTESIAN_POINT ( 'NONE',  ( 37.31647492878124694, -28.30384086642191477, 72.03616607671141026 ) ) ;
#16537=CARTESIAN_POINT ( 'NONE',  ( 39.41296390513587511, -29.20384086642191335, 71.08074471024438878 ) ) ;
#16544=CARTESIAN_POINT ( 'NONE',  ( 36.49096545463212493, -8.103840866421908373, 71.32335560751963044 ) ) ;
#16554=CARTESIAN_POINT ( 'NONE',  ( 38.82593461698262871, -8.913682088886101695, 69.62690120949091011 ) ) ;
#16569=CARTESIAN_POINT ( 'NONE',  ( 37.50301148336529167, -27.11368208888610454, 69.06206559358663810 ) ) ;
#16572=CARTESIAN_POINT ( 'NONE',  ( 38.37017380507020192, -16.01368208888609956, 72.51602215082118619 ) ) ;
#16577=CARTESIAN_POINT ( 'NONE',  ( 39.38009889167650357, -2.213682088886108179, 72.75271321436733274 ) ) ;
#16578=CARTESIAN_POINT ( 'NONE',  ( 38.93987200065210175, -0.8038408664219099942, 72.33091598616827866 ) ) ;
#16581=CARTESIAN_POINT ( 'NONE',  ( 37.61123632939165873, -9.913682088886107024, 73.73360434286902887 ) ) ;
#16600=CARTESIAN_POINT ( 'NONE',  ( 40.26954217208372455, -16.90384086642191619, 72.86986841596734621 ) ) ;
#16602=CARTESIAN_POINT ( 'NONE',  ( 39.82603832034400426, -22.31368208888610738, 72.40698646996133903 ) ) ;
#16609=CARTESIAN_POINT ( 'NONE',  ( 38.26194895904384197, 1.396159133578080080, 73.71602215082117482 ) ) ;
#16614=CARTESIAN_POINT ( 'NONE',  ( 36.87297107704152666, -3.713682088886109511, 72.49904802271743165 ) ) ;
#16617=CARTESIAN_POINT ( 'NONE',  ( 36.68196826583682935, -17.61368208888610454, 71.96809898377888715 ) ) ;
#16623=CARTESIAN_POINT ( 'NONE',  ( 38.37017380507018771, -19.60384086642191193, 70.24448340153875847 ) ) ;
#16624=CARTESIAN_POINT ( 'NONE',  ( 40.14115730948191185, -4.513682088886103116, 71.32335560751961623 ) ) ;
#16628=CARTESIAN_POINT ( 'NONE',  ( 36.68196826583682935, -6.003840866421913169, 70.79240656858108593 ) ) ;
#16633=CARTESIAN_POINT ( 'NONE',  ( 39.98359781491296161, -2.413682088886103472, 71.86517103874048473 ) ) ;
#16635=CARTESIAN_POINT ( 'NONE',  ( 36.36258059203031934, -7.713682088886110400, 72.86986841596736042 ) ) ;
#16640=CARTESIAN_POINT ( 'NONE',  ( 39.24876120206129571, -14.90384086642191264, 72.12822762946747446 ) ) ;
#16647=CARTESIAN_POINT ( 'NONE',  ( 36.29569395875881099, -16.30384086642192187, 72.77780686321128201 ) ) ;
#16650=SURFACE_STYLE_USAGE ( .BOTH. , #22952 ) ;
#16651=CARTESIAN_POINT ( 'NONE',  ( 38.82593461698262871, -18.91368208888609459, 69.62690120949091011 ) ) ;
#16659=CARTESIAN_POINT ( 'NONE',  ( 39.38009889167648936, -15.40384086642190908, 70.00779233799262613 ) ) ;
#16663=CARTESIAN_POINT ( 'NONE',  ( 36.49096545463212493, -27.51368208888610312, 71.43714994484030001 ) ) ;
#16666=CARTESIAN_POINT ( 'NONE',  ( 39.82603832034400426, -23.30384086642190766, 70.35351908239857721 ) ) ;
#16669=CARTESIAN_POINT ( 'NONE',  ( 39.98359781491296161, -22.41368208888610525, 71.86517103874047052 ) ) ;
#16674=CARTESIAN_POINT ( 'NONE',  ( 38.73920764526925353, -0.1136820888861002354, 72.49843995877331793 ) ) ;
#16676=CARTESIAN_POINT ( 'NONE',  ( 39.24876120206128860, -0.7136820888861000745, 70.63227792289247020 ) ) ;
#16683=CARTESIAN_POINT ( 'NONE',  ( 38.93415946300896024, -1.503840866421908729, 69.66206559358663242 ) ) ;
#16690=CARTESIAN_POINT ( 'NONE',  ( 37.69796330110504101, -3.113682088886099208, 69.66206559358664663 ) ) ;
#16706=CARTESIAN_POINT ( 'NONE',  ( 38.93987200065208754, -14.81368208888610205, 70.42958956619168021 ) ) ;
#16710=CARTESIAN_POINT ( 'NONE',  ( 36.87297107704152666, 0.2863179111138939303, 72.49904802271743165 ) ) ;
#16711=CARTESIAN_POINT ( 'NONE',  ( 37.80618814713138676, -21.70384086642190979, 69.62690120949091011 ) ) ;
#16713=CARTESIAN_POINT ( 'NONE',  ( 35.86008812008917346, -9.513682088886103116, 71.43714994484035685 ) ) ;
#16721=CARTESIAN_POINT ( 'NONE',  ( 39.66066260159759338, -29.10876147765399224, 69.64448340153876416 ) ) ;
#16728=ORIENTED_EDGE ( 'NONE', *, *, #19356, .F. ) ;
#16731=CARTESIAN_POINT ( 'NONE',  ( 39.02088643472237806, -18.70384086642192045, 73.73360434286898624 ) ) ;
#16733=CARTESIAN_POINT ( 'NONE',  ( 39.38009889167650357, -20.21368208888610951, 72.75271321436731853 ) ) ;
#16736=FILL_AREA_STYLE ('',( #17001 ) ) ;
#16740=CARTESIAN_POINT ( 'NONE',  ( 36.29569395875879678, -25.31368208888610027, 69.98269868914866265 ) ) ;
#16745=CARTESIAN_POINT ( 'NONE',  ( 39.29254315202756231, -0.8136820888860994971, 69.94417936956673998 ) ) ;
#16747=CARTESIAN_POINT ( 'NONE',  ( 36.64852494920107517, -23.41368208888610525, 70.89533451361945993 ) ) ;
#16750=CARTESIAN_POINT ( 'NONE',  ( 38.26194895904384197, -18.60384086642190837, 72.51602215082118619 ) ) ;
#16751=CARTESIAN_POINT ( 'NONE',  ( 36.68196826583682935, -3.613682088886103205, 71.96809898377890136 ) ) ;
#16754=CLOSED_SHELL ( 'NONE', ( #3807, #21469, #16338, #24873, #9597 ) ) ;
#16755=CARTESIAN_POINT ( 'NONE',  ( 37.69796330110505522, -2.503840866421913613, 73.09843995877331224 ) ) ;
#16760=CARTESIAN_POINT ( 'NONE',  ( 37.80618814713140097, -5.913682088886107024, 73.13360434286904876 ) ) ;
#16762=CARTESIAN_POINT ( 'NONE',  ( 36.29569395875879678, -11.31368208888609850, 69.98269868914867686 ) ) ;
#16765=CARTESIAN_POINT ( 'NONE',  ( 37.69225076346193504, -9.803840866421911215, 70.42958956619168021 ) ) ;
#16770=CARTESIAN_POINT ( 'NONE',  ( 39.12911128074872380, -19.50384086642191406, 69.06206559358665231 ) ) ;
#16773=CARTESIAN_POINT ( 'NONE',  ( 36.68196826583682935, -17.61368208888610454, 71.96809898377888715 ) ) ;
#16784=CARTESIAN_POINT ( 'NONE',  ( 39.75915168707251723, -14.90384086642191264, 72.49904802271738902 ) ) ;
#16788=CARTESIAN_POINT ( 'NONE',  ( 36.68196826583682935, -23.61368208888610454, 71.96809898377887293 ) ) ;
#16790=CARTESIAN_POINT ( 'NONE',  ( 39.82603832034400426, -27.30384086642191122, 70.35351908239857721 ) ) ;
#16793=CARTESIAN_POINT ( 'NONE',  ( 39.29254315202756231, -24.81368208888610383, 69.94417936956671156 ) ) ;
#16798=CARTESIAN_POINT ( 'NONE',  ( 37.21915885897815457, -1.413682088886099253, 71.08074471024443142 ) ) ;
#16800=CARTESIAN_POINT ( 'NONE',  ( 38.63098279924288647, 1.086317911113899415, 70.22690120949094705 ) ) ;
#16807=CARTESIAN_POINT ( 'NONE',  ( 36.80608444377001831, -2.303840866421914768, 72.40698646996136745 ) ) ;
#16818=CARTESIAN_POINT ( 'NONE',  ( 39.29254315202756231, -2.813682088886101162, 69.94417936956673998 ) ) ;
#16838=CARTESIAN_POINT ( 'NONE',  ( 38.93987200065208754, -18.81368208888610027, 70.42958956619168021 ) ) ;
#16842=CARTESIAN_POINT ( 'NONE',  ( 39.82603832034400426, -0.3136820888861094336, 72.40698646996135324 ) ) ;
#16843=CARTESIAN_POINT ( 'NONE',  ( 37.25202387243754032, -26.40384086642191619, 72.75271321436730432 ) ) ;
#16847=CARTESIAN_POINT ( 'NONE',  ( 40.55423172469004811, -10.41368208888610347, 72.05058123536544201 ) ) ;
#16865=CARTESIAN_POINT ( 'NONE',  ( 36.29569395875881099, -16.30384086642192187, 72.77780686321128201 ) ) ;
#16867=CARTESIAN_POINT ( 'NONE',  ( 36.64852494920107517, -21.41368208888610525, 70.89533451361947414 ) ) ;
#16877=CARTESIAN_POINT ( 'NONE',  ( 40.52078840805428683, -26.61368208888610809, 70.60699637195608602 ) ) ;
#16880=CARTESIAN_POINT ( 'NONE',  ( 36.64852494920107517, 0.5863179111138955291, 70.89533451361948835 ) ) ;
#16882=CARTESIAN_POINT ( 'NONE',  ( 39.82603832034401847, -20.31368208888610738, 72.40698646996131060 ) ) ;
#16888=CARTESIAN_POINT ( 'NONE',  ( 39.41296390513587511, -19.20384086642191335, 71.08074471024441721 ) ) ;
#16889=CARTESIAN_POINT ( 'NONE',  ( 40.14115730948191185, -8.513682088886104893, 71.32335560751961623 ) ) ;
#16893=CARTESIAN_POINT ( 'NONE',  ( 36.80608444377001831, -6.303840866421912104, 72.40698646996136745 ) ) ;
#16895=CARTESIAN_POINT ( 'NONE',  ( 36.80608444377001121, -5.313682088886100274, 70.35351908239860563 ) ) ;
#16897=CARTESIAN_POINT ( 'NONE',  ( 39.64521430340304420, -6.813682088886101162, 69.45876917294177133 ) ) ;
#16901=CARTESIAN_POINT ( 'NONE',  ( 38.00113996487112189, -9.703840866421911571, 70.22690120949091863 ) ) ;
#16909=CARTESIAN_POINT ( 'NONE',  ( 40.26954217208372455, -16.90384086642191619, 72.86986841596734621 ) ) ;
#16913=CARTESIAN_POINT ( 'NONE',  ( 37.33957961208646736, -17.81368208888611093, 72.81632618279321889 ) ) ;
#16920=CARTESIAN_POINT ( 'NONE',  ( 39.38009889167648936, -11.40384086642190908, 70.00779233799264034 ) ) ;
#16923=CARTESIAN_POINT ( 'NONE',  ( 37.25202387243752611, -25.21368208888610241, 70.00779233799262613 ) ) ;
#16926=CARTESIAN_POINT ( 'NONE',  ( 38.37017380507018771, -27.60384086642191193, 69.64448340153876416 ) ) ;
#16927=CARTESIAN_POINT ( 'NONE',  ( 39.75145154291258365, -29.60384086642190837, 69.64448340153876416 ) ) ;
#16928=CARTESIAN_POINT ( 'NONE',  ( 39.29254315202756231, -22.81368208888610027, 69.94417936956672577 ) ) ;
#16933=CARTESIAN_POINT ( 'NONE',  ( 39.51027997493896748, -0.5136820888861012291, 71.32335560751961623 ) ) ;
#16940=CARTESIAN_POINT ( 'NONE',  ( 38.93415946300896024, -7.503840866421907840, 69.66206559358663242 ) ) ;
#16948=CARTESIAN_POINT ( 'NONE',  ( 39.29254315202756231, 1.186317911113898838, 69.94417936956675419 ) ) ;
#16950=CARTESIAN_POINT ( 'NONE',  ( 39.75915168707251723, -24.90384086642191619, 72.49904802271737481 ) ) ;
#16966=CARTESIAN_POINT ( 'NONE',  ( 38.26194895904383486, -19.01368208888609956, 70.24448340153875847 ) ) ;
#16972=CARTESIAN_POINT ( 'NONE',  ( 36.80608444377001121, -3.313682088886100718, 70.35351908239860563 ) ) ;
#16973=CARTESIAN_POINT ( 'NONE',  ( 39.38009889167648936, -25.40384086642190908, 70.00779233799262613 ) ) ;
#16978=CARTESIAN_POINT ( 'NONE',  ( 38.26194895904383486, 0.9863179111139001032, 69.04448340153882668 ) ) ;
#16996=CARTESIAN_POINT ( 'NONE',  ( 38.37017380507018771, -19.60384086642191193, 69.04448340153878405 ) ) ;
#16999=CARTESIAN_POINT ( 'NONE',  ( 38.93415946300897446, -20.11368208888610809, 73.09843995877329803 ) ) ;
#17001=FILL_AREA_STYLE_COLOUR ( '', #16396 ) ;
#17006=CARTESIAN_POINT ( 'NONE',  ( 39.02088643472237095, -24.91368208888610170, 69.02690120949091579 ) ) ;
#17010=CARTESIAN_POINT ( 'NONE',  ( 37.69796330110504101, -1.113682088886101207, 69.66206559358663242 ) ) ;
#17013=CARTESIAN_POINT ( 'NONE',  ( 37.69796330110504101, -11.11368208888610276, 69.66206559358664663 ) ) ;
#17017=CARTESIAN_POINT ( 'NONE',  ( 38.26194895904384907, 1.396159133578083633, 73.11602215082119471 ) ) ;
#17018=CARTESIAN_POINT ( 'NONE',  ( 37.21915885897815457, -18.20384086642190979, 71.67976084211552745 ) ) ;
#17019=CARTESIAN_POINT ( 'NONE',  ( 37.33957961208646736, -3.813682088886109156, 72.81632618279323310 ) ) ;
#17025=CARTESIAN_POINT ( 'NONE',  ( 39.98359781491296161, -3.203840866421912903, 70.89533451361947414 ) ) ;
#17028=CARTESIAN_POINT ( 'NONE',  ( 37.80618814713140097, -1.913682088886106136, 73.13360434286904876 ) ) ;
#17030=CARTESIAN_POINT ( 'NONE',  ( 36.89935272106204422, -9.213682088886100630, 69.52238214136768590 ) ) ;
#17033=CARTESIAN_POINT ( 'NONE',  ( 38.73920764526923932, -5.503840866421911393, 70.26206559358664094 ) ) ;
#17039=CARTESIAN_POINT ( 'NONE',  ( 40.33642880535521869, -19.30384086642191477, 69.98269868914866265 ) ) ;
#17043=CARTESIAN_POINT ( 'NONE',  ( 39.75915168707250302, -18.71368208888610241, 70.26145752964251301 ) ) ;
#17050=CARTESIAN_POINT ( 'NONE',  ( 38.37017380507018771, -11.60384086642190660, 69.64448340153879258 ) ) ;
#17054=CARTESIAN_POINT ( 'NONE',  ( 39.38009889167650357, -24.21368208888610596, 72.75271321436730432 ) ) ;
#17060=CARTESIAN_POINT ( 'NONE',  ( 38.26194895904384907, -26.60384086642191548, 73.11602215082115208 ) ) ;
#17063=CARTESIAN_POINT ( 'NONE',  ( 38.37017380507020192, -18.01368208888611022, 73.11602215082116629 ) ) ;
#17065=CARTESIAN_POINT ( 'NONE',  ( 39.64521430340305841, -0.8038408664219169886, 73.30173637941818754 ) ) ;
#17069=CARTESIAN_POINT ( 'NONE',  ( 38.73920764526923932, -29.50384086642191050, 70.26206559358661252 ) ) ;
#17077=CARTESIAN_POINT ( 'NONE',  ( 39.82603832034400426, -3.303840866421908995, 70.35351908239857721 ) ) ;
#17084=CARTESIAN_POINT ( 'NONE',  ( 37.80618814713140097, 0.08631791111389161553, 73.13360434286904876 ) ) ;
#17086=CARTESIAN_POINT ( 'NONE',  ( 39.75915168707251723, -28.90384086642191619, 72.49904802271737481 ) ) ;
#17100=CARTESIAN_POINT ( 'NONE',  ( 38.26194895904383486, -15.01368208888610134, 70.24448340153875847 ) ) ;
#17107=CARTESIAN_POINT ( 'NONE',  ( 38.93415946300896024, -25.50384086642190340, 69.66206559358660400 ) ) ;
#17109=CARTESIAN_POINT ( 'NONE',  ( 36.29569395875879678, -1.313682088886099830, 69.98269868914869107 ) ) ;
#17126=CARTESIAN_POINT ( 'NONE',  ( 38.26194895904384197, -10.60384086642192081, 73.71602215082116061 ) ) ;
#17129=CARTESIAN_POINT ( 'NONE',  ( 39.98359781491296161, -16.41368208888610525, 71.86517103874047052 ) ) ;
#17133=CARTESIAN_POINT ( 'NONE',  ( 39.64521430340304420, -18.81368208888610027, 69.45876917294175712 ) ) ;
#17142=CARTESIAN_POINT ( 'NONE',  ( 37.60469502381300799, -16.40384086642191264, 72.26730301774234988 ) ) ;
#17143=CARTESIAN_POINT ( 'NONE',  ( 39.38009889167650357, 1.786317911113891821, 72.75271321436734695 ) ) ;
#17150=CARTESIAN_POINT ( 'NONE',  ( 37.69796330110505522, -0.5038408664219152788, 73.09843995877331224 ) ) ;
#17152=CARTESIAN_POINT ( 'NONE',  ( 36.49096545463212493, 0.4863179111138959954, 71.43714994484035685 ) ) ;
#17153=CARTESIAN_POINT ( 'NONE',  ( 40.26954217208371034, -10.71368208888610063, 69.89063713639259845 ) ) ;
#17157=CARTESIAN_POINT ( 'NONE',  ( 39.37952058850012804, -3.003840866421910505, 71.78268878715392987 ) ) ;
#17164=CARTESIAN_POINT ( 'NONE',  ( 39.73277004305197124, -7.403840866421910860, 69.52238214136768590 ) ) ;
#17167=CARTESIAN_POINT ( 'NONE',  ( 39.29254315202756231, -20.81368208888610027, 69.94417936956672577 ) ) ;
#17173=CARTESIAN_POINT ( 'NONE',  ( 39.98359781491296161, -9.203840866421911571, 70.89533451361947414 ) ) ;
#17176=CARTESIAN_POINT ( 'NONE',  ( 39.82603832034400426, -24.31368208888611093, 72.40698646996131060 ) ) ;
#17180=CARTESIAN_POINT ( 'NONE',  ( 39.98359781491296161, -27.20384086642191335, 70.89533451361944572 ) ) ;
#17182=CARTESIAN_POINT ( 'NONE',  ( 36.80608444377001121, -21.31368208888610027, 70.35351908239857721 ) ) ;
#17184=CARTESIAN_POINT ( 'NONE',  ( 38.26194895904384197, -0.6038408664219181432, 73.71602215082116061 ) ) ;
#17188=CARTESIAN_POINT ( 'NONE',  ( 37.69225076346193504, -25.80384086642191477, 70.42958956619166599 ) ) ;
#17195=CARTESIAN_POINT ( 'NONE',  ( 37.25202387243754032, -6.403840866421914413, 72.75271321436733274 ) ) ;
#17205=CARTESIAN_POINT ( 'NONE',  ( 37.33957961208646736, -1.813682088886107380, 72.81632618279323310 ) ) ;
#17223=CARTESIAN_POINT ( 'NONE',  ( 38.37017380507020192, -10.01368208888610312, 72.51602215082118619 ) ) ;
#17224=CARTESIAN_POINT ( 'NONE',  ( 37.69225076346193504, -9.813682088886100274, 72.33091598616827866 ) ) ;
#17228=CARTESIAN_POINT ( 'NONE',  ( 39.82603832034400426, 1.686317911113891732, 72.40698646996136745 ) ) ;
#17229=CARTESIAN_POINT ( 'NONE',  ( 36.49096545463212493, -22.10384086642191548, 71.32335560751961623 ) ) ;
#17243=MANIFOLD_SOLID_BREP ( 'Stock-MAS-155-1', #16754 ) ;
#17247=CARTESIAN_POINT ( 'NONE',  ( 37.61123632939164452, -13.70384086642191157, 69.02690120949091579 ) ) ;
#17250=CARTESIAN_POINT ( 'NONE',  ( 37.69796330110504101, -15.11368208888609743, 69.66206559358661821 ) ) ;
#17255=CARTESIAN_POINT ( 'NONE',  ( 40.52078840805428683, -20.61368208888610454, 70.60699637195608602 ) ) ;
#17266=CARTESIAN_POINT ( 'NONE',  ( 38.63098279924290068, -10.70384086642191335, 72.53360434286905445 ) ) ;
#17267=CARTESIAN_POINT ( 'NONE',  ( 39.29254315202756231, 1.186317911113898838, 69.94417936956675419 ) ) ;
#17275=CARTESIAN_POINT ( 'NONE',  ( 36.68196826583682935, -0.003840866421911393047, 70.79240656858108593 ) ) ;
#17276=CARTESIAN_POINT ( 'NONE',  ( 38.82593461698262871, -0.9136820888861022505, 69.62690120949091011 ) ) ;
#17277=CARTESIAN_POINT ( 'NONE',  ( 36.36258059203031934, -5.713682088886106847, 72.86986841596736042 ) ) ;
#17281=CARTESIAN_POINT ( 'NONE',  ( 38.93987200065210175, -6.803840866421912104, 72.33091598616827866 ) ) ;
#17288=CARTESIAN_POINT ( 'NONE',  ( 39.73277004305197124, -9.403840866421907307, 69.52238214136768590 ) ) ;
#17294=CARTESIAN_POINT ( 'NONE',  ( 37.33957961208646736, -15.81368208888610916, 72.81632618279321889 ) ) ;
#17301=CARTESIAN_POINT ( 'NONE',  ( 39.38009889167648936, -7.403840866421908196, 70.00779233799264034 ) ) ;
#17305=CARTESIAN_POINT ( 'NONE',  ( 36.49096545463212493, -15.51368208888610667, 71.43714994484034264 ) ) ;
#17307=CARTESIAN_POINT ( 'NONE',  ( 40.14115730948191185, -21.10384086642191193, 71.43714994484030001 ) ) ;
#17310=CARTESIAN_POINT ( 'NONE',  ( 38.82593461698262871, -18.91368208888609459, 69.62690120949091011 ) ) ;
#17312=CARTESIAN_POINT ( 'NONE',  ( 37.50301148336529167, -25.11368208888610454, 69.06206559358663810 ) ) ;
#17317=CARTESIAN_POINT ( 'NONE',  ( 37.21915885897815457, -26.20384086642190979, 71.67976084211551324 ) ) ;
#17320=CARTESIAN_POINT ( 'NONE',  ( 39.60857575084318682, -28.82472769709708516, 70.68354409430698126 ) ) ;
#17323=CARTESIAN_POINT ( 'NONE',  ( 35.86008812008917346, -26.10384086642191903, 71.32335560751960202 ) ) ;
#17331=CARTESIAN_POINT ( 'NONE',  ( 39.38009889167648936, -25.40384086642190908, 70.00779233799262613 ) ) ;
#17339=CARTESIAN_POINT ( 'NONE',  ( 37.89291511884479036, -8.503840866421912281, 72.49843995877331793 ) ) ;
#17346=CARTESIAN_POINT ( 'NONE',  ( 37.38336156205274818, -13.71368208888610241, 72.12822762946750288 ) ) ;
#17347=CARTESIAN_POINT ( 'NONE',  ( 39.24876120206128860, -12.71368208888610241, 70.63227792289245599 ) ) ;
#17353=CARTESIAN_POINT ( 'NONE',  ( 37.69796330110505522, -20.50384086642191050, 73.09843995877329803 ) ) ;
#17356=CARTESIAN_POINT ( 'NONE',  ( 37.25260217561390874, -15.61368208888610276, 71.78268878715392987 ) ) ;
#17374=CARTESIAN_POINT ( 'NONE',  ( 36.11133435605973574, -14.00384086642191583, 70.60699637195608602 ) ) ;
#17376=CARTESIAN_POINT ( 'NONE',  ( 40.14115730948191185, -12.51368208888610489, 71.32335560751960202 ) ) ;
#17383=CARTESIAN_POINT ( 'NONE',  ( 38.26194895904383486, -23.01368208888610312, 69.04448340153878405 ) ) ;
#17387=CARTESIAN_POINT ( 'NONE',  ( 38.37017380507020192, 1.986317911113890444, 73.11602215082119471 ) ) ;
#17394=CARTESIAN_POINT ( 'NONE',  ( 39.31564783533279694, -15.30384086642191477, 70.72433947564853440 ) ) ;
#17395=CARTESIAN_POINT ( 'NONE',  ( 40.14115730948191185, -0.5136820888861047818, 71.32335560751961623 ) ) ;
#17402=CARTESIAN_POINT ( 'NONE',  ( 40.55423172469004101, -27.20384086642191690, 70.70992431699446001 ) ) ;
#17404=CARTESIAN_POINT ( 'NONE',  ( 37.80618814713140097, 0.08631791111389161553, 73.13360434286904876 ) ) ;
#17405=CARTESIAN_POINT ( 'NONE',  ( 40.52078840805428683, -0.6136820888861042045, 70.60699637195608602 ) ) ;
#17408=CARTESIAN_POINT ( 'NONE',  ( 39.41296390513587511, -3.203840866421912903, 71.08074471024443142 ) ) ;
#17410=ORIENTED_EDGE ( 'NONE', *, *, #11243, .F. ) ;
#17416=CARTESIAN_POINT ( 'NONE',  ( 40.52078840805429394, -13.00384086642191761, 72.15350918040381600 ) ) ;
#17419=CARTESIAN_POINT ( 'NONE',  ( 39.75915168707250302, -16.71368208888609885, 70.26145752964251301 ) ) ;
#17426=CARTESIAN_POINT ( 'NONE',  ( 36.49096545463212493, -4.103840866421911038, 71.32335560751963044 ) ) ;
#17430=CARTESIAN_POINT ( 'NONE',  ( 37.25202387243752611, -21.21368208888610241, 70.00779233799262613 ) ) ;
#17435=CARTESIAN_POINT ( 'NONE',  ( 36.49096545463212493, -16.10384086642191548, 71.32335560751961623 ) ) ;
#17439=CARTESIAN_POINT ( 'NONE',  ( 37.25202387243752611, -15.21368208888610063, 70.00779233799262613 ) ) ;
#17441=CARTESIAN_POINT ( 'NONE',  ( 40.33642880535524000, -24.31368208888611093, 72.77780686321125359 ) ) ;
#17446=CARTESIAN_POINT ( 'NONE',  ( 37.38336156205273397, -25.90384086642191264, 70.63227792289245599 ) ) ;
#17455=CARTESIAN_POINT ( 'NONE',  ( 36.87297107704149823, 0.09615913357809147133, 70.26145752964255564 ) ) ;
#17474=CARTESIAN_POINT ( 'NONE',  ( 38.93987200065210175, -6.803840866421912104, 72.33091598616827866 ) ) ;
#17481=CARTESIAN_POINT ( 'NONE',  ( 37.89291511884476904, -13.11368208888610454, 70.26206559358661252 ) ) ;
#17483=CARTESIAN_POINT ( 'NONE',  ( 37.25260217561390874, -13.61368208888610098, 71.78268878715392987 ) ) ;
#17491=CARTESIAN_POINT ( 'NONE',  ( 38.37017380507018771, -17.60384086642190837, 69.64448340153877837 ) ) ;
#17494=CARTESIAN_POINT ( 'NONE',  ( 37.69225076346193504, -17.81368208888610383, 72.33091598616826445 ) ) ;
#17497=CARTESIAN_POINT ( 'NONE',  ( 37.25202387243752611, -11.21368208888610241, 70.00779233799262613 ) ) ;
#17510=CARTESIAN_POINT ( 'NONE',  ( 40.52078840805429394, -13.00384086642191761, 72.15350918040381600 ) ) ;
#17513=CARTESIAN_POINT ( 'NONE',  ( 36.87297107704152666, -15.71368208888610596, 72.49904802271740323 ) ) ;
#17517=CARTESIAN_POINT ( 'NONE',  ( 36.29569395875879678, -21.31368208888610027, 69.98269868914867686 ) ) ;
#17528=CARTESIAN_POINT ( 'NONE',  ( 37.25260217561390874, -12.00384086642191228, 70.97781676520601479 ) ) ;
#17529=CARTESIAN_POINT ( 'NONE',  ( 39.75915168707250302, 1.286317911113898260, 70.26145752964255564 ) ) ;
#17536=CARTESIAN_POINT ( 'NONE',  ( 39.98359781491296161, 0.7961591335780872081, 70.89533451361948835 ) ) ;
#17537=CARTESIAN_POINT ( 'NONE',  ( 39.41296390513587511, -26.41368208888610170, 71.67976084211548482 ) ) ;
#17539=CARTESIAN_POINT ( 'NONE',  ( 36.29569395875879678, -5.313682088886097610, 69.98269868914869107 ) ) ;
#17542=CARTESIAN_POINT ( 'NONE',  ( 39.31564783533279694, -5.303840866421911215, 70.72433947564853440 ) ) ;
#17547=CARTESIAN_POINT ( 'NONE',  ( 39.73277004305197124, -11.40384086642191086, 69.52238214136768590 ) ) ;
#17550=CARTESIAN_POINT ( 'NONE',  ( 38.82593461698262871, -10.91368208888609992, 69.62690120949091011 ) ) ;
#17554=CARTESIAN_POINT ( 'NONE',  ( 38.82593461698264292, -2.703840866421916012, 73.13360434286904876 ) ) ;
#17557=CARTESIAN_POINT ( 'NONE',  ( 37.80618814713140097, -17.91368208888609814, 73.13360434286903455 ) ) ;
#17560=CARTESIAN_POINT ( 'NONE',  ( 39.29254315202757653, -18.80384086642191477, 72.81632618279321889 ) ) ;
#17562=CARTESIAN_POINT ( 'NONE',  ( 38.37017380507020192, -20.01368208888610667, 73.11602215082116629 ) ) ;
#17564=CARTESIAN_POINT ( 'NONE',  ( 36.36258059203031934, -19.71368208888610951, 72.86986841596736042 ) ) ;
#17568=CARTESIAN_POINT ( 'NONE',  ( 38.37017380507018771, -27.60384086642191548, 70.24448340153875847 ) ) ;
#17575=CARTESIAN_POINT ( 'NONE',  ( 36.98690846071097127, -27.80384086642191477, 69.45876917294174291 ) ) ;
#17578=CARTESIAN_POINT ( 'NONE',  ( 40.52078840805428683, -0.6136820888861042045, 70.60699637195608602 ) ) ;
#17587=CARTESIAN_POINT ( 'NONE',  ( 39.75915168707251723, -20.90384086642190908, 72.49904802271738902 ) ) ;
#17594=CARTESIAN_POINT ( 'NONE',  ( 38.00113996487112189, -7.703840866421914235, 70.22690120949091863 ) ) ;
#17600=CARTESIAN_POINT ( 'NONE',  ( 39.31564783533280405, -14.31368208888609850, 72.03616607671141026 ) ) ;
#17603=CARTESIAN_POINT ( 'NONE',  ( 38.37017380507020192, -8.013682088886101340, 72.51602215082118619 ) ) ;
#17609=CARTESIAN_POINT ( 'NONE',  ( 39.75915168707250302, 1.286317911113898260, 70.26145752964255564 ) ) ;
#17610=CARTESIAN_POINT ( 'NONE',  ( 37.69796330110505522, -16.50384086642191761, 73.09843995877329803 ) ) ;
#17614=CARTESIAN_POINT ( 'NONE',  ( 39.24876120206128860, -16.71368208888610241, 70.63227792289245599 ) ) ;
#17620=CARTESIAN_POINT ( 'NONE',  ( 37.69796330110504101, -17.11368208888610098, 69.66206559358663242 ) ) ;
#17626=FACE_OUTER_BOUND ( 'NONE', #17727, .T. ) ;
#17635=CARTESIAN_POINT ( 'NONE',  ( 39.02088643472237806, -8.703840866421918676, 73.73360434286902887 ) ) ;
#17639=CARTESIAN_POINT ( 'NONE',  ( 36.49096545463212493, -15.51368208888610667, 71.43714994484034264 ) ) ;
#17644=CARTESIAN_POINT ( 'NONE',  ( 36.98690846071097837, -23.81368208888611093, 73.30173637941817333 ) ) ;
#17652=CARTESIAN_POINT ( 'NONE',  ( 37.31647492878124694, -12.30384086642191299, 72.03616607671141026 ) ) ;
#17653=CARTESIAN_POINT ( 'NONE',  ( 39.98359781491296161, -2.413682088886103472, 71.86517103874048473 ) ) ;
#17661=CARTESIAN_POINT ( 'NONE',  ( 39.29254315202757653, -0.8038408664219134359, 72.81632618279323310 ) ) ;
#17664=CARTESIAN_POINT ( 'NONE',  ( 37.69225076346193504, -21.81368208888610027, 72.33091598616826445 ) ) ;
#17665=CARTESIAN_POINT ( 'NONE',  ( 36.11133435605973574, -1.613682088886104982, 72.15350918040385864 ) ) ;
#17668=CARTESIAN_POINT ( 'NONE',  ( 39.38009889167648936, -29.40384086642190908, 70.00779233799262613 ) ) ;
#17673=CARTESIAN_POINT ( 'NONE',  ( 39.64521430340305841, -8.803840866421916544, 73.30173637941818754 ) ) ;
#17676=CARTESIAN_POINT ( 'NONE',  ( 36.64852494920107517, -15.41368208888610525, 70.89533451361947414 ) ) ;
#17681=CARTESIAN_POINT ( 'NONE',  ( 39.98359781491296161, -1.203840866421911127, 70.89533451361947414 ) ) ;
#17684=CARTESIAN_POINT ( 'NONE',  ( 36.87297107704152666, -21.71368208888610951, 72.49904802271740323 ) ) ;
#17687=CARTESIAN_POINT ( 'NONE',  ( 38.82593461698265003, -20.70384086642191335, 73.13360434286903455 ) ) ;
#17691=CARTESIAN_POINT ( 'NONE',  ( 37.80618814713140097, -13.91368208888610347, 73.13360434286903455 ) ) ;
#17693=CARTESIAN_POINT ( 'NONE',  ( 40.26954217208371034, -20.71368208888610596, 69.89063713639258424 ) ) ;
#17697=CARTESIAN_POINT ( 'NONE',  ( 39.37952058850012804, -25.00384086642191406, 71.78268878715390144 ) ) ;
#17705=CARTESIAN_POINT ( 'NONE',  ( 40.33642880535521869, -27.30384086642191477, 69.98269868914864844 ) ) ;
#17708=CARTESIAN_POINT ( 'NONE',  ( 40.33642880535524000, -0.3136820888861093781, 72.77780686321128201 ) ) ;
#17716=CARTESIAN_POINT ( 'NONE',  ( 39.98359781491296161, -21.20384086642190979, 70.89533451361945993 ) ) ;
#17723=CARTESIAN_POINT ( 'NONE',  ( 39.41296390513587511, -3.203840866421912903, 71.08074471024443142 ) ) ;
#17727=EDGE_LOOP ( 'NONE', ( #19576, #15113, #21213, #5475, #869 ) ) ;
#17730=CARTESIAN_POINT ( 'NONE',  ( 39.37952058850012804, -14.61368208888610098, 70.97781676520601479 ) ) ;
#17731=CARTESIAN_POINT ( 'NONE',  ( 38.93987200065208754, -8.813682088886096722, 70.42958956619168021 ) ) ;
#17738=CARTESIAN_POINT ( 'NONE',  ( 39.95015449827720744, -19.00384086642191406, 71.96809898377887293 ) ) ;
#17742=CARTESIAN_POINT ( 'NONE',  ( 39.02742774030102879, -20.21368208888610241, 72.26730301774234988 ) ) ;
#17747=CARTESIAN_POINT ( 'NONE',  ( 39.38009889167650357, -14.21368208888610773, 72.75271321436731853 ) ) ;
#17762=CARTESIAN_POINT ( 'NONE',  ( 40.33642880535521869, -5.303840866421911215, 69.98269868914867686 ) ) ;
#17768=CARTESIAN_POINT ( 'NONE',  ( 37.69796330110504101, -11.11368208888610276, 69.66206559358663242 ) ) ;
#17773=CARTESIAN_POINT ( 'NONE',  ( 40.77203464402485622, -12.51368208888610667, 71.32335560751960202 ) ) ;
#17784=CARTESIAN_POINT ( 'NONE',  ( 37.25260217561390874, -14.00384086642191050, 70.97781676520601479 ) ) ;
#17785=CARTESIAN_POINT ( 'NONE',  ( 39.24876120206128860, -22.71368208888610241, 70.63227792289245599 ) ) ;
#17791=CARTESIAN_POINT ( 'NONE',  ( 39.64521430340305841, -24.80384086642191832, 73.30173637941817333 ) ) ;
#17792=CARTESIAN_POINT ( 'NONE',  ( 39.31564783533280405, -22.31368208888609672, 72.03616607671141026 ) ) ;
#17793=CARTESIAN_POINT ( 'NONE',  ( 38.37017380507020192, -4.013682088886107557, 73.71602215082116061 ) ) ;
#17798=CARTESIAN_POINT ( 'NONE',  ( 38.37017380507018771, -29.60384086642190837, 69.64448340153876416 ) ) ;
#17804=CARTESIAN_POINT ( 'NONE',  ( 36.11133435605973574, -6.003840866421917610, 70.60699637195612866 ) ) ;
#17807=CARTESIAN_POINT ( 'NONE',  ( 39.75915168707250302, -12.71368208888610063, 70.26145752964251301 ) ) ;
#17811=CARTESIAN_POINT ( 'NONE',  ( 37.80618814713140097, -23.91368208888610880, 73.13360434286902034 ) ) ;
#17814=CARTESIAN_POINT ( 'NONE',  ( 37.69796330110505522, -2.503840866421913613, 73.09843995877331224 ) ) ;
#17817=CARTESIAN_POINT ( 'NONE',  ( 38.82593461698262871, -20.91368208888609459, 69.62690120949091011 ) ) ;
#17820=CARTESIAN_POINT ( 'NONE',  ( 38.37017380507018771, -17.60384086642190837, 69.64448340153877837 ) ) ;
#17823=CARTESIAN_POINT ( 'NONE',  ( 36.49096545463212493, -11.51368208888609956, 71.43714994484034264 ) ) ;
#17825=CARTESIAN_POINT ( 'NONE',  ( 38.37017380507020192, -20.01368208888611022, 73.71602215082113219 ) ) ;
#17829=CARTESIAN_POINT ( 'NONE',  ( 37.89291511884479036, -18.50384086642191406, 72.49843995877330372 ) ) ;
#17835=CARTESIAN_POINT ( 'NONE',  ( 36.29569395875881099, -22.30384086642192187, 72.77780686321128201 ) ) ;
#17838=CARTESIAN_POINT ( 'NONE',  ( 39.64521430340304420, -4.813682088886099386, 69.45876917294177133 ) ) ;
#17848=CARTESIAN_POINT ( 'NONE',  ( 38.37017380507018771, -19.60384086642191193, 69.64448340153877837 ) ) ;
#17855=CARTESIAN_POINT ( 'NONE',  ( 37.60469502381300799, -8.403840866421912636, 72.26730301774236409 ) ) ;
#17864=CARTESIAN_POINT ( 'NONE',  ( 38.00113996487114321, -7.913682088886101695, 72.53360434286905445 ) ) ;
#17865=CARTESIAN_POINT ( 'NONE',  ( 38.93987200065208754, -4.813682088886099386, 70.42958956619168021 ) ) ;
#17872=CARTESIAN_POINT ( 'NONE',  ( 36.68196826583682935, -20.00384086642191050, 70.79240656858107172 ) ) ;
#17881=CARTESIAN_POINT ( 'NONE',  ( 36.49096545463212493, -11.51368208888610312, 71.43714994484034264 ) ) ;
#17897=CARTESIAN_POINT ( 'NONE',  ( 39.73277004305197124, -1.403840866421909972, 69.52238214136768590 ) ) ;
#17900=CARTESIAN_POINT ( 'NONE',  ( 36.49096545463212493, -7.513682088886102228, 71.43714994484035685 ) ) ;
#17903=CARTESIAN_POINT ( 'NONE',  ( 38.26194895904383486, -17.01368208888610312, 69.04448340153878405 ) ) ;
#17916=CARTESIAN_POINT ( 'NONE',  ( 37.60469502381300089, -27.21368208888609885, 70.49320253461758057 ) ) ;
#17923=CARTESIAN_POINT ( 'NONE',  ( 36.11133435605973574, -26.00384086642192116, 70.60699637195608602 ) ) ;
#17924=CARTESIAN_POINT ( 'NONE',  ( 38.82593461698262871, -26.91368208888610170, 69.62690120949091011 ) ) ;
#17927=CARTESIAN_POINT ( 'NONE',  ( 38.00113996487112189, 0.2961591335780902612, 70.22690120949094705 ) ) ;
#17932=CARTESIAN_POINT ( 'NONE',  ( 39.12911128074872380, -3.503840866421911393, 69.06206559358666652 ) ) ;
#17936=CARTESIAN_POINT ( 'NONE',  ( 39.75915168707250302, -4.713682088886100630, 70.26145752964252722 ) ) ;
#17939=CARTESIAN_POINT ( 'NONE',  ( 39.82603832034401847, -28.31368208888610738, 72.40698646996131060 ) ) ;
#17943=CARTESIAN_POINT ( 'NONE',  ( 37.25202387243754032, -0.4038408664219159117, 72.75271321436733274 ) ) ;
#17945=CARTESIAN_POINT ( 'NONE',  ( 37.12184278917507640, -28.10384086642191193, 71.32335560751960202 ) ) ;
#17946=CARTESIAN_POINT ( 'NONE',  ( 36.49096545463212493, -9.513682088886101340, 71.43714994484035685 ) ) ;
#17949=CARTESIAN_POINT ( 'NONE',  ( 37.80618814713138676, -9.703840866421904465, 69.62690120949091011 ) ) ;
#17951=CARTESIAN_POINT ( 'NONE',  ( 38.82593461698262871, -14.91368208888609637, 69.62690120949091011 ) ) ;
#17953=CARTESIAN_POINT ( 'NONE',  ( 39.64521430340304420, -18.81368208888610027, 69.45876917294175712 ) ) ;
#17957=CARTESIAN_POINT ( 'NONE',  ( 39.41296390513587511, -17.20384086642191335, 71.08074471024441721 ) ) ;
#17963=CARTESIAN_POINT ( 'NONE',  ( 36.98690846071097127, -19.80384086642191477, 69.45876917294175712 ) ) ;
#17965=CARTESIAN_POINT ( 'NONE',  ( 39.98359781491296161, -28.41368208888610525, 71.86517103874045631 ) ) ;
#17971=CARTESIAN_POINT ( 'NONE',  ( 38.37017380507018771, -21.60384086642190837, 69.64448340153877837 ) ) ;
#17976=CARTESIAN_POINT ( 'NONE',  ( 39.41296390513587511, 0.7961591335780872081, 71.08074471024443142 ) ) ;
#17979=CARTESIAN_POINT ( 'NONE',  ( 39.75915168707250302, -28.71368208888609175, 70.26145752964249880 ) ) ;
#17986=CARTESIAN_POINT ( 'NONE',  ( 38.73920764526925353, -8.113682088886099208, 72.49843995877331793 ) ) ;
#17988=CARTESIAN_POINT ( 'NONE',  ( 37.25260217561390874, -3.613682088886100097, 71.78268878715394408 ) ) ;
#17995=CARTESIAN_POINT ( 'NONE',  ( 40.14115730948191185, -9.103840866421911926, 71.43714994484034264 ) ) ;
#18004=CARTESIAN_POINT ( 'NONE',  ( 37.25202387243752611, -9.213682088886100630, 70.00779233799264034 ) ) ;
#18020=PRODUCT_DEFINITION_CONTEXT ( 'detailed design', #15233, 'design' ) ;
#18021=CARTESIAN_POINT ( 'NONE',  ( 40.52078840805429394, -3.003840866421914502, 72.15350918040385864 ) ) ;
#18025=CARTESIAN_POINT ( 'NONE',  ( 37.33957961208646736, -7.813682088886109156, 72.81632618279323310 ) ) ;
#18028=CARTESIAN_POINT ( 'NONE',  ( 39.64521430340304420, -12.81368208888610383, 69.45876917294175712 ) ) ;
#18039=CARTESIAN_POINT ( 'NONE',  ( 37.21915885897815457, -25.41368208888610170, 71.08074471024441721 ) ) ;
#18045=CARTESIAN_POINT ( 'NONE',  ( 38.26194895904384197, -26.60384086642191903, 73.71602215082113219 ) ) ;
#18047=CARTESIAN_POINT ( 'NONE',  ( 36.87297107704152666, -27.71368208888610241, 72.49904802271738902 ) ) ;
#18053=CARTESIAN_POINT ( 'NONE',  ( 36.89935272106205133, -2.403840866421917521, 73.23812341099225875 ) ) ;
#18057=CARTESIAN_POINT ( 'NONE',  ( 39.95015449827720744, -6.613682088886106314, 70.79240656858107172 ) ) ;
#18060=CARTESIAN_POINT ( 'NONE',  ( 39.83125377402841139, -28.67593286074587411, 70.46188669365974988 ) ) ;
#18067=CARTESIAN_POINT ( 'NONE',  ( 37.25260217561390874, -28.00384086642191406, 70.97781676520601479 ) ) ;
#18068=CARTESIAN_POINT ( 'NONE',  ( 37.69796330110504101, -13.11368208888609743, 69.66206559358661821 ) ) ;
#18071=CARTESIAN_POINT ( 'NONE',  ( 36.80608444377001831, -10.30384086642191654, 72.40698646996136745 ) ) ;
#18075=CARTESIAN_POINT ( 'NONE',  ( 36.68196826583682935, -9.613682088886104538, 71.96809898377890136 ) ) ;
#18077=CARTESIAN_POINT ( 'NONE',  ( 40.33642880535524000, -18.31368208888610383, 72.77780686321126780 ) ) ;
#18082=CARTESIAN_POINT ( 'NONE',  ( 37.12184278917507640, -18.10384086642191193, 71.32335560751961623 ) ) ;
#18090=CARTESIAN_POINT ( 'NONE',  ( 37.50301148336529877, -24.50384086642192116, 73.69843995877326392 ) ) ;
#18092=CARTESIAN_POINT ( 'NONE',  ( 40.55423172469004811, 1.586317911113896306, 72.05058123536544201 ) ) ;
#18100=CARTESIAN_POINT ( 'NONE',  ( 37.69796330110505522, -18.50384086642191406, 73.09843995877329803 ) ) ;
#18107=CARTESIAN_POINT ( 'NONE',  ( 39.41296390513587511, -1.203840866421910905, 71.08074471024443142 ) ) ;
#18117=CARTESIAN_POINT ( 'NONE',  ( 38.73920764526925353, -4.113682088886099208, 72.49843995877331793 ) ) ;
#18118=CARTESIAN_POINT ( 'NONE',  ( 39.37952058850012804, -6.613682088886101873, 70.97781676520601479 ) ) ;
#18124=CARTESIAN_POINT ( 'NONE',  ( 39.82603832034400426, -13.30384086642190233, 70.35351908239857721 ) ) ;
#18132=CARTESIAN_POINT ( 'NONE',  ( 36.68196826583682935, -9.613682088886104538, 71.96809898377890136 ) ) ;
#18146=CARTESIAN_POINT ( 'NONE',  ( 40.26954217208372455, -4.903840866421919742, 72.86986841596736042 ) ) ;
#18150=CARTESIAN_POINT ( 'NONE',  ( 36.49096545463212493, -5.513682088886105781, 71.43714994484035685 ) ) ;
#18153=CARTESIAN_POINT ( 'NONE',  ( 36.89935272106204422, -17.21368208888610241, 69.52238214136768590 ) ) ;
#18164=CARTESIAN_POINT ( 'NONE',  ( 39.37952058850012804, -24.61368208888610454, 70.97781676520600058 ) ) ;
#18171=CARTESIAN_POINT ( 'NONE',  ( 39.73277004305197124, -21.40384086642191619, 69.52238214136768590 ) ) ;
#18174=CARTESIAN_POINT ( 'NONE',  ( 36.68196826583682935, -27.61368208888610809, 71.96809898377887293 ) ) ;
#18181=CARTESIAN_POINT ( 'NONE',  ( 36.29569395875881099, -4.303840866421919209, 72.77780686321129622 ) ) ;
#18184=CARTESIAN_POINT ( 'NONE',  ( 37.25202387243752611, -9.213682088886100630, 70.00779233799264034 ) ) ;
#18190=CARTESIAN_POINT ( 'NONE',  ( 37.31647492878124694, -26.30384086642190766, 72.03616607671141026 ) ) ;
#18191=CARTESIAN_POINT ( 'NONE',  ( 37.69796330110504101, -11.11368208888610276, 69.66206559358663242 ) ) ;
#18195=CARTESIAN_POINT ( 'NONE',  ( 37.69796330110505522, -14.50384086642191583, 73.09843995877329803 ) ) ;
#18199=CARTESIAN_POINT ( 'NONE',  ( 39.29254315202756231, -8.813682088886100274, 69.94417936956673998 ) ) ;
#18201=CARTESIAN_POINT ( 'NONE',  ( 35.86008812008917346, -13.51368208888610667, 71.43714994484034264 ) ) ;
#18205=CARTESIAN_POINT ( 'NONE',  ( 39.24876120206129571, -16.90384086642190553, 72.12822762946747446 ) ) ;
#18210=CARTESIAN_POINT ( 'NONE',  ( 40.26954217208372455, -22.90384086642191974, 72.86986841596734621 ) ) ;
#18212=CARTESIAN_POINT ( 'NONE',  ( 39.75915168707250302, -28.71368208888609175, 70.26145752964249880 ) ) ;
#18221=CARTESIAN_POINT ( 'NONE',  ( 36.49096545463212493, -12.10384086642191193, 71.32335560751961623 ) ) ;
#18229=CARTESIAN_POINT ( 'NONE',  ( 36.64852494920107517, -28.20384086642191335, 71.86517103874047052 ) ) ;
#18241=CARTESIAN_POINT ( 'NONE',  ( 37.69225076346193504, -5.813682088886100274, 72.33091598616827866 ) ) ;
#18242=CARTESIAN_POINT ( 'NONE',  ( 39.24876120206128860, -6.713682088886101518, 70.63227792289247020 ) ) ;
#18249=CARTESIAN_POINT ( 'NONE',  ( 38.37017380507018771, -9.603840866421908373, 69.64448340153879258 ) ) ;
#18256=CARTESIAN_POINT ( 'NONE',  ( 36.64852494920107517, -7.413682088886104360, 70.89533451361948835 ) ) ;
#18263=CARTESIAN_POINT ( 'NONE',  ( 36.80608444377001121, -23.31368208888610383, 70.35351908239857721 ) ) ;
#18274=CARTESIAN_POINT ( 'NONE',  ( 36.36258059203030513, -1.903840866421910638, 69.89063713639259845 ) ) ;
#18275=CARTESIAN_POINT ( 'NONE',  ( 38.63098279924288647, -22.91368208888609814, 70.22690120949090442 ) ) ;
#18279=CARTESIAN_POINT ( 'NONE',  ( 36.68196826583682935, -11.61368208888610276, 71.96809898377888715 ) ) ;
#18285=CARTESIAN_POINT ( 'NONE',  ( 39.64521430340304420, -6.813682088886101162, 69.45876917294177133 ) ) ;
#18300=CARTESIAN_POINT ( 'NONE',  ( 39.64521430340305841, -22.80384086642191832, 73.30173637941818754 ) ) ;
#18301=CARTESIAN_POINT ( 'NONE',  ( 39.75915168707250302, -28.71368208888609175, 70.26145752964249880 ) ) ;
#18311=CARTESIAN_POINT ( 'NONE',  ( 36.89935272106205133, -4.403840866421918854, 73.23812341099225875 ) ) ;
#18314=CARTESIAN_POINT ( 'NONE',  ( 37.80618814713140097, -7.913682088886107913, 73.13360434286904876 ) ) ;
#18316=CARTESIAN_POINT ( 'NONE',  ( 37.33957961208646736, -19.81368208888611093, 72.81632618279321889 ) ) ;
#18321=CARTESIAN_POINT ( 'NONE',  ( 37.12184278917507640, -24.10384086642191193, 71.32335560751960202 ) ) ;
#18322=CARTESIAN_POINT ( 'NONE',  ( 39.29254315202756231, -10.81368208888610205, 69.94417936956673998 ) ) ;
#18325=CARTESIAN_POINT ( 'NONE',  ( 40.14115730948191185, -13.10384086642191015, 71.43714994484030001 ) ) ;
#18327=CARTESIAN_POINT ( 'NONE',  ( 39.29254315202756231, -6.813682088886101162, 69.94417936956673998 ) ) ;
#18329=CARTESIAN_POINT ( 'NONE',  ( 40.26954217208371034, -16.71368208888610241, 69.89063713639258424 ) ) ;
#18333=CARTESIAN_POINT ( 'NONE',  ( 38.37017380507018771, -19.60384086642191193, 70.24448340153875847 ) ) ;
#18338=CARTESIAN_POINT ( 'NONE',  ( 40.77203464402485622, -25.10384086642191903, 71.43714994484031422 ) ) ;
#18340=CARTESIAN_POINT ( 'NONE',  ( 36.80608444377001121, -25.31368208888610383, 70.35351908239857721 ) ) ;
#18347=CARTESIAN_POINT ( 'NONE',  ( 37.25202387243754032, -14.40384086642191619, 72.75271321436731853 ) ) ;
#18352=CARTESIAN_POINT ( 'NONE',  ( 39.24876120206129571, -0.9038408664219128585, 72.12822762946750288 ) ) ;
#18355=CARTESIAN_POINT ( 'NONE',  ( 39.95015449827720744, -26.61368208888610809, 70.79240656858104330 ) ) ;
#18360=CARTESIAN_POINT ( 'NONE',  ( 37.60469502381300089, -3.213682088886101962, 70.49320253461759478 ) ) ;
#18362=CARTESIAN_POINT ( 'NONE',  ( 38.63098279924288647, -6.913682088886101695, 70.22690120949091863 ) ) ;
#18367=CARTESIAN_POINT ( 'NONE',  ( 39.98359781491296161, -13.20384086642191157, 70.89533451361945993 ) ) ;
#18374=CARTESIAN_POINT ( 'NONE',  ( 40.14115730948191185, -8.513682088886106669, 71.32335560751961623 ) ) ;
#18386=CARTESIAN_POINT ( 'NONE',  ( 35.86008812008917346, -27.51368208888610667, 71.43714994484032843 ) ) ;
#18391=CARTESIAN_POINT ( 'NONE',  ( 37.60469502381300089, -25.21368208888610241, 70.49320253461758057 ) ) ;
#18395=CARTESIAN_POINT ( 'NONE',  ( 38.82593461698262871, -2.913682088886099919, 69.62690120949091011 ) ) ;
#18396=CARTESIAN_POINT ( 'NONE',  ( 38.93415946300896024, -27.50384086642189985, 69.66206559358660400 ) ) ;
#18401=CARTESIAN_POINT ( 'NONE',  ( 36.11133435605973574, -5.613682088886105426, 72.15350918040385864 ) ) ;
#18419=CARTESIAN_POINT ( 'NONE',  ( 40.52078840805429394, -17.00384086642191406, 72.15350918040381600 ) ) ;
#18420=CARTESIAN_POINT ( 'NONE',  ( 37.69796330110504101, -25.11368208888609388, 69.66206559358660400 ) ) ;
#18429=CARTESIAN_POINT ( 'NONE',  ( 40.77203464402485622, -26.51368208888610667, 71.32335560751960202 ) ) ;
#18432=CARTESIAN_POINT ( 'NONE',  ( 39.82603832034400426, -10.31368208888610383, 72.40698646996135324 ) ) ;
#18434=CARTESIAN_POINT ( 'NONE',  ( 39.29254315202756231, -18.81368208888610027, 69.94417936956672577 ) ) ;
#18439=CARTESIAN_POINT ( 'NONE',  ( 38.63098279924290068, -26.70384086642191690, 72.53360434286901182 ) ) ;
#18440=CARTESIAN_POINT ( 'NONE',  ( 37.69796330110504101, -15.11368208888609743, 69.66206559358661821 ) ) ;
#18445=CARTESIAN_POINT ( 'NONE',  ( 38.26194895904384907, -8.603840866421915479, 73.11602215082118050 ) ) ;
#18447=CARTESIAN_POINT ( 'NONE',  ( 39.82603832034400426, -4.313682088886107380, 72.40698646996135324 ) ) ;
#18449=CARTESIAN_POINT ( 'NONE',  ( 37.61123632939165873, -13.91368208888610525, 73.73360434286898624 ) ) ;
#18453=CARTESIAN_POINT ( 'NONE',  ( 37.69225076346193504, -13.80384086642191122, 70.42958956619168021 ) ) ;
#18458=CARTESIAN_POINT ( 'NONE',  ( 37.50301148336529877, -16.50384086642191761, 73.69843995877327814 ) ) ;
#18460=CARTESIAN_POINT ( 'NONE',  ( 37.80618814713140097, -23.91368208888610880, 73.13360434286902034 ) ) ;
#18467=CARTESIAN_POINT ( 'NONE',  ( 37.33957961208645315, -17.80384086642190766, 69.94417936956672577 ) ) ;
#18475=CARTESIAN_POINT ( 'NONE',  ( 37.33957961208645315, -27.80384086642191122, 69.94417936956671156 ) ) ;
#18479=CARTESIAN_POINT ( 'NONE',  ( 36.64852494920107517, -27.41368208888610525, 70.89533451361945993 ) ) ;
#18484=CARTESIAN_POINT ( 'NONE',  ( 39.24876120206129571, -28.90384086642191264, 72.12822762946746025 ) ) ;
#18486=CARTESIAN_POINT ( 'NONE',  ( 39.51027997493896748, 1.486317911113900658, 71.32335560751961623 ) ) ;
#18494=CARTESIAN_POINT ( 'NONE',  ( 40.14115730948191185, -13.10384086642191015, 71.43714994484030001 ) ) ;
#18501=CARTESIAN_POINT ( 'NONE',  ( 39.95015449827720744, -4.613682088886104538, 70.79240656858107172 ) ) ;
#18514=CARTESIAN_POINT ( 'NONE',  ( 38.37017380507020192, -28.01368208888610667, 73.71602215082113219 ) ) ;
#18515=CARTESIAN_POINT ( 'NONE',  ( 37.12184278917507640, -19.51368208888610312, 71.43714994484034264 ) ) ;
#18519=CARTESIAN_POINT ( 'NONE',  ( 39.98359781491296161, -2.413682088886103472, 71.86517103874048473 ) ) ;
#18520=CARTESIAN_POINT ( 'NONE',  ( 38.37017380507018771, -1.603840866421912148, 70.24448340153877268 ) ) ;
#18523=CARTESIAN_POINT ( 'NONE',  ( 40.55423172469004811, -6.413682088886103472, 72.05058123536544201 ) ) ;
#18543=CARTESIAN_POINT ( 'NONE',  ( 36.07789103942399578, -20.20384086642191335, 72.05058123536544201 ) ) ;
#18545=CARTESIAN_POINT ( 'NONE',  ( 37.80618814713140097, -19.91368208888610170, 73.13360434286903455 ) ) ;
#18549=( NAMED_UNIT ( * ) SI_UNIT ( $, .STERADIAN. ) SOLID_ANGLE_UNIT ( ) );
#18553=CARTESIAN_POINT ( 'NONE',  ( 40.55423172469004101, 0.7961591335780838774, 70.70992431699450265 ) ) ;
#18557=CARTESIAN_POINT ( 'NONE',  ( 39.38009889167650357, -2.213682088886108179, 72.75271321436733274 ) ) ;
#18559=CARTESIAN_POINT ( 'NONE',  ( 36.80608444377001121, -21.31368208888610027, 70.35351908239860563 ) ) ;
#18563=CARTESIAN_POINT ( 'NONE',  ( 37.38336156205273397, -17.90384086642190908, 70.63227792289247020 ) ) ;
#18564=CARTESIAN_POINT ( 'NONE',  ( 38.82593461698262871, -6.913682088886100807, 69.62690120949091011 ) ) ;
#18568=CARTESIAN_POINT ( 'NONE',  ( 39.38009889167648936, -7.403840866421908196, 70.00779233799264034 ) ) ;
#18570=CARTESIAN_POINT ( 'NONE',  ( 38.93415946300897446, -4.113682088886107202, 73.09843995877331224 ) ) ;
#18572=CARTESIAN_POINT ( 'NONE',  ( 36.98690846071097837, -9.813682088886107380, 73.30173637941818754 ) ) ;
#18575=CARTESIAN_POINT ( 'NONE',  ( 37.69225076346193504, -11.80384086642191477, 70.42958956619168021 ) ) ;
#18580=CARTESIAN_POINT ( 'NONE',  ( 38.26194895904384197, -14.60384086642191726, 73.71602215082113219 ) ) ;
#18583=CARTESIAN_POINT ( 'NONE',  ( 39.82603832034400426, -20.31368208888610738, 72.40698646996133903 ) ) ;
#18591=CARTESIAN_POINT ( 'NONE',  ( 37.69796330110505522, -12.50384086642191406, 73.09843995877329803 ) ) ;
#18595=CARTESIAN_POINT ( 'NONE',  ( 36.68196826583682935, -26.00384086642191406, 70.79240656858105751 ) ) ;
#18598=CARTESIAN_POINT ( 'NONE',  ( 36.80608444377001121, -23.31368208888610383, 70.35351908239857721 ) ) ;
#18603=CARTESIAN_POINT ( 'NONE',  ( 38.37017380507020192, -0.01368208888610084051, 72.51602215082118619 ) ) ;
#18604=CARTESIAN_POINT ( 'NONE',  ( 38.73920764526923932, -29.50384086642191050, 70.26206559358661252 ) ) ;
#18611=CARTESIAN_POINT ( 'NONE',  ( 39.75915168707251723, -6.903840866421915301, 72.49904802271740323 ) ) ;
#18622=CARTESIAN_POINT ( 'NONE',  ( 36.80608444377001121, -1.313682088886099830, 70.35351908239861984 ) ) ;
#18624=CARTESIAN_POINT ( 'NONE',  ( 39.89531854050225235, -29.10876147765329591, 71.21617469530100664 ) ) ;
#18640=CARTESIAN_POINT ( 'NONE',  ( 37.31647492878122563, -19.31368208888610027, 70.72433947564853440 ) ) ;
#18645=CARTESIAN_POINT ( 'NONE',  ( 37.80618814713140097, 0.08631791111389161553, 73.13360434286904876 ) ) ;
#18646=CARTESIAN_POINT ( 'NONE',  ( 39.95015449827720744, -23.00384086642191050, 71.96809898377887293 ) ) ;
#18650=CARTESIAN_POINT ( 'NONE',  ( 35.86008812008917346, -11.51368208888610134, 71.43714994484034264 ) ) ;
#18668=CARTESIAN_POINT ( 'NONE',  ( 40.26954217208372455, -14.90384086642191797, 72.86986841596734621 ) ) ;
#18670=CARTESIAN_POINT ( 'NONE',  ( 38.82593461698262871, -20.91368208888609459, 69.62690120949091011 ) ) ;
#18674=( LENGTH_UNIT ( ) NAMED_UNIT ( * ) SI_UNIT ( .MILLI., .METRE. ) );
#18679=CARTESIAN_POINT ( 'NONE',  ( 36.98690846071097837, -25.81368208888611093, 73.30173637941817333 ) ) ;
#18684=CARTESIAN_POINT ( 'NONE',  ( 36.64852494920107517, -3.413682088886104360, 70.89533451361948835 ) ) ;
#18686=CARTESIAN_POINT ( 'NONE',  ( 38.82593461698262871, -22.91368208888609814, 69.62690120949091011 ) ) ;
#18692=CARTESIAN_POINT ( 'NONE',  ( 38.63098279924290068, -20.70384086642191335, 72.53360434286904024 ) ) ;
#18693=CARTESIAN_POINT ( 'NONE',  ( 39.95015449827720744, -6.613682088886106314, 70.79240656858107172 ) ) ;
#18697=CARTESIAN_POINT ( 'NONE',  ( 37.33957961208645315, -3.803840866421909439, 69.94417936956673998 ) ) ;
#18700=CARTESIAN_POINT ( 'NONE',  ( 37.69796330110504101, -5.113682088886101873, 69.66206559358663242 ) ) ;
#18702=CARTESIAN_POINT ( 'NONE',  ( 39.12911128074873801, -12.11368208888610987, 73.69843995877327814 ) ) ;
#18705=CARTESIAN_POINT ( 'NONE',  ( 39.31564783533279694, -13.30384086642190944, 70.72433947564853440 ) ) ;
#18712=CARTESIAN_POINT ( 'NONE',  ( 38.37017380507018771, -15.60384086642191370, 69.04448340153878405 ) ) ;
#18718=CARTESIAN_POINT ( 'NONE',  ( 38.82593461698262871, -20.91368208888609459, 69.62690120949091011 ) ) ;
#18724=CARTESIAN_POINT ( 'NONE',  ( 36.87297107704151244, -15.90384086642190908, 70.26145752964255564 ) ) ;
#18728=CARTESIAN_POINT ( 'NONE',  ( 39.95015449827720744, -24.61368208888610454, 70.79240656858104330 ) ) ;
#18730=CARTESIAN_POINT ( 'NONE',  ( 37.69796330110505522, -22.50384086642191050, 73.09843995877329803 ) ) ;
#18733=CARTESIAN_POINT ( 'NONE',  ( 36.87297107704152666, -21.71368208888610951, 72.49904802271740323 ) ) ;
#18738=CARTESIAN_POINT ( 'NONE',  ( 39.31564783533279694, -29.30384086642190766, 70.72433947564850598 ) ) ;
#18739=CARTESIAN_POINT ( 'NONE',  ( 38.73920764526925353, -0.1136820888861002354, 72.49843995877331793 ) ) ;
#18746=CARTESIAN_POINT ( 'NONE',  ( 39.29254315202757653, -2.803840866421915212, 72.81632618279323310 ) ) ;
#18754=CARTESIAN_POINT ( 'NONE',  ( 37.80618814713140097, -1.913682088886106580, 73.13360434286904876 ) ) ;
#18755=CARTESIAN_POINT ( 'NONE',  ( 40.02061183432068958, -29.10876147765278787, 71.40071884891759169 ) ) ;
#18769=CARTESIAN_POINT ( 'NONE',  ( 37.12184278917507640, -17.51368208888609956, 71.43714994484034264 ) ) ;
#18773=CARTESIAN_POINT ( 'NONE',  ( 39.29254315202756231, -0.8136820888860994971, 69.94417936956673998 ) ) ;
#18774=CARTESIAN_POINT ( 'NONE',  ( 37.80618814713138676, -25.70384086642190979, 69.62690120949091011 ) ) ;
#18777=CARTESIAN_POINT ( 'NONE',  ( 40.33642880535524000, -8.313682088886110932, 72.77780686321128201 ) ) ;
#18794=CARTESIAN_POINT ( 'NONE',  ( 36.36258059203030513, -19.90384086642191264, 69.89063713639259845 ) ) ;
#18795=CARTESIAN_POINT ( 'NONE',  ( 36.68196826583682935, -21.61368208888610454, 71.96809898377888715 ) ) ;
#18801=EDGE_CURVE ( 'NONE', #21877, #2631, #4466, .T. ) ;
#18802=CARTESIAN_POINT ( 'NONE',  ( 40.77203464402485622, 0.8961591335780867418, 71.43714994484035685 ) ) ;
#18809=CARTESIAN_POINT ( 'NONE',  ( 38.37017380507020192, -0.01368208888610777940, 73.11602215082118050 ) ) ;
#18811=CARTESIAN_POINT ( 'NONE',  ( 36.87297107704153376, -21.71368208888610951, 72.49904802271740323 ) ) ;
#18814=CARTESIAN_POINT ( 'NONE',  ( 37.31647492878124694, -16.30384086642191122, 72.03616607671141026 ) ) ;
#18815=CARTESIAN_POINT ( 'NONE',  ( 37.69796330110504101, -3.113682088886098764, 69.66206559358663242 ) ) ;
#18819=CARTESIAN_POINT ( 'NONE',  ( 37.80618814713138676, -5.703840866421908018, 69.62690120949091011 ) ) ;
#18823=CARTESIAN_POINT ( 'NONE',  ( 38.93415946300897446, -8.113682088886108090, 73.09843995877331224 ) ) ;
#18825=CARTESIAN_POINT ( 'NONE',  ( 38.26194895904383486, -7.013682088886100452, 69.04448340153881247 ) ) ;
#18828=CARTESIAN_POINT ( 'NONE',  ( 38.63098279924290068, -12.70384086642191157, 72.53360434286904024 ) ) ;
#18834=CARTESIAN_POINT ( 'NONE',  ( 36.89935272106205133, -18.40384086642191974, 73.23812341099225875 ) ) ;
#18837=CARTESIAN_POINT ( 'NONE',  ( 36.64852494920107517, -19.41368208888610525, 70.89533451361947414 ) ) ;
#18846=CARTESIAN_POINT ( 'NONE',  ( 37.69796330110505522, -6.503840866421914058, 73.09843995877331224 ) ) ;
#18850=CARTESIAN_POINT ( 'NONE',  ( 40.14115730948191185, -22.51368208888609956, 71.32335560751960202 ) ) ;
#18855=CARTESIAN_POINT ( 'NONE',  ( 36.68196826583682935, -24.00384086642191050, 70.79240656858105751 ) ) ;
#18857=DIRECTION ( 'NONE',  ( -0.9835979625596985576, -0.1803747433772529551, 0.000000000000000000 ) ) ;
#18858=CARTESIAN_POINT ( 'NONE',  ( 37.69796330110504101, -27.11368208888609388, 69.66206559358660400 ) ) ;
#18863=CARTESIAN_POINT ( 'NONE',  ( 39.02742774030102879, -0.2136820888860996304, 72.26730301774236409 ) ) ;
#18872=CARTESIAN_POINT ( 'NONE',  ( 39.75915168707251723, -2.903840866421913525, 72.49904802271740323 ) ) ;
#18881=CARTESIAN_POINT ( 'NONE',  ( 38.93415946300898867, -0.1136820888861071605, 73.09843995877331224 ) ) ;
#18883=CARTESIAN_POINT ( 'NONE',  ( 40.14115730948191185, -25.10384086642190837, 71.43714994484030001 ) ) ;
#18899=CARTESIAN_POINT ( 'NONE',  ( 37.69225076346193504, -15.81368208888610205, 72.33091598616826445 ) ) ;
#18903=CARTESIAN_POINT ( 'NONE',  ( 37.25202387243752611, -3.213682088886102406, 70.00779233799264034 ) ) ;
#18904=CARTESIAN_POINT ( 'NONE',  ( 39.98359781491296161, -21.20384086642190979, 70.89533451361945993 ) ) ;
#18907=CARTESIAN_POINT ( 'NONE',  ( 36.07789103942398867, -1.413682088886102584, 70.70992431699450265 ) ) ;
#18927=CARTESIAN_POINT ( 'NONE',  ( 39.02088643472237806, -14.70384086642192045, 73.73360434286898624 ) ) ;
#18930=CARTESIAN_POINT ( 'NONE',  ( 36.80608444377001121, -19.31368208888609672, 70.35351908239857721 ) ) ;
#18937=CARTESIAN_POINT ( 'NONE',  ( 40.52078840805429394, 0.9961591335780859424, 72.15350918040385864 ) ) ;
#18943=CARTESIAN_POINT ( 'NONE',  ( 39.29254315202756231, -2.813682088886101162, 69.94417936956673998 ) ) ;
#18946=CARTESIAN_POINT ( 'NONE',  ( 37.80618814713140097, -15.91368208888610880, 73.13360434286903455 ) ) ;
#18949=CARTESIAN_POINT ( 'NONE',  ( 39.24876120206129571, -18.90384086642191264, 72.12822762946747446 ) ) ;
#18950=CARTESIAN_POINT ( 'NONE',  ( 37.33957961208646736, -7.813682088886109156, 72.81632618279323310 ) ) ;
#18953=EDGE_CURVE ( 'NONE', #21877, #12953, #15675, .T. ) ;
#18955=CARTESIAN_POINT ( 'NONE',  ( 36.64852494920107517, -8.203840866421909794, 71.86517103874049894 ) ) ;
#18957=CARTESIAN_POINT ( 'NONE',  ( 39.38009889167650357, 1.786317911113891821, 72.75271321436734695 ) ) ;
#18959=CARTESIAN_POINT ( 'NONE',  ( 39.12911128074873801, -10.11368208888610987, 73.69843995877330656 ) ) ;
#18962=CARTESIAN_POINT ( 'NONE',  ( 37.31647492878124694, -12.30384086642191299, 72.03616607671141026 ) ) ;
#18968=CARTESIAN_POINT ( 'NONE',  ( 39.12911128074872380, -15.50384086642191228, 69.06206559358665231 ) ) ;
#18972=CARTESIAN_POINT ( 'NONE',  ( 39.82603832034400426, -18.31368208888610738, 72.40698646996133903 ) ) ;
#18978=CARTESIAN_POINT ( 'NONE',  ( 39.75915168707251723, -8.903840866421916189, 72.49904802271740323 ) ) ;
#18981=CARTESIAN_POINT ( 'NONE',  ( 38.26194895904383486, -25.01368208888610312, 69.64448340153876416 ) ) ;
#18985=CARTESIAN_POINT ( 'NONE',  ( 39.95015449827720744, -23.00384086642191050, 71.96809898377887293 ) ) ;
#18987=CARTESIAN_POINT ( 'NONE',  ( 36.49096545463212493, -21.51368208888609956, 71.43714994484034264 ) ) ;
#18989=CARTESIAN_POINT ( 'NONE',  ( 39.02088643472237806, 1.296159133578080658, 73.73360434286904308 ) ) ;
#18993=CARTESIAN_POINT ( 'NONE',  ( 38.63098279924288647, 1.086317911113899415, 70.22690120949094705 ) ) ;
#19000=CARTESIAN_POINT ( 'NONE',  ( 37.33957961208645315, -3.803840866421909439, 69.94417936956673998 ) ) ;
#19011=CARTESIAN_POINT ( 'NONE',  ( 38.82593461698262871, -2.913682088886100363, 69.62690120949091011 ) ) ;
#19028=CARTESIAN_POINT ( 'NONE',  ( 39.41296390513587511, -16.41368208888610525, 71.67976084211551324 ) ) ;
#19033=CARTESIAN_POINT ( 'NONE',  ( 40.14115730948191185, -23.10384086642191193, 71.43714994484030001 ) ) ;
#19036=CARTESIAN_POINT ( 'NONE',  ( 38.37017380507020192, -2.013682088886109334, 73.71602215082116061 ) ) ;
#19047=EDGE_CURVE ( 'NONE', #2631, #3300, #23964, .T. ) ;
#19056=CARTESIAN_POINT ( 'NONE',  ( 36.89935272106205133, -12.40384086642192152, 73.23812341099225875 ) ) ;
#19060=CARTESIAN_POINT ( 'NONE',  ( 39.75915168707250302, -20.71368208888610596, 70.26145752964251301 ) ) ;
#19065=CARTESIAN_POINT ( 'NONE',  ( 40.33642880535524000, -24.31368208888611093, 72.77780686321125359 ) ) ;
#19071=CARTESIAN_POINT ( 'NONE',  ( 36.49096545463212493, -13.51368208888610489, 71.43714994484034264 ) ) ;
#19075=CARTESIAN_POINT ( 'NONE',  ( 37.21915885897815457, -16.20384086642190979, 71.67976084211552745 ) ) ;
#19076=CARTESIAN_POINT ( 'NONE',  ( 37.80618814713140097, -5.913682088886107024, 73.13360434286904876 ) ) ;
#19084=CARTESIAN_POINT ( 'NONE',  ( 40.55423172469004101, -29.20384086642191335, 70.70992431699446001 ) ) ;
#19088=CARTESIAN_POINT ( 'NONE',  ( 36.87297107704152666, 0.2863179111138939303, 72.49904802271743165 ) ) ;
#19089=CARTESIAN_POINT ( 'NONE',  ( 40.33642880535524000, -10.31368208888610738, 72.77780686321128201 ) ) ;
#19092=CARTESIAN_POINT ( 'NONE',  ( 37.60469502381300799, -8.403840866421912636, 72.26730301774236409 ) ) ;
#19098=CARTESIAN_POINT ( 'NONE',  ( 36.36258059203030513, -7.903840866421910860, 69.89063713639259845 ) ) ;
#19102=CARTESIAN_POINT ( 'NONE',  ( 38.26194895904383486, -21.01368208888610312, 69.64448340153877837 ) ) ;
#19109=CARTESIAN_POINT ( 'NONE',  ( 39.82603832034401137, -11.30384086642190944, 70.35351908239860563 ) ) ;
#19112=CARTESIAN_POINT ( 'NONE',  ( 39.75915168707250302, -22.71368208888610241, 70.26145752964251301 ) ) ;
#19115=CARTESIAN_POINT ( 'NONE',  ( 38.93415946300896024, -21.50384086642190340, 69.66206559358661821 ) ) ;
#19117=CARTESIAN_POINT ( 'NONE',  ( 38.37017380507020192, -16.01368208888610667, 73.11602215082116629 ) ) ;
#19119=CARTESIAN_POINT ( 'NONE',  ( 37.50301148336529877, -0.5038408664219187205, 73.69843995877330656 ) ) ;
#19123=CARTESIAN_POINT ( 'NONE',  ( 39.37952058850012804, -27.00384086642191050, 71.78268878715390144 ) ) ;
#19129=CARTESIAN_POINT ( 'NONE',  ( 37.69796330110505522, -2.503840866421913613, 73.09843995877331224 ) ) ;
#19137=DIRECTION ( 'NONE',  ( 0.9835979625596965592, -0.1803747433772641684, -2.086002012065537230E-15 ) ) ;
#19138=CARTESIAN_POINT ( 'NONE',  ( 39.38009889167650357, -4.213682088886106847, 72.75271321436733274 ) ) ;
#19139=CARTESIAN_POINT ( 'NONE',  ( 37.69796330110505522, -24.50384086642191406, 73.09843995877328382 ) ) ;
#19141=( BOUNDED_SURFACE ( )  B_SPLINE_SURFACE ( 3, 2, ( 
 ( #16031, #10121, #21963, #17979, #6382, #12313, #23882, #12445, #9868, #12190, #20159, #10627, #6623, #12945, #5080, #4947, #18479, #14484, #8568, #18858, #4814, #22845, #20797, #3132, #18355, #4701, #12693, #813, #22717, #10758, #5206, #20665, #24502, #13068, #10502, #2998, #8700, #16531, #11002, #14992, #2624, #20534, #16793, #1197, #6756, #2867, #9085, #12575, #22341, #680, #24253, #16405, #8948, #10880, #20406, #24626, #2739, #18598, #24382, #14609, #22464, #939, #16928, #1065, #8831, #24759, #16669, #7006, #7138, #6876, #14730, #22592, #12817, #18733, #14855, #18987, #19230, #17182, #5333, #13324, #11520, #9711, #19359, #7261, #23216, #1694, #25006, #7775, #25266, #21175, #17562, #1568, #5706, #19485, #11389, #15488, #15619, #9461, #5835, #3260, #23340, #17310, #20919, #7396, #1328, #15240, #3633, #11135, #9214, #13569, #17063, #21421, #25132, #24882, #23093, #15112, #5454, #9589, #22969, #13198, #3765, #9336, #25390, #3391, #3514, #11648, #21049, #1828, #11271, #23470, #19117, #7518, #15366, #7647, #1456, #5583, #13441, #21292, #17439, #19874, #3902, #17951, #11899, #6218, #10212, #19740, #8411, #14210, #2083, #13946, #21675, #17691, #23974, #16122, #15994, #4026, #21, #19608, #4414, #15872, #16251, #6351, #22050, #11776, #15750, #23725, #9964, #8279, #21803, #24096, #14076, #10093, #13696, #21554, #21930, #17823, #153, #12281, #527, #1951, #6091, #2336, #20123, #8032, #4161, #2458, #23605, #7903, #9834, #5967, #13817, #19996, #4292, #12031, #18075, #2213, #271, #8150, #23845, #12160, #397, #10336, #18199, #20378, #1035, #10472, #20631, #24594, #14326, #18823, #14451, #6718, #4782, #4915, #4544, #12661, #2708, #16369, #24344, #22560, #20767, #12787, #18327, #8795, #2966, #10596, #1161, #10851, #14574, #3097, #20503, #16760, #5042, #22432, #8916, #9054, #2835, #16895, #6593, #18700, #12408, #10724, #22179, #12914, #6842, #4664, #24469, #18447, #20249, #18570, #6976, #6469, #777, #2587, #651, #905, #8536, #22305, #10970, #24217, #8669, #14827, #12542, #14698, #22685, #16499, #16633, #5179, #19203, #15207, #13164, #17028, #24858, #13414, #14959, #21144, #20888, #9431, #9310, #11361, #11102, #17276, #3735, #7358, #7235, #21394, #3359, #1427, #1796, #23308, #7104, #17404, #22817, #19088, #25237, #17152, #13032, #21017, #5553, #15081, #3488, #23187, #1661, #21262, #7482, #22935, #19454, #5299, #18957, #9688, #15338 ),
 ( #23059, #11236, #9182, #24979, #3607, #13538, #11490, #1295, #1541, #19330, #5425, #11611, #9554, #13294, #24728, #25101, #7620, #5675, #15461, #3224, #12609, #8006, #2779, #25360, #12484, #13921, #17537, #21645, #15587, #3997, #603, #7746, #23444, #10541, #5936, #22380, #4332, #19709, #18391, #19583, #722, #5810, #24292, #8605, #6061, #21776, #2057, #20447, #16444, #2660, #13666, #1921, #9934, #7875, #20328, #124, #21522, #10410, #4134, #3870, #11748, #18275, #15720, #13792, #6660, #4736, #9808, #17792, #6537, #14522, #11875, #15842, #17664, #23573, #23696, #12003, #19842, #2530, #24162, #8480, #16314, #14396, #22250, #4610, #4857, #22504, #20574, #12731, #5244, #9124, #24539, #13111, #14644, #24799, #3303, #18515, #23008, #18640, #10920, #8990, #16966, #8736, #16838, #6920, #2904, #3042, #1243, #24919, #7180, #10789, #12985, #15028, #14773, #5373, #22883, #18769, #7304, #24673, #20962, #9256, #1104, #11178, #13239, #7045, #21089, #845, #19028, #14896, #10669, #22631, #16572, #4987, #18899, #24422, #6795, #1369, #12851, #15154, #980, #20706, #17100, #8868, #16706, #22755, #5124, #20833, #3172, #11042, #7814, #15280, #15659, #9631, #19654, #13612, #17483, #19152, #7684, #1610, #21461, #25432, #9502, #23648, #3942, #17347, #3678, #11429, #7432, #13738, #5877, #5746, #19272, #23129, #9375, #1992, #1488, #25309, #25046, #3805, #13481, #15531, #5501, #11691, #7946, #11560, #3550, #62, #7564, #5618, #6006, #9875, #11312, #21595, #17224, #23257, #11813, #21330, #13365, #25172, #9752, #21211, #23379, #1866, #17731, #23508, #19530, #15414, #13859, #19397, #1733, #3434, #17603, #15790, #8321, #12068, #6388, #20165, #14244, #2376, #2501, #10375, #6630, #18362, #22089, #18242, #18118, #8577, #16160, #21841, #313, #16038, #16412, #2630, #21717, #21969, #24131, #23890, #16284, #13992, #11943, #10001, #24260, #22219, #17865, #567, #4198, #23767, #6254, #24013, #189, #4454, #14117, #2120, #2253, #687, #17988, #4072, #20296, #19783, #4333, #8192, #8069, #6508, #19915, #12322, #15909, #10508, #10127, #8449, #6132, #10252, #12196, #20034, #14365, #440, #4584, #12451, #22348, #2874, #1073, #12951, #22471, #4707, #2745, #16676, #14490, #14615, #3138, #20412, #20541, #18739, #20803, #12823, #8954, #10764, #10886, #10636, #4955, #8837, #12701, #24389, #6763, #16800, #24633, #7013, #12582, #18486, #14861, #22723, #20671, #820, #5087 ),
 ( #8706, #18604, #4820, #946, #16537, #24508, #3005, #6882, #14738, #22599, #6342, #6460, #8141, #4535, #4406, #17945, #18067, #8661, #8273, #24336, #10583, #2208, #12274, #16113, #15986, #6585, #4284, #20239, #16492, #18439, #12154, #24209, #10086, #18190, #263, #770, #12400, #10205, #2578, #23967, #23840, #20117, #14445, #6708, #14202, #6211, #14068, #24089, #12023, #19991, #14566, #19865, #22045, #10462, #22423, #18321, #640, #2451, #8524, #21922, #14318, #10329, #389, #2327, #520, #16361, #8405, #16243, #22172, #22293, #4656, #12534, #20370, #2701, #9301, #12904, #4904, #1417, #8910, #6968, #7348, #3349, #12653, #22925, #20492, #24585, #5286, #14819, #2827, #18692, #11093, #22552, #1151, #3215, #7226, #1288, #13025, #2956, #24967, #10841, #16623, #15195, #20877, #10718, #16888, #20624, #14951, #18949, #22808, #10961, #16750, #9171, #11225, #5170, #17018, #22677, #24851, #18563, #24719, #20758, #1026, #12781, #5033, #15071, #894, #9044, #8787, #13155, #3091, #7093, #24463, #21007, #17142, #18814, #19075, #4774, #6835, #14687, #112, #21636, #5416, #15710, #13283, #17394, #23561, #25227, #21134, #11479, #3861, #15326, #19441, #21511, #25487, #19574, #5800, #21253, #17784, #3597, #9420, #7996, #13658, #3477, #9679, #13405, #7732, #11740, #15576, #3726, #1913, #9797, #23051, #19699, #23435, #17652, #1787, #9926, #17528, #23177, #1653, #7611, #11352, #3988, #19195, #23297, #7867, #15453, #5927, #5545, #1529, #17266, #25091, #13784, #7474, #11864, #19319, #9544, #5663, #25352, #13528, #2047, #21382, #11603, #19773, #21705, #181, #7677, #19388, #13604, #4059, #13471, #11932, #17339, #17855, #2112, #25420, #7805, #15782, #23249, #23638, #17594, #9993, #21586, #15652, #1601, #23500, #9623, #3935, #7936, #17474, #6121, #8059, #25299, #11681, #1723, #15404, #15900, #13851, #25163, #15519, #13728, #7555, #23756, #13980, #9491, #19522, #23371, #5609, #5997, #3667, #19642, #21833, #11419, #11553, #19263, #21322, #5869, #5737, #21454, #11805, #3795, #1982, #1858, #9743, #9865, #17723, #54, #8311, #19905, #16027, #16275, #4189, #12186, #8697, #12059, #16149, #2619, #10624, #22207, #10499, #24001, #20284, #10118, #24121, #20154, #18107, #21959, #4323, #18352, #2243, #557, #301, #14355, #14235, #6496, #23878, #4574, #16528, #12309, #20025, #808, #6379, #22078, #6752, #2736, #17976, #22337, #8181, #4442, #4696, #2491, #6245 ),
 ( #24376, #10240, #14105, #14605, #12442, #2363, #677, #429, #8565, #16400, #24248, #10365, #6620, #14480, #18229, #8438, #12571, #20403, #18475, #9334, #16926, #22588, #1063, #16790, #17180, #3388, #7392, #22715, #24880, #24623, #17060, #14728, #12690, #10754, #25004, #22967, #18595, #11131, #4944, #24498, #7004, #24757, #935, #14989, #14853, #22460, #15110, #7259, #20530, #6872, #5076, #12815, #5330, #12942, #4811, #22843, #18855, #2863, #8826, #5204, #20662, #10878, #13195, #16666, #2996, #20795, #18985, #21045, #8945, #3129, #11266, #18730, #11000, #1193, #9082, #7136, #3256, #13066, #20917, #1325, #9211, #19115, #1454, #1566, #25127, #17307, #9832, #13693, #3631, #17687, #19228, #3898, #7900, #23089, #2079, #23214, #15486, #13566, #21552, #13321, #21418, #11517, #7514, #7645, #5833, #4023, #11773, #9458, #17560, #19605, #19357, #9961, #1949, #23337, #11897, #3762, #18, #13813, #5704, #15747, #17820, #11644, #151, #5451, #23602, #19480, #15236, #1690, #21173, #9584, #23467, #3512, #5964, #21671, #19737, #17435, #5581, #25263, #11387, #15362, #13438, #21290, #1825, #9709, #25388, #7772, #15616, #19871, #20246, #14207, #24215, #18195, #22048, #23719, #12278, #6215, #524, #4541, #14073, #2706, #8532, #21927, #8276, #15991, #12028, #18325, #10469, #10333, #23843, #2211, #13944, #6591, #10210, #2583, #20376, #12158, #6088, #10090, #20121, #8031, #4289, #12538, #15869, #19994, #6466, #14449, #8408, #14324, #2332, #24093, #21801, #2455, #23971, #18071, #267, #8146, #22177, #4158, #4410, #17949, #16248, #393, #12404, #16119, #647, #10590, #6346, #16367, #4661, #22299, #18445, #3357, #24856, #8666, #18955, #16497, #20628, #1293, #2962, #24341, #14694, #7101, #18568, #22683, #24725, #3222, #22814, #9051, #24467, #21014, #6839, #12657, #11233, #16893, #6713, #12911, #16628, #10966, #14957, #18819, #6974, #5177, #13030, #775, #22931, #1158, #20883, #5039, #13162, #20764, #902, #4911, #10848, #14571, #7232, #22429, #1031, #11099, #18697, #9178, #8793, #4780, #20499, #2833, #17025, #10722, #15079, #22558, #12785, #8914, #3095, #16755, #5294, #24592, #14824, #25098, #21392, #7356, #7874, #9805, #9308, #19329, #23186, #15204, #13665, #11360, #1795, #15718, #17661, #19202, #5808, #17150, #25235, #24977, #7179, #19450, #17275, #11610, #15335, #23058, #1660, #11488, #9686, #23571, #17536, #5423, #3734, #25359, #5552, #5935, #23443 ),
 ( #3995, #1425, #21520, #15460, #19084, #13413, #13292, #21261, #7741, #21142, #1920, #3869, #13791, #3605, #1538, #9551, #11747, #3485, #19581, #9430, #21643, #7481, #7619, #23305, #17402, #5672, #13536, #15585, #2557, #22024, #18045, #2056, #16094, #10063, #4386, #8381, #17923, #6561, #12381, #240, #12131, #19841, #15841, #22146, #14296, #14182, #2183, #23695, #17791, #10439, #14045, #14423, #4508, #20220, #9933, #13917, #21900, #8120, #6441, #19972, #22274, #12248, #8251, #11873, #19707, #20091, #15963, #23818, #18300, #24189, #121, #4263, #495, #622, #6194, #2304, #8506, #21774, #6060, #8005, #4133, #12002, #18171, #2431, #10178, #16223, #365, #23944, #6318, #10310, #24073, #16337, #24701, #3070, #18543, #7072, #8633, #18794, #22786, #12513, #16996, #12630, #4881, #2934, #10943, #2681, #10815, #870, #14546, #16731, #16468, #14799, #9150, #12760, #4755, #1270, #8762, #6819, #7209, #3196, #20352, #5149, #10563, #24446, #13007, #14665, #18419, #16600, #1131, #22405, #1008, #9018, #14926, #16865, #12882, #2808, #24829, #10695, #24314, #15050, #20735, #747, #24562, #20471, #22660, #20857, #5012, #18668, #11071, #18927, #4634, #6685, #22528, #20603, #8891, #6944, #17374, #23032, #1512, #17247, #9778, #3837, #7845, #23156, #25333, #25071, #17510, #15177, #13135, #11205, #25464, #23408, #19056, #11588, #5399, #24945, #7458, #25203, #1400, #15436, #15307, #3330, #3460, #7593, #9281, #11721, #13638, #20988, #5530, #9399, #17126, #7714, #13263, #5644, #19557, #21492, #21116, #9660, #7329, #3577, #11337, #1892, #23285, #19177, #13509, #13392, #21237, #11459, #15556, #17635, #19297, #1634, #9530, #21358, #22907, #3704, #5269, #19420, #1765, #5776, #22122, #8223, #22003, #19814, #6291, #21622, #10156, #6162, #4105, #7977, #15820, #4359, #5908, #12102, #11844, #341, #220, #12222, #13769, #8097, #9906, #2027, #91, #17762, #10284, #14149, #11977, #18146, #19682, #20068, #8354, #23538, #2529, #23675, #15940, #14021, #2405, #3970, #21876, #2153, #6036, #23793, #470, #4486, #16196, #13891, #18021, #24046, #10033, #10409, #6420, #4230, #12354, #19944, #14270, #20196, #2280, #18274, #602, #16068, #15689, #21745, #17897, #23919, #19232, #12608, #6535, #20444, #17065, #8476, #17184, #19119, #23095, #4735, #16442, #10666, #1458, #10540, #9338, #14394, #15242, #25008, #22500, #4855, #13200, #20327, #21051, #14642, #7398, #18989, #13070 ),
 ( #8735, #24291, #12483, #5456, #11273, #11137, #6658, #2659, #22248, #13326, #18514, #3516, #21177, #11391, #24161, #18386, #844, #14521, #3393, #16569, #16311, #1330, #20921, #4609, #720, #9216, #22378, #2776, #8603, #24420, #6793, #3262, #22971, #24884, #7263, #15114, #5335, #11522, #13443, #17312, #23218, #12033, #7905, #19610, #3635, #7520, #13698, #17441, #11778, #23, #1953, #7777, #15752, #23607, #1570, #23727, #9836, #5969, #23472, #13948, #21556, #1696, #5708, #21423, #21805, #8034, #9463, #1830, #4028, #3767, #21677, #19361, #25134, #15368, #4163, #2085, #5585, #13819, #9591, #25268, #11650, #3904, #21294, #17693, #19487, #7649, #15490, #11901, #23342, #15874, #17825, #13571, #9713, #17564, #25392, #19742, #15621, #9966, #6093, #155, #5837, #6595, #17953, #529, #10095, #779, #20251, #18077, #12410, #16124, #273, #20125, #14453, #6720, #23976, #8152, #6220, #6471, #19876, #2338, #24346, #2215, #6353, #18329, #8671, #2589, #653, #14212, #10474, #15996, #14328, #10338, #8281, #12162, #19998, #8538, #23847, #16253, #14078, #4546, #4416, #22181, #21932, #16371, #14576, #2461, #10214, #16501, #22052, #12283, #22434, #18449, #4294, #12544, #399, #18201, #20380, #8413, #24098, #24219, #22307, #4666, #2710, #10598, #4784, #9184, #20890, #10853, #7359, #18702, #24471, #23061, #3226, #2837, #12916, #7237, #24980, #16762, #10726, #6844, #24730, #12663, #20633, #17153, #20505, #24596, #11104, #19089, #5181, #18959, #6978, #1297, #18572, #7106, #3100, #1037, #4917, #12789, #17030, #907, #9056, #8797, #22819, #22687, #14961, #14700, #13034, #15208, #20769, #2968, #9312, #14829, #5044, #16635, #11238, #22562, #5301, #8918, #10972, #13166, #18825, #1163, #16897, #24860, #15083, #22937, #21020, #3361, #1428, #13667, #3608, #125, #11491, #17277, #15843, #21523, #11363, #17539, #21263, #15588, #3871, #23445, #11612, #11749, #19585, #5426, #2058, #5811, #1922, #1797, #17793, #25361, #5554, #9555, #25238, #8007, #11876, #13295, #5676, #7877, #7621, #3877, #23188, #21145, #19204, #3489, #5937, #1542, #9809, #13416, #7483, #15462, #7747, #9432, #17665, #23309, #25102, #19331, #15721, #15339, #19710, #21647, #1663, #13539, #17405, #21395, #23574, #3737, #13793, #9936, #3998, #19455, #9689, #21777, #4389, #13922, #4635, #24074, #21902, #16225, #19974, #8383, #22148, #6444, #12249, #4510, #12382, #8637, #20353, #14298, #20221 ),
 ( #23945, #624, #367, #18301, #15965, #4135, #12005, #751, #24191, #19843, #2559, #23821, #241, #18047, #18174, #2186, #10441, #16096, #10065, #4265, #496, #17924, #12515, #14424, #8121, #6321, #2306, #6195, #8507, #14047, #16340, #2682, #22275, #12134, #6563, #10179, #20093, #8253, #10565, #18420, #14183, #23698, #22027, #2433, #10311, #6062, #3332, #20606, #6686, #2810, #3071, #16469, #24447, #20992, #24315, #2936, #14930, #22909, #9020, #22790, #10817, #7073, #22407, #10944, #6946, #4884, #8763, #16602, #5150, #14548, #12885, #12631, #1133, #1009, #18795, #10700, #16867, #11207, #24563, #6820, #13138, #18670, #8892, #19060, #15052, #4756, #9153, #20473, #16733, #16999, #14802, #18545, #12762, #13008, #14666, #20737, #20858, #18930, #3197, #24703, #22529, #1403, #22661, #871, #5015, #11075, #1272, #24833, #7212, #5271, #21119, #11590, #7718, #5533, #21625, #13641, #9532, #23542, #7596, #19560, #7851, #25207, #3841, #3973, #15438, #19685, #17129, #11724, #5646, #9285, #13395, #7331, #21239, #17513, #24947, #17639, #1895, #5911, #3580, #17250, #11462, #9781, #11339, #25468, #15180, #15693, #13772, #23287, #13513, #21495, #3464, #11847, #21362, #23036, #19423, #3706, #5402, #1769, #7460, #9665, #5781, #15310, #13265, #19181, #23158, #17376, #25074, #1515, #9401, #19300, #25336, #1637, #15559, #23414, #18279, #4236, #22255, #20201, #12360, #17768, #4109, #12107, #10036, #22125, #10159, #4615, #20071, #23923, #12489, #9910, #2410, #223, #15943, #10415, #14400, #2031, #19948, #16199, #607, #6165, #2283, #8484, #11982, #13894, #96, #23678, #7981, #8358, #10288, #19819, #24051, #15823, #18025, #21749, #2159, #17900, #8100, #4490, #474, #23797, #2535, #6039, #6424, #16318, #14025, #21881, #344, #8227, #16072, #14274, #6296, #14155, #22008, #4363, #12225, #18150, #24166, #6541, #22384, #14648, #14777, #16448, #12857, #12735, #726, #850, #22635, #8610, #9128, #11046, #10546, #20578, #24426, #24297, #14901, #12613, #3046, #16972, #18903, #20452, #7049, #18395, #984, #6665, #1247, #20711, #18519, #10925, #16577, #14527, #2911, #22761, #7185, #6799, #4740, #2783, #6925, #20332, #10673, #24805, #2664, #22508, #18773, #15032, #1109, #8994, #4861, #16842, #8741, #4991, #10794, #18645, #8872, #16710, #24677, #24543, #5128, #12989, #20838, #3176, #22887, #5249, #23263, #17609, #21216, #13244, #9758, #17228, #15284, #15666, #11698 ) ),
 .UNSPECIFIED., .T., .F., .F. ) 
 B_SPLINE_SURFACE_WITH_KNOTS ( ( 4, 3, 4 ),
 ( 3, 2, 2, 2, 2, 2, 2, 2, 2, 2, 2, 2, 2, 2, 2, 2, 2, 2, 2, 2, 2, 2, 2, 2, 2, 2, 2, 2, 2, 2, 2, 2, 2, 2, 2, 2, 2, 2, 2, 2, 2, 2, 2, 2, 2, 2, 2, 2, 2, 2, 2, 2, 2, 2, 2, 2, 2, 2, 2, 2, 2, 2, 2, 2, 2, 2, 2, 2, 2, 2, 2, 2, 2, 2, 2, 2, 2, 2, 2, 2, 2, 2, 2, 2, 2, 2, 2, 2, 2, 2, 2, 2, 2, 2, 2, 2, 2, 2, 2, 2, 2, 2, 2, 2, 2, 2, 2, 2, 2, 2, 2, 2, 2, 2, 2, 2, 2, 2, 2, 2, 2, 2, 2, 2, 2, 2, 2, 2, 2, 2, 2, 2, 2, 2, 2, 2, 2, 2, 2, 2, 2, 2, 2, 2, 2, 2, 2, 2, 2, 2, 2, 2, 2, 2, 2, 3 ),
 ( 0.000000000000000000, 0.5000000000000000000, 1.000000000000000000 ),
 ( 0.000000000000000000, 0.006250000000000000347, 0.01250000000000000069, 0.01874999999999999931, 0.02500000000000000139, 0.03125000000000000000, 0.03749999999999999861, 0.04374999999999999722, 0.05000000000000000278, 0.05625000000000000139, 0.06250000000000000000, 0.06875000000000000555, 0.07499999999999999722, 0.08125000000000000278, 0.08749999999999999445, 0.09375000000000000000, 0.1000000000000000056, 0.1062499999999999972, 0.1125000000000000028, 0.1187499999999999944, 0.1250000000000000000, 0.1312500000000000056, 0.1375000000000000111, 0.1437499999999999889, 0.1499999999999999944, 0.1562500000000000000, 0.1625000000000000056, 0.1687500000000000111, 0.1749999999999999889, 0.1812499999999999944, 0.1875000000000000000, 0.1937500000000000056, 0.2000000000000000111, 0.2062499999999999889, 0.2124999999999999944, 0.2187500000000000000, 0.2250000000000000056, 0.2312500000000000111, 0.2374999999999999889, 0.2437499999999999944, 0.2500000000000000000, 0.2562499999999999778, 0.2625000000000000111, 0.2687499999999999889, 0.2750000000000000222, 0.2812500000000000000, 0.2874999999999999778, 0.2937500000000000111, 0.2999999999999999889, 0.3062500000000000222, 0.3125000000000000000, 0.3187499999999999778, 0.3250000000000000111, 0.3312499999999999889, 0.3375000000000000222, 0.3437500000000000000, 0.3499999999999999778, 0.3562500000000000111, 0.3624999999999999889, 0.3687500000000000222, 0.3750000000000000000, 0.3812499999999999778, 0.3875000000000000111, 0.3937499999999999889, 0.4000000000000000222, 0.4062500000000000000, 0.4124999999999999778, 0.4187500000000000111, 0.4249999999999999889, 0.4312500000000000222, 0.4375000000000000000, 0.4437499999999999778, 0.4500000000000000111, 0.4562499999999999889, 0.4625000000000000222, 0.4687500000000000000, 0.4749999999999999778, 0.4812500000000000111, 0.4874999999999999889, 0.4937500000000000222, 0.5000000000000000000, 0.5062499999999999778, 0.5124999999999999556, 0.5187500000000000444, 0.5250000000000000222, 0.5312500000000000000, 0.5374999999999999778, 0.5437499999999999556, 0.5500000000000000444, 0.5562500000000000222, 0.5625000000000000000, 0.5687499999999999778, 0.5749999999999999556, 0.5812500000000000444, 0.5875000000000000222, 0.5937500000000000000, 0.5999999999999999778, 0.6062499999999999556, 0.6125000000000000444, 0.6187500000000000222, 0.6250000000000000000, 0.6312499999999999778, 0.6374999999999999556, 0.6437500000000000444, 0.6500000000000000222, 0.6562500000000000000, 0.6624999999999999778, 0.6687499999999999556, 0.6750000000000000444, 0.6812500000000000222, 0.6875000000000000000, 0.6937499999999999778, 0.6999999999999999556, 0.7062500000000000444, 0.7125000000000000222, 0.7187500000000000000, 0.7249999999999999778, 0.7312499999999999556, 0.7375000000000000444, 0.7437500000000000222, 0.7500000000000000000, 0.7562499999999999778, 0.7624999999999999556, 0.7687500000000000444, 0.7750000000000000222, 0.7812500000000000000, 0.7874999999999999778, 0.7937499999999999556, 0.8000000000000000444, 0.8062500000000000222, 0.8125000000000000000, 0.8187499999999999778, 0.8249999999999999556, 0.8312500000000000444, 0.8375000000000000222, 0.8437500000000000000, 0.8499999999999999778, 0.8562499999999999556, 0.8625000000000000444, 0.8687500000000000222, 0.8750000000000000000, 0.8812499999999999778, 0.8874999999999999556, 0.8937500000000000444, 0.9000000000000000222, 0.9062500000000000000, 0.9124999999999999778, 0.9187499999999999556, 0.9250000000000000444, 0.9312500000000000222, 0.9375000000000000000, 0.9437499999999999778, 0.9499999999999999556, 0.9562500000000000444, 0.9625000000000000222, 0.9687500000000000000 ),
 .UNSPECIFIED. ) 
 GEOMETRIC_REPRESENTATION_ITEM ( )  RATIONAL_B_SPLINE_SURFACE ( (
 ( 1.000000000000000000, 0.9510565162951535312, 1.000000000000000000, 0.9510565162951535312, 1.000000000000000000, 0.9510565162951535312, 1.000000000000000000, 0.9510565162951535312, 1.000000000000000000, 0.9510565162951535312, 1.000000000000000000, 0.9510565162951535312, 1.000000000000000000, 0.9510565162951535312, 1.000000000000000000, 0.9510565162951535312, 1.000000000000000000, 0.9510565162951535312, 1.000000000000000000, 0.9510565162951535312, 1.000000000000000000, 0.9510565162951535312, 1.000000000000000000, 0.9510565162951535312, 1.000000000000000000, 0.9510565162951535312, 1.000000000000000000, 0.9510565162951535312, 1.000000000000000000, 0.9510565162951535312, 1.000000000000000000, 0.9510565162951535312, 1.000000000000000000, 0.9510565162951535312, 1.000000000000000000, 0.9510565162951535312, 1.000000000000000000, 0.9510565162951535312, 1.000000000000000000, 0.9510565162951535312, 1.000000000000000000, 0.9510565162951535312, 1.000000000000000000, 0.9510565162951535312, 1.000000000000000000, 0.9510565162951535312, 1.000000000000000000, 0.9510565162951535312, 1.000000000000000000, 0.9510565162951535312, 1.000000000000000000, 0.9510565162951535312, 1.000000000000000000, 0.9510565162951535312, 1.000000000000000000, 0.9510565162951535312, 1.000000000000000000, 0.9510565162951535312, 1.000000000000000000, 0.9510565162951535312, 1.000000000000000000, 0.9510565162951535312, 1.000000000000000000, 0.9510565162951535312, 1.000000000000000000, 0.9510565162951535312, 1.000000000000000000, 0.9510565162951535312, 1.000000000000000000, 0.9510565162951535312, 1.000000000000000000, 0.9510565162951535312, 1.000000000000000000, 0.9510565162951535312, 1.000000000000000000, 0.9510565162951535312, 1.000000000000000000, 0.9510565162951535312, 1.000000000000000000, 0.9510565162951535312, 1.000000000000000000, 0.9510565162951535312, 1.000000000000000000, 0.9510565162951535312, 1.000000000000000000, 0.9510565162951535312, 1.000000000000000000, 0.9510565162951535312, 1.000000000000000000, 0.9510565162951535312, 1.000000000000000000, 0.9510565162951535312, 1.000000000000000000, 0.9510565162951535312, 1.000000000000000000, 0.9510565162951535312, 1.000000000000000000, 0.9510565162951535312, 1.000000000000000000, 0.9510565162951535312, 1.000000000000000000, 0.9510565162951535312, 1.000000000000000000, 0.9510565162951535312, 1.000000000000000000, 0.9510565162951535312, 1.000000000000000000, 0.9510565162951535312, 1.000000000000000000, 0.9510565162951535312, 1.000000000000000000, 0.9510565162951535312, 1.000000000000000000, 0.9510565162951535312, 1.000000000000000000, 0.9510565162951535312, 1.000000000000000000, 0.9510565162951535312, 1.000000000000000000, 0.9510565162951535312, 1.000000000000000000, 0.9510565162951535312, 1.000000000000000000, 0.9510565162951535312, 1.000000000000000000, 0.9510565162951535312, 1.000000000000000000, 0.9510565162951535312, 1.000000000000000000, 0.9510565162951535312, 1.000000000000000000, 0.9510565162951535312, 1.000000000000000000, 0.9510565162951535312, 1.000000000000000000, 0.9510565162951535312, 1.000000000000000000, 0.9510565162951535312, 1.000000000000000000, 0.9510565162951535312, 1.000000000000000000, 0.9510565162951535312, 1.000000000000000000, 0.9510565162951535312, 1.000000000000000000, 0.9510565162951535312, 1.000000000000000000, 0.9510565162951535312, 1.000000000000000000, 0.9510565162951535312, 1.000000000000000000, 0.9510565162951535312, 1.000000000000000000, 0.9510565162951535312, 1.000000000000000000, 0.9510565162951535312, 1.000000000000000000, 0.9510565162951535312, 1.000000000000000000, 0.9510565162951535312, 1.000000000000000000, 0.9510565162951535312, 1.000000000000000000, 0.9510565162951535312, 1.000000000000000000, 0.9510565162951535312, 1.000000000000000000, 0.9510565162951535312, 1.000000000000000000, 0.9510565162951535312, 1.000000000000000000, 0.9510565162951535312, 1.000000000000000000, 0.9510565162951535312, 1.000000000000000000, 0.9510565162951535312, 1.000000000000000000, 0.9510565162951535312, 1.000000000000000000, 0.9510565162951535312, 1.000000000000000000, 0.9510565162951535312, 1.000000000000000000, 0.9510565162951535312, 1.000000000000000000, 0.9510565162951535312, 1.000000000000000000, 0.9510565162951535312, 1.000000000000000000, 0.9510565162951535312, 1.000000000000000000, 0.9510565162951535312, 1.000000000000000000, 0.9510565162951535312, 1.000000000000000000, 0.9510565162951535312, 1.000000000000000000, 0.9510565162951535312, 1.000000000000000000, 0.9510565162951535312, 1.000000000000000000, 0.9510565162951535312, 1.000000000000000000, 0.9510565162951535312, 1.000000000000000000, 0.9510565162951535312, 1.000000000000000000, 0.9510565162951535312, 1.000000000000000000, 0.9510565162951535312, 1.000000000000000000, 0.9510565162951535312, 1.000000000000000000, 0.9510565162951535312, 1.000000000000000000, 0.9510565162951535312, 1.000000000000000000, 0.9510565162951535312, 1.000000000000000000, 0.9510565162951535312, 1.000000000000000000, 0.9510565162951535312, 1.000000000000000000, 0.9510565162951535312, 1.000000000000000000, 0.9510565162951535312, 1.000000000000000000, 0.9510565162951535312, 1.000000000000000000, 0.9510565162951535312, 1.000000000000000000, 0.9510565162951535312, 1.000000000000000000, 0.9510565162951535312, 1.000000000000000000, 0.9510565162951535312, 1.000000000000000000, 0.9510565162951535312, 1.000000000000000000, 0.9510565162951535312, 1.000000000000000000, 0.9510565162951535312, 1.000000000000000000, 0.9510565162951535312, 1.000000000000000000, 0.9510565162951535312, 1.000000000000000000, 0.9510565162951535312, 1.000000000000000000, 0.9510565162951535312, 1.000000000000000000, 0.9510565162951535312, 1.000000000000000000, 0.9510565162951535312, 1.000000000000000000, 0.9510565162951535312, 1.000000000000000000, 0.9510565162951535312, 1.000000000000000000, 0.9510565162951535312, 1.000000000000000000, 0.9510565162951535312, 1.000000000000000000, 0.9510565162951535312, 1.000000000000000000, 0.9510565162951535312, 1.000000000000000000, 0.9510565162951535312, 1.000000000000000000, 0.9510565162951535312, 1.000000000000000000, 0.9510565162951535312, 1.000000000000000000, 0.9510565162951535312, 1.000000000000000000, 0.9510565162951535312, 1.000000000000000000, 0.9510565162951535312, 1.000000000000000000, 0.9510565162951535312, 1.000000000000000000, 0.9510565162951535312, 1.000000000000000000, 0.9510565162951535312, 1.000000000000000000, 0.9510565162951535312, 1.000000000000000000, 0.9510565162951535312, 1.000000000000000000, 0.9510565162951535312, 1.000000000000000000, 0.9510565162951535312, 1.000000000000000000, 0.9510565162951535312, 1.000000000000000000, 0.9510565162951535312, 1.000000000000000000, 0.9510565162951535312, 1.000000000000000000, 0.9510565162951535312, 1.000000000000000000, 0.9510565162951535312, 1.000000000000000000, 0.9510565162951535312, 1.000000000000000000, 0.9510565162951535312, 1.000000000000000000, 0.9510565162951535312, 1.000000000000000000, 0.9510565162951535312, 1.000000000000000000),
 ( 0.3333333333333333703, 0.3170188387650512141, 0.3333333333333333703, 0.3170188387650512141, 0.3333333333333333703, 0.3170188387650512141, 0.3333333333333333703, 0.3170188387650512141, 0.3333333333333333703, 0.3170188387650512141, 0.3333333333333333703, 0.3170188387650512141, 0.3333333333333333703, 0.3170188387650512141, 0.3333333333333333703, 0.3170188387650512141, 0.3333333333333333703, 0.3170188387650512141, 0.3333333333333333703, 0.3170188387650512141, 0.3333333333333333703, 0.3170188387650512141, 0.3333333333333333703, 0.3170188387650512141, 0.3333333333333333703, 0.3170188387650512141, 0.3333333333333333703, 0.3170188387650512141, 0.3333333333333333703, 0.3170188387650512141, 0.3333333333333333703, 0.3170188387650512141, 0.3333333333333333703, 0.3170188387650512141, 0.3333333333333333703, 0.3170188387650512141, 0.3333333333333333703, 0.3170188387650512141, 0.3333333333333333703, 0.3170188387650512141, 0.3333333333333333703, 0.3170188387650512141, 0.3333333333333333703, 0.3170188387650512141, 0.3333333333333333703, 0.3170188387650512141, 0.3333333333333333703, 0.3170188387650512141, 0.3333333333333333703, 0.3170188387650512141, 0.3333333333333333703, 0.3170188387650512141, 0.3333333333333333703, 0.3170188387650512141, 0.3333333333333333703, 0.3170188387650512141, 0.3333333333333333703, 0.3170188387650512141, 0.3333333333333333703, 0.3170188387650512141, 0.3333333333333333703, 0.3170188387650512141, 0.3333333333333333703, 0.3170188387650512141, 0.3333333333333333703, 0.3170188387650512141, 0.3333333333333333703, 0.3170188387650512141, 0.3333333333333333703, 0.3170188387650512141, 0.3333333333333333703, 0.3170188387650512141, 0.3333333333333333703, 0.3170188387650512141, 0.3333333333333333703, 0.3170188387650512141, 0.3333333333333333703, 0.3170188387650512141, 0.3333333333333333703, 0.3170188387650512141, 0.3333333333333333703, 0.3170188387650512141, 0.3333333333333333703, 0.3170188387650512141, 0.3333333333333333703, 0.3170188387650512141, 0.3333333333333333703, 0.3170188387650512141, 0.3333333333333333703, 0.3170188387650512141, 0.3333333333333333703, 0.3170188387650512141, 0.3333333333333333703, 0.3170188387650512141, 0.3333333333333333703, 0.3170188387650512141, 0.3333333333333333703, 0.3170188387650512141, 0.3333333333333333703, 0.3170188387650512141, 0.3333333333333333703, 0.3170188387650512141, 0.3333333333333333703, 0.3170188387650512141, 0.3333333333333333703, 0.3170188387650512141, 0.3333333333333333703, 0.3170188387650512141, 0.3333333333333333703, 0.3170188387650512141, 0.3333333333333333703, 0.3170188387650512141, 0.3333333333333333703, 0.3170188387650512141, 0.3333333333333333703, 0.3170188387650512141, 0.3333333333333333703, 0.3170188387650512141, 0.3333333333333333703, 0.3170188387650512141, 0.3333333333333333703, 0.3170188387650512141, 0.3333333333333333703, 0.3170188387650512141, 0.3333333333333333703, 0.3170188387650512141, 0.3333333333333333703, 0.3170188387650512141, 0.3333333333333333703, 0.3170188387650512141, 0.3333333333333333703, 0.3170188387650512141, 0.3333333333333333703, 0.3170188387650512141, 0.3333333333333333703, 0.3170188387650512141, 0.3333333333333333703, 0.3170188387650512141, 0.3333333333333333703, 0.3170188387650512141, 0.3333333333333333703, 0.3170188387650512141, 0.3333333333333333703, 0.3170188387650512141, 0.3333333333333333703, 0.3170188387650512141, 0.3333333333333333703, 0.3170188387650512141, 0.3333333333333333703, 0.3170188387650512141, 0.3333333333333333703, 0.3170188387650512141, 0.3333333333333333703, 0.3170188387650512141, 0.3333333333333333703, 0.3170188387650512141, 0.3333333333333333703, 0.3170188387650512141, 0.3333333333333333703, 0.3170188387650512141, 0.3333333333333333703, 0.3170188387650512141, 0.3333333333333333703, 0.3170188387650512141, 0.3333333333333333703, 0.3170188387650512141, 0.3333333333333333703, 0.3170188387650512141, 0.3333333333333333703, 0.3170188387650512141, 0.3333333333333333703, 0.3170188387650512141, 0.3333333333333333703, 0.3170188387650512141, 0.3333333333333333703, 0.3170188387650512141, 0.3333333333333333703, 0.3170188387650512141, 0.3333333333333333703, 0.3170188387650512141, 0.3333333333333333703, 0.3170188387650512141, 0.3333333333333333703, 0.3170188387650512141, 0.3333333333333333703, 0.3170188387650512141, 0.3333333333333333703, 0.3170188387650512141, 0.3333333333333333703, 0.3170188387650512141, 0.3333333333333333703, 0.3170188387650512141, 0.3333333333333333703, 0.3170188387650512141, 0.3333333333333333703, 0.3170188387650512141, 0.3333333333333333703, 0.3170188387650512141, 0.3333333333333333703, 0.3170188387650512141, 0.3333333333333333703, 0.3170188387650512141, 0.3333333333333333703, 0.3170188387650512141, 0.3333333333333333703, 0.3170188387650512141, 0.3333333333333333703, 0.3170188387650512141, 0.3333333333333333703, 0.3170188387650512141, 0.3333333333333333703, 0.3170188387650512141, 0.3333333333333333703, 0.3170188387650512141, 0.3333333333333333703, 0.3170188387650512141, 0.3333333333333333703, 0.3170188387650512141, 0.3333333333333333703, 0.3170188387650512141, 0.3333333333333333703, 0.3170188387650512141, 0.3333333333333333703, 0.3170188387650512141, 0.3333333333333333703, 0.3170188387650512141, 0.3333333333333333703, 0.3170188387650512141, 0.3333333333333333703, 0.3170188387650512141, 0.3333333333333333703, 0.3170188387650512141, 0.3333333333333333703, 0.3170188387650512141, 0.3333333333333333703, 0.3170188387650512141, 0.3333333333333333703, 0.3170188387650512141, 0.3333333333333333703, 0.3170188387650512141, 0.3333333333333333703, 0.3170188387650512141, 0.3333333333333333703, 0.3170188387650512141, 0.3333333333333333703, 0.3170188387650512141, 0.3333333333333333703, 0.3170188387650512141, 0.3333333333333333703, 0.3170188387650512141, 0.3333333333333333703, 0.3170188387650512141, 0.3333333333333333703, 0.3170188387650512141, 0.3333333333333333703, 0.3170188387650512141, 0.3333333333333333703, 0.3170188387650512141, 0.3333333333333333703, 0.3170188387650512141, 0.3333333333333333703, 0.3170188387650512141, 0.3333333333333333703, 0.3170188387650512141, 0.3333333333333333703, 0.3170188387650512141, 0.3333333333333333703, 0.3170188387650512141, 0.3333333333333333703, 0.3170188387650512141, 0.3333333333333333703, 0.3170188387650512141, 0.3333333333333333703, 0.3170188387650512141, 0.3333333333333333703, 0.3170188387650512141, 0.3333333333333333703, 0.3170188387650512141, 0.3333333333333333703, 0.3170188387650512141, 0.3333333333333333703, 0.3170188387650512141, 0.3333333333333333703, 0.3170188387650512141, 0.3333333333333333703, 0.3170188387650512141, 0.3333333333333333703, 0.3170188387650512141, 0.3333333333333333703, 0.3170188387650512141, 0.3333333333333333703, 0.3170188387650512141, 0.3333333333333333703, 0.3170188387650512141, 0.3333333333333333703, 0.3170188387650512141, 0.3333333333333333703, 0.3170188387650512141, 0.3333333333333333703, 0.3170188387650512141, 0.3333333333333333703, 0.3170188387650512141, 0.3333333333333333703, 0.3170188387650512141, 0.3333333333333333703, 0.3170188387650512141, 0.3333333333333333703, 0.3170188387650512141, 0.3333333333333333703, 0.3170188387650512141, 0.3333333333333333703),
 ( 0.3333333333333333703, 0.3170188387650512141, 0.3333333333333333703, 0.3170188387650512141, 0.3333333333333333703, 0.3170188387650512141, 0.3333333333333333703, 0.3170188387650512141, 0.3333333333333333703, 0.3170188387650512141, 0.3333333333333333703, 0.3170188387650512141, 0.3333333333333333703, 0.3170188387650512141, 0.3333333333333333703, 0.3170188387650512141, 0.3333333333333333703, 0.3170188387650512141, 0.3333333333333333703, 0.3170188387650512141, 0.3333333333333333703, 0.3170188387650512141, 0.3333333333333333703, 0.3170188387650512141, 0.3333333333333333703, 0.3170188387650512141, 0.3333333333333333703, 0.3170188387650512141, 0.3333333333333333703, 0.3170188387650512141, 0.3333333333333333703, 0.3170188387650512141, 0.3333333333333333703, 0.3170188387650512141, 0.3333333333333333703, 0.3170188387650512141, 0.3333333333333333703, 0.3170188387650512141, 0.3333333333333333703, 0.3170188387650512141, 0.3333333333333333703, 0.3170188387650512141, 0.3333333333333333703, 0.3170188387650512141, 0.3333333333333333703, 0.3170188387650512141, 0.3333333333333333703, 0.3170188387650512141, 0.3333333333333333703, 0.3170188387650512141, 0.3333333333333333703, 0.3170188387650512141, 0.3333333333333333703, 0.3170188387650512141, 0.3333333333333333703, 0.3170188387650512141, 0.3333333333333333703, 0.3170188387650512141, 0.3333333333333333703, 0.3170188387650512141, 0.3333333333333333703, 0.3170188387650512141, 0.3333333333333333703, 0.3170188387650512141, 0.3333333333333333703, 0.3170188387650512141, 0.3333333333333333703, 0.3170188387650512141, 0.3333333333333333703, 0.3170188387650512141, 0.3333333333333333703, 0.3170188387650512141, 0.3333333333333333703, 0.3170188387650512141, 0.3333333333333333703, 0.3170188387650512141, 0.3333333333333333703, 0.3170188387650512141, 0.3333333333333333703, 0.3170188387650512141, 0.3333333333333333703, 0.3170188387650512141, 0.3333333333333333703, 0.3170188387650512141, 0.3333333333333333703, 0.3170188387650512141, 0.3333333333333333703, 0.3170188387650512141, 0.3333333333333333703, 0.3170188387650512141, 0.3333333333333333703, 0.3170188387650512141, 0.3333333333333333703, 0.3170188387650512141, 0.3333333333333333703, 0.3170188387650512141, 0.3333333333333333703, 0.3170188387650512141, 0.3333333333333333703, 0.3170188387650512141, 0.3333333333333333703, 0.3170188387650512141, 0.3333333333333333703, 0.3170188387650512141, 0.3333333333333333703, 0.3170188387650512141, 0.3333333333333333703, 0.3170188387650512141, 0.3333333333333333703, 0.3170188387650512141, 0.3333333333333333703, 0.3170188387650512141, 0.3333333333333333703, 0.3170188387650512141, 0.3333333333333333703, 0.3170188387650512141, 0.3333333333333333703, 0.3170188387650512141, 0.3333333333333333703, 0.3170188387650512141, 0.3333333333333333703, 0.3170188387650512141, 0.3333333333333333703, 0.3170188387650512141, 0.3333333333333333703, 0.3170188387650512141, 0.3333333333333333703, 0.3170188387650512141, 0.3333333333333333703, 0.3170188387650512141, 0.3333333333333333703, 0.3170188387650512141, 0.3333333333333333703, 0.3170188387650512141, 0.3333333333333333703, 0.3170188387650512141, 0.3333333333333333703, 0.3170188387650512141, 0.3333333333333333703, 0.3170188387650512141, 0.3333333333333333703, 0.3170188387650512141, 0.3333333333333333703, 0.3170188387650512141, 0.3333333333333333703, 0.3170188387650512141, 0.3333333333333333703, 0.3170188387650512141, 0.3333333333333333703, 0.3170188387650512141, 0.3333333333333333703, 0.3170188387650512141, 0.3333333333333333703, 0.3170188387650512141, 0.3333333333333333703, 0.3170188387650512141, 0.3333333333333333703, 0.3170188387650512141, 0.3333333333333333703, 0.3170188387650512141, 0.3333333333333333703, 0.3170188387650512141, 0.3333333333333333703, 0.3170188387650512141, 0.3333333333333333703, 0.3170188387650512141, 0.3333333333333333703, 0.3170188387650512141, 0.3333333333333333703, 0.3170188387650512141, 0.3333333333333333703, 0.3170188387650512141, 0.3333333333333333703, 0.3170188387650512141, 0.3333333333333333703, 0.3170188387650512141, 0.3333333333333333703, 0.3170188387650512141, 0.3333333333333333703, 0.3170188387650512141, 0.3333333333333333703, 0.3170188387650512141, 0.3333333333333333703, 0.3170188387650512141, 0.3333333333333333703, 0.3170188387650512141, 0.3333333333333333703, 0.3170188387650512141, 0.3333333333333333703, 0.3170188387650512141, 0.3333333333333333703, 0.3170188387650512141, 0.3333333333333333703, 0.3170188387650512141, 0.3333333333333333703, 0.3170188387650512141, 0.3333333333333333703, 0.3170188387650512141, 0.3333333333333333703, 0.3170188387650512141, 0.3333333333333333703, 0.3170188387650512141, 0.3333333333333333703, 0.3170188387650512141, 0.3333333333333333703, 0.3170188387650512141, 0.3333333333333333703, 0.3170188387650512141, 0.3333333333333333703, 0.3170188387650512141, 0.3333333333333333703, 0.3170188387650512141, 0.3333333333333333703, 0.3170188387650512141, 0.3333333333333333703, 0.3170188387650512141, 0.3333333333333333703, 0.3170188387650512141, 0.3333333333333333703, 0.3170188387650512141, 0.3333333333333333703, 0.3170188387650512141, 0.3333333333333333703, 0.3170188387650512141, 0.3333333333333333703, 0.3170188387650512141, 0.3333333333333333703, 0.3170188387650512141, 0.3333333333333333703, 0.3170188387650512141, 0.3333333333333333703, 0.3170188387650512141, 0.3333333333333333703, 0.3170188387650512141, 0.3333333333333333703, 0.3170188387650512141, 0.3333333333333333703, 0.3170188387650512141, 0.3333333333333333703, 0.3170188387650512141, 0.3333333333333333703, 0.3170188387650512141, 0.3333333333333333703, 0.3170188387650512141, 0.3333333333333333703, 0.3170188387650512141, 0.3333333333333333703, 0.3170188387650512141, 0.3333333333333333703, 0.3170188387650512141, 0.3333333333333333703, 0.3170188387650512141, 0.3333333333333333703, 0.3170188387650512141, 0.3333333333333333703, 0.3170188387650512141, 0.3333333333333333703, 0.3170188387650512141, 0.3333333333333333703, 0.3170188387650512141, 0.3333333333333333703, 0.3170188387650512141, 0.3333333333333333703, 0.3170188387650512141, 0.3333333333333333703, 0.3170188387650512141, 0.3333333333333333703, 0.3170188387650512141, 0.3333333333333333703, 0.3170188387650512141, 0.3333333333333333703, 0.3170188387650512141, 0.3333333333333333703, 0.3170188387650512141, 0.3333333333333333703, 0.3170188387650512141, 0.3333333333333333703, 0.3170188387650512141, 0.3333333333333333703, 0.3170188387650512141, 0.3333333333333333703, 0.3170188387650512141, 0.3333333333333333703, 0.3170188387650512141, 0.3333333333333333703, 0.3170188387650512141, 0.3333333333333333703, 0.3170188387650512141, 0.3333333333333333703, 0.3170188387650512141, 0.3333333333333333703, 0.3170188387650512141, 0.3333333333333333703, 0.3170188387650512141, 0.3333333333333333703, 0.3170188387650512141, 0.3333333333333333703, 0.3170188387650512141, 0.3333333333333333703, 0.3170188387650512141, 0.3333333333333333703, 0.3170188387650512141, 0.3333333333333333703, 0.3170188387650512141, 0.3333333333333333703, 0.3170188387650512141, 0.3333333333333333703, 0.3170188387650512141, 0.3333333333333333703, 0.3170188387650512141, 0.3333333333333333703),
 ( 1.000000000000000000, 0.9510565162951535312, 1.000000000000000000, 0.9510565162951535312, 1.000000000000000000, 0.9510565162951535312, 1.000000000000000000, 0.9510565162951535312, 1.000000000000000000, 0.9510565162951535312, 1.000000000000000000, 0.9510565162951535312, 1.000000000000000000, 0.9510565162951535312, 1.000000000000000000, 0.9510565162951535312, 1.000000000000000000, 0.9510565162951535312, 1.000000000000000000, 0.9510565162951535312, 1.000000000000000000, 0.9510565162951535312, 1.000000000000000000, 0.9510565162951535312, 1.000000000000000000, 0.9510565162951535312, 1.000000000000000000, 0.9510565162951535312, 1.000000000000000000, 0.9510565162951535312, 1.000000000000000000, 0.9510565162951535312, 1.000000000000000000, 0.9510565162951535312, 1.000000000000000000, 0.9510565162951535312, 1.000000000000000000, 0.9510565162951535312, 1.000000000000000000, 0.9510565162951535312, 1.000000000000000000, 0.9510565162951535312, 1.000000000000000000, 0.9510565162951535312, 1.000000000000000000, 0.9510565162951535312, 1.000000000000000000, 0.9510565162951535312, 1.000000000000000000, 0.9510565162951535312, 1.000000000000000000, 0.9510565162951535312, 1.000000000000000000, 0.9510565162951535312, 1.000000000000000000, 0.9510565162951535312, 1.000000000000000000, 0.9510565162951535312, 1.000000000000000000, 0.9510565162951535312, 1.000000000000000000, 0.9510565162951535312, 1.000000000000000000, 0.9510565162951535312, 1.000000000000000000, 0.9510565162951535312, 1.000000000000000000, 0.9510565162951535312, 1.000000000000000000, 0.9510565162951535312, 1.000000000000000000, 0.9510565162951535312, 1.000000000000000000, 0.9510565162951535312, 1.000000000000000000, 0.9510565162951535312, 1.000000000000000000, 0.9510565162951535312, 1.000000000000000000, 0.9510565162951535312, 1.000000000000000000, 0.9510565162951535312, 1.000000000000000000, 0.9510565162951535312, 1.000000000000000000, 0.9510565162951535312, 1.000000000000000000, 0.9510565162951535312, 1.000000000000000000, 0.9510565162951535312, 1.000000000000000000, 0.9510565162951535312, 1.000000000000000000, 0.9510565162951535312, 1.000000000000000000, 0.9510565162951535312, 1.000000000000000000, 0.9510565162951535312, 1.000000000000000000, 0.9510565162951535312, 1.000000000000000000, 0.9510565162951535312, 1.000000000000000000, 0.9510565162951535312, 1.000000000000000000, 0.9510565162951535312, 1.000000000000000000, 0.9510565162951535312, 1.000000000000000000, 0.9510565162951535312, 1.000000000000000000, 0.9510565162951535312, 1.000000000000000000, 0.9510565162951535312, 1.000000000000000000, 0.9510565162951535312, 1.000000000000000000, 0.9510565162951535312, 1.000000000000000000, 0.9510565162951535312, 1.000000000000000000, 0.9510565162951535312, 1.000000000000000000, 0.9510565162951535312, 1.000000000000000000, 0.9510565162951535312, 1.000000000000000000, 0.9510565162951535312, 1.000000000000000000, 0.9510565162951535312, 1.000000000000000000, 0.9510565162951535312, 1.000000000000000000, 0.9510565162951535312, 1.000000000000000000, 0.9510565162951535312, 1.000000000000000000, 0.9510565162951535312, 1.000000000000000000, 0.9510565162951535312, 1.000000000000000000, 0.9510565162951535312, 1.000000000000000000, 0.9510565162951535312, 1.000000000000000000, 0.9510565162951535312, 1.000000000000000000, 0.9510565162951535312, 1.000000000000000000, 0.9510565162951535312, 1.000000000000000000, 0.9510565162951535312, 1.000000000000000000, 0.9510565162951535312, 1.000000000000000000, 0.9510565162951535312, 1.000000000000000000, 0.9510565162951535312, 1.000000000000000000, 0.9510565162951535312, 1.000000000000000000, 0.9510565162951535312, 1.000000000000000000, 0.9510565162951535312, 1.000000000000000000, 0.9510565162951535312, 1.000000000000000000, 0.9510565162951535312, 1.000000000000000000, 0.9510565162951535312, 1.000000000000000000, 0.9510565162951535312, 1.000000000000000000, 0.9510565162951535312, 1.000000000000000000, 0.9510565162951535312, 1.000000000000000000, 0.9510565162951535312, 1.000000000000000000, 0.9510565162951535312, 1.000000000000000000, 0.9510565162951535312, 1.000000000000000000, 0.9510565162951535312, 1.000000000000000000, 0.9510565162951535312, 1.000000000000000000, 0.9510565162951535312, 1.000000000000000000, 0.9510565162951535312, 1.000000000000000000, 0.9510565162951535312, 1.000000000000000000, 0.9510565162951535312, 1.000000000000000000, 0.9510565162951535312, 1.000000000000000000, 0.9510565162951535312, 1.000000000000000000, 0.9510565162951535312, 1.000000000000000000, 0.9510565162951535312, 1.000000000000000000, 0.9510565162951535312, 1.000000000000000000, 0.9510565162951535312, 1.000000000000000000, 0.9510565162951535312, 1.000000000000000000, 0.9510565162951535312, 1.000000000000000000, 0.9510565162951535312, 1.000000000000000000, 0.9510565162951535312, 1.000000000000000000, 0.9510565162951535312, 1.000000000000000000, 0.9510565162951535312, 1.000000000000000000, 0.9510565162951535312, 1.000000000000000000, 0.9510565162951535312, 1.000000000000000000, 0.9510565162951535312, 1.000000000000000000, 0.9510565162951535312, 1.000000000000000000, 0.9510565162951535312, 1.000000000000000000, 0.9510565162951535312, 1.000000000000000000, 0.9510565162951535312, 1.000000000000000000, 0.9510565162951535312, 1.000000000000000000, 0.9510565162951535312, 1.000000000000000000, 0.9510565162951535312, 1.000000000000000000, 0.9510565162951535312, 1.000000000000000000, 0.9510565162951535312, 1.000000000000000000, 0.9510565162951535312, 1.000000000000000000, 0.9510565162951535312, 1.000000000000000000, 0.9510565162951535312, 1.000000000000000000, 0.9510565162951535312, 1.000000000000000000, 0.9510565162951535312, 1.000000000000000000, 0.9510565162951535312, 1.000000000000000000, 0.9510565162951535312, 1.000000000000000000, 0.9510565162951535312, 1.000000000000000000, 0.9510565162951535312, 1.000000000000000000, 0.9510565162951535312, 1.000000000000000000, 0.9510565162951535312, 1.000000000000000000, 0.9510565162951535312, 1.000000000000000000, 0.9510565162951535312, 1.000000000000000000, 0.9510565162951535312, 1.000000000000000000, 0.9510565162951535312, 1.000000000000000000, 0.9510565162951535312, 1.000000000000000000, 0.9510565162951535312, 1.000000000000000000, 0.9510565162951535312, 1.000000000000000000, 0.9510565162951535312, 1.000000000000000000, 0.9510565162951535312, 1.000000000000000000, 0.9510565162951535312, 1.000000000000000000, 0.9510565162951535312, 1.000000000000000000, 0.9510565162951535312, 1.000000000000000000, 0.9510565162951535312, 1.000000000000000000, 0.9510565162951535312, 1.000000000000000000, 0.9510565162951535312, 1.000000000000000000, 0.9510565162951535312, 1.000000000000000000, 0.9510565162951535312, 1.000000000000000000, 0.9510565162951535312, 1.000000000000000000, 0.9510565162951535312, 1.000000000000000000, 0.9510565162951535312, 1.000000000000000000, 0.9510565162951535312, 1.000000000000000000, 0.9510565162951535312, 1.000000000000000000, 0.9510565162951535312, 1.000000000000000000),
 ( 0.3333333333333333703, 0.3170188387650512141, 0.3333333333333333703, 0.3170188387650512141, 0.3333333333333333703, 0.3170188387650512141, 0.3333333333333333703, 0.3170188387650512141, 0.3333333333333333703, 0.3170188387650512141, 0.3333333333333333703, 0.3170188387650512141, 0.3333333333333333703, 0.3170188387650512141, 0.3333333333333333703, 0.3170188387650512141, 0.3333333333333333703, 0.3170188387650512141, 0.3333333333333333703, 0.3170188387650512141, 0.3333333333333333703, 0.3170188387650512141, 0.3333333333333333703, 0.3170188387650512141, 0.3333333333333333703, 0.3170188387650512141, 0.3333333333333333703, 0.3170188387650512141, 0.3333333333333333703, 0.3170188387650512141, 0.3333333333333333703, 0.3170188387650512141, 0.3333333333333333703, 0.3170188387650512141, 0.3333333333333333703, 0.3170188387650512141, 0.3333333333333333703, 0.3170188387650512141, 0.3333333333333333703, 0.3170188387650512141, 0.3333333333333333703, 0.3170188387650512141, 0.3333333333333333703, 0.3170188387650512141, 0.3333333333333333703, 0.3170188387650512141, 0.3333333333333333703, 0.3170188387650512141, 0.3333333333333333703, 0.3170188387650512141, 0.3333333333333333703, 0.3170188387650512141, 0.3333333333333333703, 0.3170188387650512141, 0.3333333333333333703, 0.3170188387650512141, 0.3333333333333333703, 0.3170188387650512141, 0.3333333333333333703, 0.3170188387650512141, 0.3333333333333333703, 0.3170188387650512141, 0.3333333333333333703, 0.3170188387650512141, 0.3333333333333333703, 0.3170188387650512141, 0.3333333333333333703, 0.3170188387650512141, 0.3333333333333333703, 0.3170188387650512141, 0.3333333333333333703, 0.3170188387650512141, 0.3333333333333333703, 0.3170188387650512141, 0.3333333333333333703, 0.3170188387650512141, 0.3333333333333333703, 0.3170188387650512141, 0.3333333333333333703, 0.3170188387650512141, 0.3333333333333333703, 0.3170188387650512141, 0.3333333333333333703, 0.3170188387650512141, 0.3333333333333333703, 0.3170188387650512141, 0.3333333333333333703, 0.3170188387650512141, 0.3333333333333333703, 0.3170188387650512141, 0.3333333333333333703, 0.3170188387650512141, 0.3333333333333333703, 0.3170188387650512141, 0.3333333333333333703, 0.3170188387650512141, 0.3333333333333333703, 0.3170188387650512141, 0.3333333333333333703, 0.3170188387650512141, 0.3333333333333333703, 0.3170188387650512141, 0.3333333333333333703, 0.3170188387650512141, 0.3333333333333333703, 0.3170188387650512141, 0.3333333333333333703, 0.3170188387650512141, 0.3333333333333333703, 0.3170188387650512141, 0.3333333333333333703, 0.3170188387650512141, 0.3333333333333333703, 0.3170188387650512141, 0.3333333333333333703, 0.3170188387650512141, 0.3333333333333333703, 0.3170188387650512141, 0.3333333333333333703, 0.3170188387650512141, 0.3333333333333333703, 0.3170188387650512141, 0.3333333333333333703, 0.3170188387650512141, 0.3333333333333333703, 0.3170188387650512141, 0.3333333333333333703, 0.3170188387650512141, 0.3333333333333333703, 0.3170188387650512141, 0.3333333333333333703, 0.3170188387650512141, 0.3333333333333333703, 0.3170188387650512141, 0.3333333333333333703, 0.3170188387650512141, 0.3333333333333333703, 0.3170188387650512141, 0.3333333333333333703, 0.3170188387650512141, 0.3333333333333333703, 0.3170188387650512141, 0.3333333333333333703, 0.3170188387650512141, 0.3333333333333333703, 0.3170188387650512141, 0.3333333333333333703, 0.3170188387650512141, 0.3333333333333333703, 0.3170188387650512141, 0.3333333333333333703, 0.3170188387650512141, 0.3333333333333333703, 0.3170188387650512141, 0.3333333333333333703, 0.3170188387650512141, 0.3333333333333333703, 0.3170188387650512141, 0.3333333333333333703, 0.3170188387650512141, 0.3333333333333333703, 0.3170188387650512141, 0.3333333333333333703, 0.3170188387650512141, 0.3333333333333333703, 0.3170188387650512141, 0.3333333333333333703, 0.3170188387650512141, 0.3333333333333333703, 0.3170188387650512141, 0.3333333333333333703, 0.3170188387650512141, 0.3333333333333333703, 0.3170188387650512141, 0.3333333333333333703, 0.3170188387650512141, 0.3333333333333333703, 0.3170188387650512141, 0.3333333333333333703, 0.3170188387650512141, 0.3333333333333333703, 0.3170188387650512141, 0.3333333333333333703, 0.3170188387650512141, 0.3333333333333333703, 0.3170188387650512141, 0.3333333333333333703, 0.3170188387650512141, 0.3333333333333333703, 0.3170188387650512141, 0.3333333333333333703, 0.3170188387650512141, 0.3333333333333333703, 0.3170188387650512141, 0.3333333333333333703, 0.3170188387650512141, 0.3333333333333333703, 0.3170188387650512141, 0.3333333333333333703, 0.3170188387650512141, 0.3333333333333333703, 0.3170188387650512141, 0.3333333333333333703, 0.3170188387650512141, 0.3333333333333333703, 0.3170188387650512141, 0.3333333333333333703, 0.3170188387650512141, 0.3333333333333333703, 0.3170188387650512141, 0.3333333333333333703, 0.3170188387650512141, 0.3333333333333333703, 0.3170188387650512141, 0.3333333333333333703, 0.3170188387650512141, 0.3333333333333333703, 0.3170188387650512141, 0.3333333333333333703, 0.3170188387650512141, 0.3333333333333333703, 0.3170188387650512141, 0.3333333333333333703, 0.3170188387650512141, 0.3333333333333333703, 0.3170188387650512141, 0.3333333333333333703, 0.3170188387650512141, 0.3333333333333333703, 0.3170188387650512141, 0.3333333333333333703, 0.3170188387650512141, 0.3333333333333333703, 0.3170188387650512141, 0.3333333333333333703, 0.3170188387650512141, 0.3333333333333333703, 0.3170188387650512141, 0.3333333333333333703, 0.3170188387650512141, 0.3333333333333333703, 0.3170188387650512141, 0.3333333333333333703, 0.3170188387650512141, 0.3333333333333333703, 0.3170188387650512141, 0.3333333333333333703, 0.3170188387650512141, 0.3333333333333333703, 0.3170188387650512141, 0.3333333333333333703, 0.3170188387650512141, 0.3333333333333333703, 0.3170188387650512141, 0.3333333333333333703, 0.3170188387650512141, 0.3333333333333333703, 0.3170188387650512141, 0.3333333333333333703, 0.3170188387650512141, 0.3333333333333333703, 0.3170188387650512141, 0.3333333333333333703, 0.3170188387650512141, 0.3333333333333333703, 0.3170188387650512141, 0.3333333333333333703, 0.3170188387650512141, 0.3333333333333333703, 0.3170188387650512141, 0.3333333333333333703, 0.3170188387650512141, 0.3333333333333333703, 0.3170188387650512141, 0.3333333333333333703, 0.3170188387650512141, 0.3333333333333333703, 0.3170188387650512141, 0.3333333333333333703, 0.3170188387650512141, 0.3333333333333333703, 0.3170188387650512141, 0.3333333333333333703, 0.3170188387650512141, 0.3333333333333333703, 0.3170188387650512141, 0.3333333333333333703, 0.3170188387650512141, 0.3333333333333333703, 0.3170188387650512141, 0.3333333333333333703, 0.3170188387650512141, 0.3333333333333333703, 0.3170188387650512141, 0.3333333333333333703, 0.3170188387650512141, 0.3333333333333333703, 0.3170188387650512141, 0.3333333333333333703, 0.3170188387650512141, 0.3333333333333333703, 0.3170188387650512141, 0.3333333333333333703, 0.3170188387650512141, 0.3333333333333333703, 0.3170188387650512141, 0.3333333333333333703, 0.3170188387650512141, 0.3333333333333333703, 0.3170188387650512141, 0.3333333333333333703),
 ( 0.3333333333333333703, 0.3170188387650512141, 0.3333333333333333703, 0.3170188387650512141, 0.3333333333333333703, 0.3170188387650512141, 0.3333333333333333703, 0.3170188387650512141, 0.3333333333333333703, 0.3170188387650512141, 0.3333333333333333703, 0.3170188387650512141, 0.3333333333333333703, 0.3170188387650512141, 0.3333333333333333703, 0.3170188387650512141, 0.3333333333333333703, 0.3170188387650512141, 0.3333333333333333703, 0.3170188387650512141, 0.3333333333333333703, 0.3170188387650512141, 0.3333333333333333703, 0.3170188387650512141, 0.3333333333333333703, 0.3170188387650512141, 0.3333333333333333703, 0.3170188387650512141, 0.3333333333333333703, 0.3170188387650512141, 0.3333333333333333703, 0.3170188387650512141, 0.3333333333333333703, 0.3170188387650512141, 0.3333333333333333703, 0.3170188387650512141, 0.3333333333333333703, 0.3170188387650512141, 0.3333333333333333703, 0.3170188387650512141, 0.3333333333333333703, 0.3170188387650512141, 0.3333333333333333703, 0.3170188387650512141, 0.3333333333333333703, 0.3170188387650512141, 0.3333333333333333703, 0.3170188387650512141, 0.3333333333333333703, 0.3170188387650512141, 0.3333333333333333703, 0.3170188387650512141, 0.3333333333333333703, 0.3170188387650512141, 0.3333333333333333703, 0.3170188387650512141, 0.3333333333333333703, 0.3170188387650512141, 0.3333333333333333703, 0.3170188387650512141, 0.3333333333333333703, 0.3170188387650512141, 0.3333333333333333703, 0.3170188387650512141, 0.3333333333333333703, 0.3170188387650512141, 0.3333333333333333703, 0.3170188387650512141, 0.3333333333333333703, 0.3170188387650512141, 0.3333333333333333703, 0.3170188387650512141, 0.3333333333333333703, 0.3170188387650512141, 0.3333333333333333703, 0.3170188387650512141, 0.3333333333333333703, 0.3170188387650512141, 0.3333333333333333703, 0.3170188387650512141, 0.3333333333333333703, 0.3170188387650512141, 0.3333333333333333703, 0.3170188387650512141, 0.3333333333333333703, 0.3170188387650512141, 0.3333333333333333703, 0.3170188387650512141, 0.3333333333333333703, 0.3170188387650512141, 0.3333333333333333703, 0.3170188387650512141, 0.3333333333333333703, 0.3170188387650512141, 0.3333333333333333703, 0.3170188387650512141, 0.3333333333333333703, 0.3170188387650512141, 0.3333333333333333703, 0.3170188387650512141, 0.3333333333333333703, 0.3170188387650512141, 0.3333333333333333703, 0.3170188387650512141, 0.3333333333333333703, 0.3170188387650512141, 0.3333333333333333703, 0.3170188387650512141, 0.3333333333333333703, 0.3170188387650512141, 0.3333333333333333703, 0.3170188387650512141, 0.3333333333333333703, 0.3170188387650512141, 0.3333333333333333703, 0.3170188387650512141, 0.3333333333333333703, 0.3170188387650512141, 0.3333333333333333703, 0.3170188387650512141, 0.3333333333333333703, 0.3170188387650512141, 0.3333333333333333703, 0.3170188387650512141, 0.3333333333333333703, 0.3170188387650512141, 0.3333333333333333703, 0.3170188387650512141, 0.3333333333333333703, 0.3170188387650512141, 0.3333333333333333703, 0.3170188387650512141, 0.3333333333333333703, 0.3170188387650512141, 0.3333333333333333703, 0.3170188387650512141, 0.3333333333333333703, 0.3170188387650512141, 0.3333333333333333703, 0.3170188387650512141, 0.3333333333333333703, 0.3170188387650512141, 0.3333333333333333703, 0.3170188387650512141, 0.3333333333333333703, 0.3170188387650512141, 0.3333333333333333703, 0.3170188387650512141, 0.3333333333333333703, 0.3170188387650512141, 0.3333333333333333703, 0.3170188387650512141, 0.3333333333333333703, 0.3170188387650512141, 0.3333333333333333703, 0.3170188387650512141, 0.3333333333333333703, 0.3170188387650512141, 0.3333333333333333703, 0.3170188387650512141, 0.3333333333333333703, 0.3170188387650512141, 0.3333333333333333703, 0.3170188387650512141, 0.3333333333333333703, 0.3170188387650512141, 0.3333333333333333703, 0.3170188387650512141, 0.3333333333333333703, 0.3170188387650512141, 0.3333333333333333703, 0.3170188387650512141, 0.3333333333333333703, 0.3170188387650512141, 0.3333333333333333703, 0.3170188387650512141, 0.3333333333333333703, 0.3170188387650512141, 0.3333333333333333703, 0.3170188387650512141, 0.3333333333333333703, 0.3170188387650512141, 0.3333333333333333703, 0.3170188387650512141, 0.3333333333333333703, 0.3170188387650512141, 0.3333333333333333703, 0.3170188387650512141, 0.3333333333333333703, 0.3170188387650512141, 0.3333333333333333703, 0.3170188387650512141, 0.3333333333333333703, 0.3170188387650512141, 0.3333333333333333703, 0.3170188387650512141, 0.3333333333333333703, 0.3170188387650512141, 0.3333333333333333703, 0.3170188387650512141, 0.3333333333333333703, 0.3170188387650512141, 0.3333333333333333703, 0.3170188387650512141, 0.3333333333333333703, 0.3170188387650512141, 0.3333333333333333703, 0.3170188387650512141, 0.3333333333333333703, 0.3170188387650512141, 0.3333333333333333703, 0.3170188387650512141, 0.3333333333333333703, 0.3170188387650512141, 0.3333333333333333703, 0.3170188387650512141, 0.3333333333333333703, 0.3170188387650512141, 0.3333333333333333703, 0.3170188387650512141, 0.3333333333333333703, 0.3170188387650512141, 0.3333333333333333703, 0.3170188387650512141, 0.3333333333333333703, 0.3170188387650512141, 0.3333333333333333703, 0.3170188387650512141, 0.3333333333333333703, 0.3170188387650512141, 0.3333333333333333703, 0.3170188387650512141, 0.3333333333333333703, 0.3170188387650512141, 0.3333333333333333703, 0.3170188387650512141, 0.3333333333333333703, 0.3170188387650512141, 0.3333333333333333703, 0.3170188387650512141, 0.3333333333333333703, 0.3170188387650512141, 0.3333333333333333703, 0.3170188387650512141, 0.3333333333333333703, 0.3170188387650512141, 0.3333333333333333703, 0.3170188387650512141, 0.3333333333333333703, 0.3170188387650512141, 0.3333333333333333703, 0.3170188387650512141, 0.3333333333333333703, 0.3170188387650512141, 0.3333333333333333703, 0.3170188387650512141, 0.3333333333333333703, 0.3170188387650512141, 0.3333333333333333703, 0.3170188387650512141, 0.3333333333333333703, 0.3170188387650512141, 0.3333333333333333703, 0.3170188387650512141, 0.3333333333333333703, 0.3170188387650512141, 0.3333333333333333703, 0.3170188387650512141, 0.3333333333333333703, 0.3170188387650512141, 0.3333333333333333703, 0.3170188387650512141, 0.3333333333333333703, 0.3170188387650512141, 0.3333333333333333703, 0.3170188387650512141, 0.3333333333333333703, 0.3170188387650512141, 0.3333333333333333703, 0.3170188387650512141, 0.3333333333333333703, 0.3170188387650512141, 0.3333333333333333703, 0.3170188387650512141, 0.3333333333333333703, 0.3170188387650512141, 0.3333333333333333703, 0.3170188387650512141, 0.3333333333333333703, 0.3170188387650512141, 0.3333333333333333703, 0.3170188387650512141, 0.3333333333333333703, 0.3170188387650512141, 0.3333333333333333703, 0.3170188387650512141, 0.3333333333333333703, 0.3170188387650512141, 0.3333333333333333703, 0.3170188387650512141, 0.3333333333333333703, 0.3170188387650512141, 0.3333333333333333703, 0.3170188387650512141, 0.3333333333333333703, 0.3170188387650512141, 0.3333333333333333703, 0.3170188387650512141, 0.3333333333333333703, 0.3170188387650512141, 0.3333333333333333703),
 ( 1.000000000000000000, 0.9510565162951535312, 1.000000000000000000, 0.9510565162951535312, 1.000000000000000000, 0.9510565162951535312, 1.000000000000000000, 0.9510565162951535312, 1.000000000000000000, 0.9510565162951535312, 1.000000000000000000, 0.9510565162951535312, 1.000000000000000000, 0.9510565162951535312, 1.000000000000000000, 0.9510565162951535312, 1.000000000000000000, 0.9510565162951535312, 1.000000000000000000, 0.9510565162951535312, 1.000000000000000000, 0.9510565162951535312, 1.000000000000000000, 0.9510565162951535312, 1.000000000000000000, 0.9510565162951535312, 1.000000000000000000, 0.9510565162951535312, 1.000000000000000000, 0.9510565162951535312, 1.000000000000000000, 0.9510565162951535312, 1.000000000000000000, 0.9510565162951535312, 1.000000000000000000, 0.9510565162951535312, 1.000000000000000000, 0.9510565162951535312, 1.000000000000000000, 0.9510565162951535312, 1.000000000000000000, 0.9510565162951535312, 1.000000000000000000, 0.9510565162951535312, 1.000000000000000000, 0.9510565162951535312, 1.000000000000000000, 0.9510565162951535312, 1.000000000000000000, 0.9510565162951535312, 1.000000000000000000, 0.9510565162951535312, 1.000000000000000000, 0.9510565162951535312, 1.000000000000000000, 0.9510565162951535312, 1.000000000000000000, 0.9510565162951535312, 1.000000000000000000, 0.9510565162951535312, 1.000000000000000000, 0.9510565162951535312, 1.000000000000000000, 0.9510565162951535312, 1.000000000000000000, 0.9510565162951535312, 1.000000000000000000, 0.9510565162951535312, 1.000000000000000000, 0.9510565162951535312, 1.000000000000000000, 0.9510565162951535312, 1.000000000000000000, 0.9510565162951535312, 1.000000000000000000, 0.9510565162951535312, 1.000000000000000000, 0.9510565162951535312, 1.000000000000000000, 0.9510565162951535312, 1.000000000000000000, 0.9510565162951535312, 1.000000000000000000, 0.9510565162951535312, 1.000000000000000000, 0.9510565162951535312, 1.000000000000000000, 0.9510565162951535312, 1.000000000000000000, 0.9510565162951535312, 1.000000000000000000, 0.9510565162951535312, 1.000000000000000000, 0.9510565162951535312, 1.000000000000000000, 0.9510565162951535312, 1.000000000000000000, 0.9510565162951535312, 1.000000000000000000, 0.9510565162951535312, 1.000000000000000000, 0.9510565162951535312, 1.000000000000000000, 0.9510565162951535312, 1.000000000000000000, 0.9510565162951535312, 1.000000000000000000, 0.9510565162951535312, 1.000000000000000000, 0.9510565162951535312, 1.000000000000000000, 0.9510565162951535312, 1.000000000000000000, 0.9510565162951535312, 1.000000000000000000, 0.9510565162951535312, 1.000000000000000000, 0.9510565162951535312, 1.000000000000000000, 0.9510565162951535312, 1.000000000000000000, 0.9510565162951535312, 1.000000000000000000, 0.9510565162951535312, 1.000000000000000000, 0.9510565162951535312, 1.000000000000000000, 0.9510565162951535312, 1.000000000000000000, 0.9510565162951535312, 1.000000000000000000, 0.9510565162951535312, 1.000000000000000000, 0.9510565162951535312, 1.000000000000000000, 0.9510565162951535312, 1.000000000000000000, 0.9510565162951535312, 1.000000000000000000, 0.9510565162951535312, 1.000000000000000000, 0.9510565162951535312, 1.000000000000000000, 0.9510565162951535312, 1.000000000000000000, 0.9510565162951535312, 1.000000000000000000, 0.9510565162951535312, 1.000000000000000000, 0.9510565162951535312, 1.000000000000000000, 0.9510565162951535312, 1.000000000000000000, 0.9510565162951535312, 1.000000000000000000, 0.9510565162951535312, 1.000000000000000000, 0.9510565162951535312, 1.000000000000000000, 0.9510565162951535312, 1.000000000000000000, 0.9510565162951535312, 1.000000000000000000, 0.9510565162951535312, 1.000000000000000000, 0.9510565162951535312, 1.000000000000000000, 0.9510565162951535312, 1.000000000000000000, 0.9510565162951535312, 1.000000000000000000, 0.9510565162951535312, 1.000000000000000000, 0.9510565162951535312, 1.000000000000000000, 0.9510565162951535312, 1.000000000000000000, 0.9510565162951535312, 1.000000000000000000, 0.9510565162951535312, 1.000000000000000000, 0.9510565162951535312, 1.000000000000000000, 0.9510565162951535312, 1.000000000000000000, 0.9510565162951535312, 1.000000000000000000, 0.9510565162951535312, 1.000000000000000000, 0.9510565162951535312, 1.000000000000000000, 0.9510565162951535312, 1.000000000000000000, 0.9510565162951535312, 1.000000000000000000, 0.9510565162951535312, 1.000000000000000000, 0.9510565162951535312, 1.000000000000000000, 0.9510565162951535312, 1.000000000000000000, 0.9510565162951535312, 1.000000000000000000, 0.9510565162951535312, 1.000000000000000000, 0.9510565162951535312, 1.000000000000000000, 0.9510565162951535312, 1.000000000000000000, 0.9510565162951535312, 1.000000000000000000, 0.9510565162951535312, 1.000000000000000000, 0.9510565162951535312, 1.000000000000000000, 0.9510565162951535312, 1.000000000000000000, 0.9510565162951535312, 1.000000000000000000, 0.9510565162951535312, 1.000000000000000000, 0.9510565162951535312, 1.000000000000000000, 0.9510565162951535312, 1.000000000000000000, 0.9510565162951535312, 1.000000000000000000, 0.9510565162951535312, 1.000000000000000000, 0.9510565162951535312, 1.000000000000000000, 0.9510565162951535312, 1.000000000000000000, 0.9510565162951535312, 1.000000000000000000, 0.9510565162951535312, 1.000000000000000000, 0.9510565162951535312, 1.000000000000000000, 0.9510565162951535312, 1.000000000000000000, 0.9510565162951535312, 1.000000000000000000, 0.9510565162951535312, 1.000000000000000000, 0.9510565162951535312, 1.000000000000000000, 0.9510565162951535312, 1.000000000000000000, 0.9510565162951535312, 1.000000000000000000, 0.9510565162951535312, 1.000000000000000000, 0.9510565162951535312, 1.000000000000000000, 0.9510565162951535312, 1.000000000000000000, 0.9510565162951535312, 1.000000000000000000, 0.9510565162951535312, 1.000000000000000000, 0.9510565162951535312, 1.000000000000000000, 0.9510565162951535312, 1.000000000000000000, 0.9510565162951535312, 1.000000000000000000, 0.9510565162951535312, 1.000000000000000000, 0.9510565162951535312, 1.000000000000000000, 0.9510565162951535312, 1.000000000000000000, 0.9510565162951535312, 1.000000000000000000, 0.9510565162951535312, 1.000000000000000000, 0.9510565162951535312, 1.000000000000000000, 0.9510565162951535312, 1.000000000000000000, 0.9510565162951535312, 1.000000000000000000, 0.9510565162951535312, 1.000000000000000000, 0.9510565162951535312, 1.000000000000000000, 0.9510565162951535312, 1.000000000000000000, 0.9510565162951535312, 1.000000000000000000, 0.9510565162951535312, 1.000000000000000000, 0.9510565162951535312, 1.000000000000000000, 0.9510565162951535312, 1.000000000000000000, 0.9510565162951535312, 1.000000000000000000, 0.9510565162951535312, 1.000000000000000000, 0.9510565162951535312, 1.000000000000000000, 0.9510565162951535312, 1.000000000000000000, 0.9510565162951535312, 1.000000000000000000, 0.9510565162951535312, 1.000000000000000000, 0.9510565162951535312, 1.000000000000000000) ) ) 
 REPRESENTATION_ITEM ( '' )  SURFACE ( )  );
#19152=CARTESIAN_POINT ( 'NONE',  ( 37.12184278917507640, -13.51368208888610312, 71.43714994484034264 ) ) ;
#19157=CARTESIAN_POINT ( 'NONE',  ( 39.29254315202757653, -24.80384086642191477, 72.81632618279320468 ) ) ;
#19177=CARTESIAN_POINT ( 'NONE',  ( 40.33642880535521869, -9.303840866421909439, 69.98269868914867686 ) ) ;
#19181=CARTESIAN_POINT ( 'NONE',  ( 39.75915168707250302, -12.71368208888610063, 70.26145752964251301 ) ) ;
#19187=CARTESIAN_POINT ( 'NONE',  ( 36.89935272106204422, -21.21368208888610241, 69.52238214136768590 ) ) ;
#19195=CARTESIAN_POINT ( 'NONE',  ( 39.02742774030101458, -11.40384086642191086, 70.49320253461759478 ) ) ;
#19196=CARTESIAN_POINT ( 'NONE',  ( 36.49096545463212493, -1.513682088886105559, 71.43714994484035685 ) ) ;
#19202=CARTESIAN_POINT ( 'NONE',  ( 38.82593461698265003, -0.7038408664219141242, 73.13360434286904876 ) ) ;
#19203=CARTESIAN_POINT ( 'NONE',  ( 39.38009889167650357, -2.213682088886108179, 72.75271321436733274 ) ) ;
#19204=CARTESIAN_POINT ( 'NONE',  ( 40.52078840805428683, -2.613682088886105870, 70.60699637195608602 ) ) ;
#19208=CARTESIAN_POINT ( 'NONE',  ( 39.24876120206129571, -4.903840866421912636, 72.12822762946750288 ) ) ;
#19214=CARTESIAN_POINT ( 'NONE',  ( 36.29569395875881099, -12.30384086642192010, 72.77780686321128201 ) ) ;
#19216=CARTESIAN_POINT ( 'NONE',  ( 38.26194895904383486, -17.01368208888610312, 69.64448340153877837 ) ) ;
#19221=CARTESIAN_POINT ( 'NONE',  ( 36.87297107704151244, -5.903840866421907307, 70.26145752964255564 ) ) ;
#19225=CARTESIAN_POINT ( 'NONE',  ( 37.33957961208646736, -15.81368208888610916, 72.81632618279321889 ) ) ;
#19228=CARTESIAN_POINT ( 'NONE',  ( 38.26194895904384907, -20.60384086642191548, 73.11602215082116629 ) ) ;
#19230=CARTESIAN_POINT ( 'NONE',  ( 36.64852494920107517, -21.41368208888610525, 70.89533451361947414 ) ) ;
#19232=CARTESIAN_POINT ( 'NONE',  ( 40.55423172469004101, -1.203840866421914457, 70.70992431699450265 ) ) ;
#19236=CARTESIAN_POINT ( 'NONE',  ( 39.24876120206129571, -26.90384086642191264, 72.12822762946746025 ) ) ;
#19243=CARTESIAN_POINT ( 'NONE',  ( 37.69796330110505522, -0.5038408664219152788, 73.09843995877331224 ) ) ;
#19255=CARTESIAN_POINT ( 'NONE',  ( 39.75915168707251723, -26.90384086642191619, 72.49904802271737481 ) ) ;
#19263=CARTESIAN_POINT ( 'NONE',  ( 37.31647492878124694, -4.303840866421912992, 72.03616607671141026 ) ) ;
#19271=CARTESIAN_POINT ( 'NONE',  ( 37.60469502381300089, -9.213682088886100630, 70.49320253461759478 ) ) ;
#19272=CARTESIAN_POINT ( 'NONE',  ( 38.37017380507020192, -12.01368208888610134, 72.51602215082118619 ) ) ;
#19278=CARTESIAN_POINT ( 'NONE',  ( 36.64852494920107517, -18.20384086642191335, 71.86517103874048473 ) ) ;
#19281=CARTESIAN_POINT ( 'NONE',  ( 37.12184278917507640, -19.51368208888610312, 71.43714994484034264 ) ) ;
#19297=CARTESIAN_POINT ( 'NONE',  ( 38.26194895904384197, -8.603840866421919031, 73.71602215082116061 ) ) ;
#19300=CARTESIAN_POINT ( 'NONE',  ( 38.93415946300897446, -12.11368208888610276, 73.09843995877329803 ) ) ;
#19305=CARTESIAN_POINT ( 'NONE',  ( 39.73277004305198545, -22.21368208888610951, 73.23812341099225875 ) ) ;
#19319=CARTESIAN_POINT ( 'NONE',  ( 37.21915885897815457, -10.20384086642191335, 71.67976084211552745 ) ) ;
#19320=CARTESIAN_POINT ( 'NONE',  ( 36.87297107704152666, -1.713682088886108179, 72.49904802271743165 ) ) ;
#19329=CARTESIAN_POINT ( 'NONE',  ( 38.93415946300896024, -1.503840866421908729, 69.66206559358663242 ) ) ;
#19330=CARTESIAN_POINT ( 'NONE',  ( 38.73920764526925353, -28.11368208888610454, 72.49843995877328950 ) ) ;
#19331=CARTESIAN_POINT ( 'NONE',  ( 36.29569395875879678, -1.313682088886099830, 69.98269868914869107 ) ) ;
#19334=CARTESIAN_POINT ( 'NONE',  ( 37.60469502381300799, -2.403840866421910416, 72.26730301774236409 ) ) ;
#19340=CARTESIAN_POINT ( 'NONE',  ( 38.26194895904384197, -8.603840866421919031, 73.71602215082116061 ) ) ;
#19342=CARTESIAN_POINT ( 'NONE',  ( 39.38009889167650357, -12.21368208888610596, 72.75271321436731853 ) ) ;
#19351=CARTESIAN_POINT ( 'NONE',  ( 38.26194895904384907, -10.60384086642191726, 73.11602215082118050 ) ) ;
#19354=CARTESIAN_POINT ( 'NONE',  ( 36.87297107704152666, -17.71368208888610951, 72.49904802271740323 ) ) ;
#19356=EDGE_CURVE ( 'NONE', #3300, #21877, #14001, .T. ) ;
#19357=CARTESIAN_POINT ( 'NONE',  ( 38.26194895904384907, -18.60384086642191548, 73.11602215082116629 ) ) ;
#19359=CARTESIAN_POINT ( 'NONE',  ( 39.29254315202756231, -20.81368208888610027, 69.94417936956672577 ) ) ;
#19361=CARTESIAN_POINT ( 'NONE',  ( 37.61123632939165873, -21.91368208888611235, 73.73360434286898624 ) ) ;
#19366=CARTESIAN_POINT ( 'NONE',  ( 39.41296390513587511, -25.20384086642191335, 71.08074471024438878 ) ) ;
#19370=CARTESIAN_POINT ( 'NONE',  ( 39.66066260159757917, -29.10876147765399580, 70.75778293607493197 ) ) ;
#19374=CARTESIAN_POINT ( 'NONE',  ( 38.26194895904384197, -28.60384086642191548, 73.71602215082113219 ) ) ;
#19388=CARTESIAN_POINT ( 'NONE',  ( 39.37952058850012804, -9.003840866421910505, 71.78268878715392987 ) ) ;
#19395=CARTESIAN_POINT ( 'NONE',  ( 37.12184278917507640, -11.51368208888610134, 71.43714994484034264 ) ) ;
#19397=CARTESIAN_POINT ( 'NONE',  ( 39.31564783533280405, -8.313682088886102051, 72.03616607671141026 ) ) ;
#19405=CARTESIAN_POINT ( 'NONE',  ( 36.49096545463212493, -20.10384086642191193, 71.32335560751961623 ) ) ;
#19407=CARTESIAN_POINT ( 'NONE',  ( 37.60469502381300089, -17.21368208888610241, 70.49320253461759478 ) ) ;
#19420=CARTESIAN_POINT ( 'NONE',  ( 36.36258059203030513, -7.903840866421910860, 69.89063713639259845 ) ) ;
#19423=CARTESIAN_POINT ( 'NONE',  ( 36.68196826583682935, -13.61368208888610454, 71.96809898377888715 ) ) ;
#19428=CARTESIAN_POINT ( 'NONE',  ( 40.55423172469004811, -22.41368208888610525, 72.05058123536544201 ) ) ;
#19441=CARTESIAN_POINT ( 'NONE',  ( 38.26194895904384197, -14.60384086642191193, 72.51602215082118619 ) ) ;
#19442=CARTESIAN_POINT ( 'NONE',  ( 38.37017380507020192, 1.986317911113890444, 73.11602215082119471 ) ) ;
#19450=CARTESIAN_POINT ( 'NONE',  ( 36.49096545463212493, -0.1038408664219107880, 71.32335560751963044 ) ) ;
#19454=CARTESIAN_POINT ( 'NONE',  ( 39.98359781491296161, 1.586317911113896528, 71.86517103874049894 ) ) ;
#19455=CARTESIAN_POINT ( 'NONE',  ( 37.61123632939165873, 0.08631791111389161553, 73.73360434286902887 ) ) ;
#19458=CARTESIAN_POINT ( 'NONE',  ( 37.25260217561390874, -4.003840866421911393, 70.97781676520604321 ) ) ;
#19465=CARTESIAN_POINT ( 'NONE',  ( 39.12911128074872380, -11.50384086642191050, 69.06206559358666652 ) ) ;
#19467=CARTESIAN_POINT ( 'NONE',  ( 38.26194895904383486, -13.01368208888610134, 69.64448340153877837 ) ) ;
#19474=CARTESIAN_POINT ( 'NONE',  ( 40.14115730948191185, 0.8961591335780899614, 71.43714994484035685 ) ) ;
#19477=CARTESIAN_POINT ( 'NONE',  ( 36.80608444377001121, -21.31368208888610027, 70.35351908239857721 ) ) ;
#19480=CARTESIAN_POINT ( 'NONE',  ( 40.14115730948191185, -17.10384086642191193, 71.43714994484030001 ) ) ;
#19485=CARTESIAN_POINT ( 'NONE',  ( 36.87297107704152666, -19.71368208888610951, 72.49904802271740323 ) ) ;
#19487=CARTESIAN_POINT ( 'NONE',  ( 40.52078840805428683, -20.61368208888610454, 70.60699637195608602 ) ) ;
#19493=CARTESIAN_POINT ( 'NONE',  ( 37.38336156205273397, -23.90384086642191619, 70.63227792289245599 ) ) ;
#19499=CARTESIAN_POINT ( 'NONE',  ( 39.65020039316494405, -29.05171021479125315, 70.79984939021886703 ) ) ;
#19503=CARTESIAN_POINT ( 'NONE',  ( 36.68196826583682935, -0.003840866421911393047, 70.79240656858108593 ) ) ;
#19505=CARTESIAN_POINT ( 'NONE',  ( 36.36258059203031934, -3.713682088886109955, 72.86986841596736042 ) ) ;
#19513=CARTESIAN_POINT ( 'NONE',  ( 38.26194895904384907, -20.60384086642191548, 73.11602215082116629 ) ) ;
#19522=CARTESIAN_POINT ( 'NONE',  ( 39.41296390513587511, -5.203840866421910683, 71.08074471024443142 ) ) ;
#19528=CARTESIAN_POINT ( 'NONE',  ( 38.93987200065208754, -14.81368208888610205, 70.42958956619168021 ) ) ;
#19530=CARTESIAN_POINT ( 'NONE',  ( 39.37952058850012804, -8.613682088886100985, 70.97781676520601479 ) ) ;
#19537=CARTESIAN_POINT ( 'NONE',  ( 36.64852494920107517, -20.20384086642191335, 71.86517103874048473 ) ) ;
#19540=CARTESIAN_POINT ( 'NONE',  ( 38.93987200065208754, -16.81368208888610383, 70.42958956619168021 ) ) ;
#19544=CARTESIAN_POINT ( 'NONE',  ( 39.95015449827720744, -16.61368208888610454, 70.79240656858105751 ) ) ;
#19557=CARTESIAN_POINT ( 'NONE',  ( 36.07789103942399578, -10.20384086642191690, 72.05058123536544201 ) ) ;
#19560=CARTESIAN_POINT ( 'NONE',  ( 37.69796330110504101, -17.11368208888610098, 69.66206559358661821 ) ) ;
#19564=CARTESIAN_POINT ( 'NONE',  ( 40.77203464402485622, -18.51368208888610312, 71.32335560751960202 ) ) ;
#19574=CARTESIAN_POINT ( 'NONE',  ( 37.31647492878124694, -14.30384086642191122, 72.03616607671141026 ) ) ;
#19575=CARTESIAN_POINT ( 'NONE',  ( 37.25260217561390874, -27.61368208888610454, 71.78268878715390144 ) ) ;
#19576=ORIENTED_EDGE ( 'NONE', *, *, #18801, .F. ) ;
#19581=CARTESIAN_POINT ( 'NONE',  ( 36.98690846071097127, -27.80384086642191477, 69.45876917294174291 ) ) ;
#19583=CARTESIAN_POINT ( 'NONE',  ( 37.89291511884476904, -25.11368208888610454, 70.26206559358661252 ) ) ;
#19585=CARTESIAN_POINT ( 'NONE',  ( 40.52078840805428683, -4.613682088886104538, 70.60699637195608602 ) ) ;
#19588=CARTESIAN_POINT ( 'NONE',  ( 39.37952058850012804, -7.003840866421911393, 71.78268878715392987 ) ) ;
#19593=CARTESIAN_POINT ( 'NONE',  ( 40.55423172469004101, -13.20384086642191690, 70.70992431699450265 ) ) ;
#19596=CARTESIAN_POINT ( 'NONE',  ( 39.29254315202756231, -12.81368208888610383, 69.94417936956672577 ) ) ;
#19600=CARTESIAN_POINT ( 'NONE',  ( 40.14115730948191185, -1.103840866421911482, 71.43714994484034264 ) ) ;
#19603=CARTESIAN_POINT ( 'NONE',  ( 36.87297107704152666, -19.71368208888610951, 72.49904802271740323 ) ) ;
#19605=CARTESIAN_POINT ( 'NONE',  ( 38.82593461698265003, -18.70384086642191690, 73.13360434286903455 ) ) ;
#19608=CARTESIAN_POINT ( 'NONE',  ( 36.80608444377001121, -13.31368208888609672, 70.35351908239857721 ) ) ;
#19610=CARTESIAN_POINT ( 'NONE',  ( 40.26954217208371034, -24.71368208888610241, 69.89063713639254161 ) ) ;
#19614=CARTESIAN_POINT ( 'NONE',  ( 38.00113996487112189, -25.70384086642191690, 70.22690120949089021 ) ) ;
#19620=CARTESIAN_POINT ( 'NONE',  ( 40.26954217208372455, -26.90384086642191619, 72.86986841596730358 ) ) ;
#19622=CARTESIAN_POINT ( 'NONE',  ( 37.61123632939165873, -1.913682088886106580, 73.73360434286902887 ) ) ;
#19633=CARTESIAN_POINT ( 'NONE',  ( 39.38009889167648936, -21.40384086642190553, 70.00779233799262613 ) ) ;
#19642=CARTESIAN_POINT ( 'NONE',  ( 38.63098279924290068, -4.703840866421909794, 72.53360434286905445 ) ) ;
#19651=CARTESIAN_POINT ( 'NONE',  ( 37.31647492878122563, -11.31368208888609850, 70.72433947564853440 ) ) ;
#19654=CARTESIAN_POINT ( 'NONE',  ( 37.69225076346193504, -13.81368208888610383, 72.33091598616826445 ) ) ;
#19661=CARTESIAN_POINT ( 'NONE',  ( 39.82603832034400426, -15.30384086642190589, 70.35351908239857721 ) ) ;
#19665=CARTESIAN_POINT ( 'NONE',  ( 39.51027997493896748, -16.51368208888610312, 71.32335560751960202 ) ) ;
#19669=CARTESIAN_POINT ( 'NONE',  ( 36.87297107704153376, -13.71368208888610773, 72.49904802271740323 ) ) ;
#19682=CARTESIAN_POINT ( 'NONE',  ( 39.64521430340305841, -4.803840866421917433, 73.30173637941818754 ) ) ;
#19685=CARTESIAN_POINT ( 'NONE',  ( 40.14115730948191185, -16.51368208888610667, 71.32335560751960202 ) ) ;
#19691=CARTESIAN_POINT ( 'NONE',  ( 37.61123632939165873, -15.91368208888610880, 73.73360434286898624 ) ) ;
#19699=CARTESIAN_POINT ( 'NONE',  ( 37.89291511884479036, -12.50384086642191228, 72.49843995877330372 ) ) ;
#19700=CARTESIAN_POINT ( 'NONE',  ( 38.63098279924288647, -28.91368208888610170, 70.22690120949089021 ) ) ;
#19707=CARTESIAN_POINT ( 'NONE',  ( 40.55423172469004101, -23.20384086642191690, 70.70992431699450265 ) ) ;
#19709=CARTESIAN_POINT ( 'NONE',  ( 37.31647492878122563, -25.31368208888610027, 70.72433947564853440 ) ) ;
#19710=CARTESIAN_POINT ( 'NONE',  ( 38.26194895904383486, -1.013682088886101784, 69.04448340153881247 ) ) ;
#19714=CARTESIAN_POINT ( 'NONE',  ( 38.63098279924290068, -0.7038408664219106825, 72.53360434286905445 ) ) ;
#19721=CARTESIAN_POINT ( 'NONE',  ( 40.55423172469004101, -1.203840866421914457, 70.70992431699450265 ) ) ;
#19725=CARTESIAN_POINT ( 'NONE',  ( 36.68196826583682935, -11.61368208888610276, 71.96809898377888715 ) ) ;
#19732=CARTESIAN_POINT ( 'NONE',  ( 37.25202387243754032, -2.403840866421914413, 72.75271321436733274 ) ) ;
#19735=CARTESIAN_POINT ( 'NONE',  ( 36.49096545463212493, -17.51368208888610667, 71.43714994484034264 ) ) ;
#19737=CARTESIAN_POINT ( 'NONE',  ( 36.64852494920107517, -16.20384086642190979, 71.86517103874048473 ) ) ;
#19740=CARTESIAN_POINT ( 'NONE',  ( 40.14115730948191185, -14.51368208888610667, 71.32335560751960202 ) ) ;
#19742=CARTESIAN_POINT ( 'NONE',  ( 35.86008812008917346, -19.51368208888610312, 71.43714994484034264 ) ) ;
#19746=CARTESIAN_POINT ( 'NONE',  ( 39.31564783533279694, -19.30384086642191477, 70.72433947564853440 ) ) ;
#19753=CARTESIAN_POINT ( 'NONE',  ( 39.95015449827720744, 0.9961591335780894951, 71.96809898377890136 ) ) ;
#19756=CARTESIAN_POINT ( 'NONE',  ( 37.50301148336529167, -5.113682088886100985, 69.06206559358666652 ) ) ;
#19764=CARTESIAN_POINT ( 'NONE',  ( 36.49096545463212493, -24.10384086642190482, 71.32335560751960202 ) ) ;
#19773=CARTESIAN_POINT ( 'NONE',  ( 39.02742774030101458, -9.403840866421907307, 70.49320253461759478 ) ) ;
#19781=CARTESIAN_POINT ( 'NONE',  ( 37.31647492878122563, -13.31368208888610205, 70.72433947564853440 ) ) ;
#19783=CARTESIAN_POINT ( 'NONE',  ( 37.31647492878122563, -3.313682088886101607, 70.72433947564853440 ) ) ;
#19790=CARTESIAN_POINT ( 'NONE',  ( 38.37017380507018771, -15.60384086642190837, 69.64448340153877837 ) ) ;
#19795=CARTESIAN_POINT ( 'NONE',  ( 39.24876120206128860, -18.71368208888610241, 70.63227792289245599 ) ) ;
#19800=CARTESIAN_POINT ( 'NONE',  ( 37.80618814713140097, -11.91368208888611058, 73.13360434286903455 ) ) ;
#19805=CARTESIAN_POINT ( 'NONE',  ( 40.16586900051838427, -29.10876147765365829, 71.27221389253728034 ) ) ;
#19806=PRODUCT ( 'Pusher Pull Spring', 'Pusher Pull Spring', '', ( #5695 ) ) ;
#19814=CARTESIAN_POINT ( 'NONE',  ( 40.33642880535521869, -7.303840866421912104, 69.98269868914867686 ) ) ;
#19819=CARTESIAN_POINT ( 'NONE',  ( 38.93415946300897446, -8.113682088886108090, 73.09843995877331224 ) ) ;
#19824=CARTESIAN_POINT ( 'NONE',  ( 40.52078840805428683, -14.61368208888610276, 70.60699637195608602 ) ) ;
#19834=CARTESIAN_POINT ( 'NONE',  ( 39.51027997493896748, -26.51368208888610667, 71.32335560751960202 ) ) ;
#19841=CARTESIAN_POINT ( 'NONE',  ( 39.12911128074872380, -25.50384086642191406, 69.06206559358663810 ) ) ;
#19842=CARTESIAN_POINT ( 'NONE',  ( 37.21915885897815457, -21.41368208888610525, 71.08074471024443142 ) ) ;
#19843=CARTESIAN_POINT ( 'NONE',  ( 38.93415946300897446, -28.11368208888610098, 73.09843995877328382 ) ) ;
#19846=CARTESIAN_POINT ( 'NONE',  ( 39.24876120206129571, -0.9038408664219128585, 72.12822762946750288 ) ) ;
#19852=CARTESIAN_POINT ( 'NONE',  ( 37.50301148336529877, -4.503840866421918498, 73.69843995877330656 ) ) ;
#19855=CARTESIAN_POINT ( 'NONE',  ( 36.68196826583682935, -9.613682088886104538, 71.96809898377890136 ) ) ;
#19857=AXIS2_PLACEMENT_3D ( 'NONE', #10043, #8366, #6304 ) ;
#19859=CARTESIAN_POINT ( 'NONE',  ( 36.49096545463212493, -25.51368208888610312, 71.43714994484031422 ) ) ;
#19861=CARTESIAN_POINT ( 'NONE',  ( 38.37017380507018771, 0.3961591335780931256, 69.64448340153880679 ) ) ;
#19865=CARTESIAN_POINT ( 'NONE',  ( 37.89291511884479036, -24.50384086642190695, 72.49843995877328950 ) ) ;
#19866=CARTESIAN_POINT ( 'NONE',  ( 36.87297107704152666, -9.713682088886107735, 72.49904802271743165 ) ) ;
#19871=CARTESIAN_POINT ( 'NONE',  ( 39.75915168707251723, -14.90384086642191086, 72.49904802271738902 ) ) ;
#19874=CARTESIAN_POINT ( 'NONE',  ( 37.69796330110504101, -15.11368208888609743, 69.66206559358661821 ) ) ;
#19876=CARTESIAN_POINT ( 'NONE',  ( 36.89935272106204422, -17.21368208888610241, 69.52238214136768590 ) ) ;
#19880=CARTESIAN_POINT ( 'NONE',  ( 38.00113996487112189, -19.70384086642190979, 70.22690120949090442 ) ) ;
#19887=CARTESIAN_POINT ( 'NONE',  ( 35.86008812008917346, -20.10384086642191548, 71.32335560751961623 ) ) ;
#19890=CARTESIAN_POINT ( 'NONE',  ( 37.69796330110504101, -27.11368208888609388, 69.66206559358660400 ) ) ;
#19898=CARTESIAN_POINT ( 'NONE',  ( 36.49096545463212493, -22.10384086642191193, 71.32335560751961623 ) ) ;
#19905=CARTESIAN_POINT ( 'NONE',  ( 39.24876120206129571, -2.903840866421911304, 72.12822762946750288 ) ) ;
#19914=CARTESIAN_POINT ( 'NONE',  ( 37.12184278917507640, -7.513682088886100452, 71.43714994484035685 ) ) ;
#19915=CARTESIAN_POINT ( 'NONE',  ( 38.93987200065208754, -2.813682088886101162, 70.42958956619168021 ) ) ;
#19922=CARTESIAN_POINT ( 'NONE',  ( 37.33957961208645315, -7.803840866421909439, 69.94417936956673998 ) ) ;
#19931=CARTESIAN_POINT ( 'NONE',  ( 39.75915168707250302, -8.713682088886098853, 70.26145752964255564 ) ) ;
#19935=CARTESIAN_POINT ( 'NONE',  ( 40.20245935045282692, -29.10876147765143429, 71.09018146340289945 ) ) ;
#19944=CARTESIAN_POINT ( 'NONE',  ( 36.29569395875881099, -2.303840866421917877, 72.77780686321129622 ) ) ;
#19948=CARTESIAN_POINT ( 'NONE',  ( 36.64852494920107517, -9.413682088886107024, 70.89533451361948835 ) ) ;
#19952=CARTESIAN_POINT ( 'NONE',  ( 36.07789103942398867, -15.41368208888610347, 70.70992431699450265 ) ) ;
#19965=CARTESIAN_POINT ( 'NONE',  ( 37.38336156205274818, -25.71368208888610241, 72.12822762946747446 ) ) ;
#19972=CARTESIAN_POINT ( 'NONE',  ( 37.61123632939164452, -23.70384086642191335, 69.02690120949091579 ) ) ;
#19974=CARTESIAN_POINT ( 'NONE',  ( 38.26194895904383486, 0.9863179111139001032, 69.04448340153882668 ) ) ;
#19982=CARTESIAN_POINT ( 'NONE',  ( 38.26194895904384197, -4.603840866421918143, 73.71602215082116061 ) ) ;
#19985=CARTESIAN_POINT ( 'NONE',  ( 38.26194895904383486, -9.013682088886101340, 69.64448340153879258 ) ) ;
#19987=CARTESIAN_POINT ( 'NONE',  ( 39.38009889167650357, -24.21368208888610596, 72.75271321436730432 ) ) ;
#19989=CARTESIAN_POINT ( 'NONE',  ( 39.95015449827720744, -1.003840866421912281, 71.96809898377888715 ) ) ;
#19991=CARTESIAN_POINT ( 'NONE',  ( 38.63098279924290068, -24.70384086642190979, 72.53360434286901182 ) ) ;
#19992=CARTESIAN_POINT ( 'NONE',  ( 36.68196826583682935, -11.61368208888610276, 71.96809898377888715 ) ) ;
#19994=CARTESIAN_POINT ( 'NONE',  ( 39.82603832034400426, -11.30384086642190944, 70.35351908239857721 ) ) ;
#19996=CARTESIAN_POINT ( 'NONE',  ( 37.80618814713140097, -9.913682088886107024, 73.13360434286904876 ) ) ;
#19998=CARTESIAN_POINT ( 'NONE',  ( 36.11133435605973574, -15.61368208888610454, 72.15350918040385864 ) ) ;
#20002=CARTESIAN_POINT ( 'NONE',  ( 38.93987200065210175, -16.80384086642191477, 72.33091598616826445 ) ) ;
#20007=CARTESIAN_POINT ( 'NONE',  ( 37.50301148336529877, -20.50384086642191761, 73.69843995877327814 ) ) ;
#20010=CARTESIAN_POINT ( 'NONE',  ( 38.82593461698262871, -26.91368208888610170, 69.62690120949091011 ) ) ;
#20019=CARTESIAN_POINT ( 'NONE',  ( 39.75915168707251723, -18.90384086642191264, 72.49904802271738902 ) ) ;
#20025=CARTESIAN_POINT ( 'NONE',  ( 37.69225076346193504, 0.1961591335780874246, 70.42958956619168021 ) ) ;
#20033=CARTESIAN_POINT ( 'NONE',  ( 37.69225076346193504, -7.813682088886102939, 72.33091598616827866 ) ) ;
#20034=CARTESIAN_POINT ( 'NONE',  ( 38.00113996487114321, -1.913682088886099475, 72.53360434286905445 ) ) ;
#20041=CARTESIAN_POINT ( 'NONE',  ( 36.64852494920107517, -12.20384086642190979, 71.86517103874048473 ) ) ;
#20053=CARTESIAN_POINT ( 'NONE',  ( 36.80608444377001121, -7.313682088886101162, 70.35351908239861984 ) ) ;
#20068=CARTESIAN_POINT ( 'NONE',  ( 39.02088643472237806, -4.703840866421917788, 73.73360434286902887 ) ) ;
#20071=CARTESIAN_POINT ( 'NONE',  ( 39.98359781491296161, -10.41368208888610347, 71.86517103874048473 ) ) ;
#20073=CARTESIAN_POINT ( 'NONE',  ( 37.50301148336529167, -17.11368208888609743, 69.06206559358665231 ) ) ;
#20084=CARTESIAN_POINT ( 'NONE',  ( 37.60469502381300089, -25.21368208888610241, 70.49320253461758057 ) ) ;
#20091=CARTESIAN_POINT ( 'NONE',  ( 40.77203464402485622, -23.10384086642191548, 71.43714994484032843 ) ) ;
#20093=CARTESIAN_POINT ( 'NONE',  ( 36.64852494920107517, -25.41368208888610525, 70.89533451361945993 ) ) ;
#20102=CARTESIAN_POINT ( 'NONE',  ( 39.02088643472237806, -6.703840866421919564, 73.73360434286902887 ) ) ;
#20109=CARTESIAN_POINT ( 'NONE',  ( 37.33957961208646736, -5.813682088886107380, 72.81632618279323310 ) ) ;
#20111=CARTESIAN_POINT ( 'NONE',  ( 39.95015449827720744, -28.61368208888610454, 70.79240656858104330 ) ) ;
#20117=CARTESIAN_POINT ( 'NONE',  ( 38.73920764526923932, -25.50384086642191406, 70.26206559358661252 ) ) ;
#20118=CARTESIAN_POINT ( 'NONE',  ( 38.93415946300897446, -12.11368208888610276, 73.09843995877329803 ) ) ;
#20121=CARTESIAN_POINT ( 'NONE',  ( 37.33957961208645315, -11.80384086642190944, 69.94417936956672577 ) ) ;
#20123=CARTESIAN_POINT ( 'NONE',  ( 39.29254315202756231, -10.81368208888610205, 69.94417936956673998 ) ) ;
#20125=CARTESIAN_POINT ( 'NONE',  ( 37.61123632939165873, -17.91368208888610525, 73.73360434286898624 ) ) ;
#20130=CARTESIAN_POINT ( 'NONE',  ( 38.00113996487112189, -17.70384086642190979, 70.22690120949090442 ) ) ;
#20136=CARTESIAN_POINT ( 'NONE',  ( 35.86008812008917346, -24.10384086642191193, 71.32335560751960202 ) ) ;
#20141=CARTESIAN_POINT ( 'NONE',  ( 39.95015449827720744, -28.61368208888610454, 70.79240656858104330 ) ) ;
#20149=CARTESIAN_POINT ( 'NONE',  ( 36.87297107704151244, -13.90384086642190731, 70.26145752964255564 ) ) ;
#20154=CARTESIAN_POINT ( 'NONE',  ( 39.31564783533279694, -1.303840866421910105, 70.72433947564853440 ) ) ;
#20159=CARTESIAN_POINT ( 'NONE',  ( 38.37017380507020192, -28.01368208888610667, 73.11602215082115208 ) ) ;
#20164=CARTESIAN_POINT ( 'NONE',  ( 39.41296390513587511, -6.413682088886100807, 71.67976084211552745 ) ) ;
#20165=CARTESIAN_POINT ( 'NONE',  ( 37.12184278917507640, -7.513682088886100452, 71.43714994484035685 ) ) ;
#20172=CARTESIAN_POINT ( 'NONE',  ( 37.69796330110505522, -12.50384086642191228, 73.09843995877329803 ) ) ;
#20180=CARTESIAN_POINT ( 'NONE',  ( 39.29254315202756231, -8.813682088886100274, 69.94417936956673998 ) ) ;
#20185=CARTESIAN_POINT ( 'NONE',  ( 38.93415946300897446, -26.11368208888610098, 73.09843995877328382 ) ) ;
#20196=CARTESIAN_POINT ( 'NONE',  ( 35.86008812008917346, -2.103840866421915923, 71.32335560751961623 ) ) ;
#20201=CARTESIAN_POINT ( 'NONE',  ( 36.80608444377001121, -11.31368208888609672, 70.35351908239857721 ) ) ;
#20205=CARTESIAN_POINT ( 'NONE',  ( 40.33642880535524000, -16.31368208888611093, 72.77780686321126780 ) ) ;
#20214=CARTESIAN_POINT ( 'NONE',  ( 38.26194895904383486, -25.01368208888610312, 70.24448340153875847 ) ) ;
#20220=CARTESIAN_POINT ( 'NONE',  ( 36.29569395875881099, -24.30384086642192187, 72.77780686321126780 ) ) ;
#20221=CARTESIAN_POINT ( 'NONE',  ( 38.37017380507020192, 1.986317911113890666, 73.71602215082117482 ) ) ;
#20229=CARTESIAN_POINT ( 'NONE',  ( 40.77203464402485622, -5.103840866421915479, 71.43714994484034264 ) ) ;
#20233=CARTESIAN_POINT ( 'NONE',  ( 36.49096545463212493, -9.513682088886101340, 71.43714994484035685 ) ) ;
#20235=MECHANICAL_DESIGN_GEOMETRIC_PRESENTATION_REPRESENTATION('',(#9146),#23518);
#20236=CARTESIAN_POINT ( 'NONE',  ( 37.80618814713140097, -25.91368208888610880, 73.13360434286902034 ) ) ;
#20239=CARTESIAN_POINT ( 'NONE',  ( 39.24876120206129571, -26.90384086642191264, 72.12822762946746025 ) ) ;
#20240=CARTESIAN_POINT ( 'NONE',  ( 38.37017380507020192, -14.01368208888610845, 73.11602215082116629 ) ) ;
#20246=CARTESIAN_POINT ( 'NONE',  ( 39.29254315202757653, -14.80384086642191477, 72.81632618279321889 ) ) ;
#20249=CARTESIAN_POINT ( 'NONE',  ( 39.38009889167650357, -4.213682088886106847, 72.75271321436733274 ) ) ;
#20251=CARTESIAN_POINT ( 'NONE',  ( 40.55423172469004811, -18.41368208888610525, 72.05058123536544201 ) ) ;
#20255=CARTESIAN_POINT ( 'NONE',  ( 38.37017380507018771, -15.60384086642191370, 70.24448340153875847 ) ) ;
#20262=CARTESIAN_POINT ( 'NONE',  ( 38.37017380507018771, -21.60384086642191548, 69.04448340153878405 ) ) ;
#20264=CARTESIAN_POINT ( 'NONE',  ( 39.98359781491296161, -26.41368208888610525, 71.86517103874045631 ) ) ;
#20273=CARTESIAN_POINT ( 'NONE',  ( 37.80618814713138676, -13.70384086642190802, 69.62690120949091011 ) ) ;
#20284=CARTESIAN_POINT ( 'NONE',  ( 38.37017380507018771, -1.603840866421912148, 70.24448340153877268 ) ) ;
#20295=CARTESIAN_POINT ( 'NONE',  ( 38.00113996487114321, -5.913682088886099919, 72.53360434286905445 ) ) ;
#20296=CARTESIAN_POINT ( 'NONE',  ( 37.21915885897815457, -3.413682088886101251, 71.08074471024443142 ) ) ;
#20304=CARTESIAN_POINT ( 'NONE',  ( 36.80608444377001831, -8.303840866421916544, 72.40698646996136745 ) ) ;
#20313=CARTESIAN_POINT ( 'NONE',  ( 39.38009889167650357, -6.213682088886108623, 72.75271321436733274 ) ) ;
#20315=CARTESIAN_POINT ( 'NONE',  ( 39.78769017101468108, -29.10876147765122823, 70.98199272578698071 ) ) ;
#20327=CARTESIAN_POINT ( 'NONE',  ( 40.77203464402485622, 0.8961591335780867418, 71.43714994484035685 ) ) ;
#20328=CARTESIAN_POINT ( 'NONE',  ( 37.25260217561390874, -23.61368208888610098, 71.78268878715390144 ) ) ;
#20332=CARTESIAN_POINT ( 'NONE',  ( 36.80608444377001121, -1.313682088886099386, 70.35351908239860563 ) ) ;
#20333=CARTESIAN_POINT ( 'NONE',  ( 39.98359781491296161, -29.20384086642191335, 70.89533451361944572 ) ) ;
#20337=CARTESIAN_POINT ( 'NONE',  ( 39.02088643472237095, -10.91368208888610170, 69.02690120949094421 ) ) ;
#20342=CARTESIAN_POINT ( 'NONE',  ( 39.66066260159681889, -29.10876147764981781, 69.85357445396793707 ) ) ;
#20343=CARTESIAN_POINT ( 'NONE',  ( 37.80618814713140097, -1.913682088886106136, 73.13360434286904876 ) ) ;
#20352=CARTESIAN_POINT ( 'NONE',  ( 38.37017380507018771, -17.60384086642191193, 69.04448340153878405 ) ) ;
#20353=CARTESIAN_POINT ( 'NONE',  ( 39.73277004305198545, 1.786317911113892043, 73.23812341099230139 ) ) ;
#20359=CARTESIAN_POINT ( 'NONE',  ( 40.52078840805428683, -24.61368208888610809, 70.60699637195608602 ) ) ;
#20365=CARTESIAN_POINT ( 'NONE',  ( 39.75915168707250302, -8.713682088886097077, 70.26145752964252722 ) ) ;
#20367=CARTESIAN_POINT ( 'NONE',  ( 36.68196826583682935, -23.61368208888610454, 71.96809898377887293 ) ) ;
#20370=CARTESIAN_POINT ( 'NONE',  ( 37.60469502381300799, -22.40384086642191264, 72.26730301774234988 ) ) ;
#20371=CARTESIAN_POINT ( 'NONE',  ( 39.98359781491296161, -10.41368208888610347, 71.86517103874048473 ) ) ;
#20376=CARTESIAN_POINT ( 'NONE',  ( 36.64852494920107517, -12.20384086642190979, 71.86517103874048473 ) ) ;
#20378=CARTESIAN_POINT ( 'NONE',  ( 39.75915168707250302, -8.713682088886097077, 70.26145752964252722 ) ) ;
#20380=CARTESIAN_POINT ( 'NONE',  ( 36.07789103942398867, -13.41368208888610525, 70.70992431699450265 ) ) ;
#20384=CARTESIAN_POINT ( 'NONE',  ( 39.41296390513587511, -9.203840866421909794, 71.08074471024443142 ) ) ;
#20389=CARTESIAN_POINT ( 'NONE',  ( 36.07789103942399578, -24.20384086642191690, 72.05058123536544201 ) ) ;
#20391=CARTESIAN_POINT ( 'NONE',  ( 38.26194895904383486, -25.01368208888610312, 69.64448340153876416 ) ) ;
#20397=CARTESIAN_POINT ( 'NONE',  ( 37.69796330110505522, -16.50384086642191406, 73.09843995877329803 ) ) ;
#20403=CARTESIAN_POINT ( 'NONE',  ( 36.87297107704149823, -27.90384086642190908, 70.26145752964251301 ) ) ;
#20404=DIRECTION ( 'NONE',  ( 0.1803747433772529551, -0.9835979625596985576, 0.000000000000000000 ) ) ;
#20406=CARTESIAN_POINT ( 'NONE',  ( 36.68196826583682935, -23.61368208888610454, 71.96809898377887293 ) ) ;
#20411=CARTESIAN_POINT ( 'NONE',  ( 39.02742774030101458, -29.40384086642191264, 70.49320253461758057 ) ) ;
#20412=CARTESIAN_POINT ( 'NONE',  ( 39.31564783533280405, -0.3136820888861025503, 72.03616607671141026 ) ) ;
#20419=CARTESIAN_POINT ( 'NONE',  ( 38.93415946300896024, -11.50384086642190340, 69.66206559358663242 ) ) ;
#20430=CARTESIAN_POINT ( 'NONE',  ( 39.98359781491296161, -8.413682088886105248, 71.86517103874048473 ) ) ;
#20444=CARTESIAN_POINT ( 'NONE',  ( 40.26954217208372455, -0.9038408664219198529, 72.86986841596736042 ) ) ;
#20447=CARTESIAN_POINT ( 'NONE',  ( 39.31564783533280405, -24.31368208888610383, 72.03616607671136762 ) ) ;
#20452=CARTESIAN_POINT ( 'NONE',  ( 37.69796330110504101, -3.113682088886098764, 69.66206559358663242 ) ) ;
#20453=CARTESIAN_POINT ( 'NONE',  ( 40.14115730948191185, -29.10384086642190482, 71.43714994484028580 ) ) ;
#20455=CARTESIAN_POINT ( 'NONE',  ( 39.02088643472237095, -6.913682088886101695, 69.02690120949094421 ) ) ;
#20461=CARTESIAN_POINT ( 'NONE',  ( 39.59324923284151510, -28.74115096347518161, 70.20355626897213597 ) ) ;
#20471=CARTESIAN_POINT ( 'NONE',  ( 40.33642880535521869, -15.30384086642191477, 69.98269868914866265 ) ) ;
#20473=CARTESIAN_POINT ( 'NONE',  ( 39.82603832034400426, -20.31368208888610738, 72.40698646996133903 ) ) ;
#20482=CARTESIAN_POINT ( 'NONE',  ( 36.11133435605973574, -0.003840866421914862494, 70.60699637195612866 ) ) ;
#20486=CARTESIAN_POINT ( 'NONE',  ( 36.80608444377001121, -3.313682088886100718, 70.35351908239860563 ) ) ;
#20488=CARTESIAN_POINT ( 'NONE',  ( 37.33957961208646736, -21.81368208888610738, 72.81632618279321889 ) ) ;
#20492=CARTESIAN_POINT ( 'NONE',  ( 39.41296390513587511, -21.20384086642190979, 71.08074471024441721 ) ) ;
#20493=CARTESIAN_POINT ( 'NONE',  ( 39.98359781491296161, -6.413682088886103472, 71.86517103874048473 ) ) ;
#20499=CARTESIAN_POINT ( 'NONE',  ( 39.38009889167648936, -3.403840866421908196, 70.00779233799264034 ) ) ;
#20503=CARTESIAN_POINT ( 'NONE',  ( 38.37017380507020192, -6.013682088886109334, 73.11602215082118050 ) ) ;
#20505=CARTESIAN_POINT ( 'NONE',  ( 40.52078840805428683, -10.61368208888610631, 70.60699637195608602 ) ) ;
#20509=CARTESIAN_POINT ( 'NONE',  ( 37.31647492878124694, -14.30384086642191122, 72.03616607671141026 ) ) ;
#20514=CARTESIAN_POINT ( 'NONE',  ( 36.29569395875881099, -14.30384086642192010, 72.77780686321128201 ) ) ;
#20517=CARTESIAN_POINT ( 'NONE',  ( 36.49096545463212493, -19.51368208888610312, 71.43714994484034264 ) ) ;
#20524=CARTESIAN_POINT ( 'NONE',  ( 36.49096545463212493, -16.10384086642191548, 71.32335560751961623 ) ) ;
#20530=CARTESIAN_POINT ( 'NONE',  ( 39.29254315202757653, -24.80384086642191477, 72.81632618279320468 ) ) ;
#20534=CARTESIAN_POINT ( 'NONE',  ( 38.82593461698262871, -24.91368208888610170, 69.62690120949091011 ) ) ;
#20539=CARTESIAN_POINT ( 'NONE',  ( 37.38336156205273397, -27.90384086642191264, 70.63227792289245599 ) ) ;
#20541=CARTESIAN_POINT ( 'NONE',  ( 39.02742774030102879, -0.2136820888860996304, 72.26730301774236409 ) ) ;
#20548=CARTESIAN_POINT ( 'NONE',  ( 37.33957961208645315, -1.803840866421907441, 69.94417936956673998 ) ) ;
#20557=CARTESIAN_POINT ( 'NONE',  ( 39.82603832034401847, 1.686317911113892176, 72.40698646996135324 ) ) ;
#20574=CARTESIAN_POINT ( 'NONE',  ( 39.41296390513587511, -20.41368208888610170, 71.67976084211551324 ) ) ;
#20576=ORIENTED_EDGE ( 'NONE', *, *, #5307, .F. ) ;
#20578=CARTESIAN_POINT ( 'NONE',  ( 37.80618814713140097, -3.913682088886108801, 73.13360434286904876 ) ) ;
#20579=CARTESIAN_POINT ( 'NONE',  ( 36.49096545463212493, -28.10384086642190127, 71.32335560751960202 ) ) ;
#20582=CARTESIAN_POINT ( 'NONE',  ( 39.73277004305198545, -6.213682088886108623, 73.23812341099225875 ) ) ;
#20603=CARTESIAN_POINT ( 'NONE',  ( 36.29569395875881099, -14.30384086642192010, 72.77780686321128201 ) ) ;
#20606=CARTESIAN_POINT ( 'NONE',  ( 39.82603832034400426, -24.31368208888611093, 72.40698646996131060 ) ) ;
#20609=SURFACE_STYLE_USAGE ( .BOTH. , #24834 ) ;
#20614=CARTESIAN_POINT ( 'NONE',  ( 36.11133435605973574, -27.61368208888610809, 72.15350918040381600 ) ) ;
#20618=CARTESIAN_POINT ( 'NONE',  ( 37.80618814713140097, -3.913682088886108801, 73.13360434286904876 ) ) ;
#20620=CARTESIAN_POINT ( 'NONE',  ( 36.64852494920107517, -17.41368208888610525, 70.89533451361947414 ) ) ;
#20624=CARTESIAN_POINT ( 'NONE',  ( 39.51027997493896748, -19.10384086642191193, 71.43714994484032843 ) ) ;
#20625=CARTESIAN_POINT ( 'NONE',  ( 37.69796330110504101, -5.113682088886101873, 69.66206559358663242 ) ) ;
#20628=CARTESIAN_POINT ( 'NONE',  ( 36.68196826583682935, -8.003840866421912281, 70.79240656858108593 ) ) ;
#20631=CARTESIAN_POINT ( 'NONE',  ( 39.98359781491296161, -8.413682088886105248, 71.86517103874048473 ) ) ;
#20633=CARTESIAN_POINT ( 'NONE',  ( 39.64521430340304420, -10.81368208888610027, 69.45876917294177133 ) ) ;
#20636=CARTESIAN_POINT ( 'NONE',  ( 38.63098279924290068, -10.70384086642191335, 72.53360434286905445 ) ) ;
#20641=CARTESIAN_POINT ( 'NONE',  ( 39.64521430340305841, -16.80384086642191832, 73.30173637941818754 ) ) ;
#20643=( NAMED_UNIT ( * ) SI_UNIT ( $, .STERADIAN. ) SOLID_ANGLE_UNIT ( ) );
#20644=CARTESIAN_POINT ( 'NONE',  ( 37.80618814713140097, -17.91368208888609814, 73.13360434286903455 ) ) ;
#20654=CARTESIAN_POINT ( 'NONE',  ( 38.37017380507018771, -15.60384086642190837, 69.64448340153877837 ) ) ;
#20658=CARTESIAN_POINT ( 'NONE',  ( 40.14115730948191185, -24.51368208888609601, 71.32335560751958781 ) ) ;
#20662=CARTESIAN_POINT ( 'NONE',  ( 38.37017380507018771, -23.60384086642190837, 69.64448340153877837 ) ) ;
#20665=CARTESIAN_POINT ( 'NONE',  ( 37.80618814713140097, -25.91368208888610880, 73.13360434286902034 ) ) ;
#20670=CARTESIAN_POINT ( 'NONE',  ( 37.38336156205274818, -1.713682088886100852, 72.12822762946751709 ) ) ;
#20671=CARTESIAN_POINT ( 'NONE',  ( 39.02742774030102879, 1.786317911113898704, 72.26730301774236409 ) ) ;
#20677=CARTESIAN_POINT ( 'NONE',  ( 37.33957961208645315, -5.803840866421907663, 69.94417936956673998 ) ) ;
#20688=CARTESIAN_POINT ( 'NONE',  ( 39.82603832034401847, -4.313682088886108268, 72.40698646996133903 ) ) ;
#20706=CARTESIAN_POINT ( 'NONE',  ( 37.89291511884476904, -15.11368208888610098, 70.26206559358661252 ) ) ;
#20711=CARTESIAN_POINT ( 'NONE',  ( 40.14115730948191185, -2.513682088886103116, 71.32335560751961623 ) ) ;
#20712=CARTESIAN_POINT ( 'NONE',  ( 38.26194895904384907, -22.60384086642191548, 73.11602215082116629 ) ) ;
#20714=CARTESIAN_POINT ( 'NONE',  ( 40.77203464402485622, -8.513682088886104893, 71.32335560751961623 ) ) ;
#20735=CARTESIAN_POINT ( 'NONE',  ( 38.37017380507018771, -15.60384086642191370, 69.04448340153878405 ) ) ;
#20737=CARTESIAN_POINT ( 'NONE',  ( 36.49096545463212493, -19.51368208888610312, 71.43714994484034264 ) ) ;
#20743=CARTESIAN_POINT ( 'NONE',  ( 35.86008812008917346, -0.1038408664219142574, 71.32335560751961623 ) ) ;
#20747=CARTESIAN_POINT ( 'NONE',  ( 37.25202387243752611, 0.7863179111138978161, 70.00779233799264034 ) ) ;
#20750=CARTESIAN_POINT ( 'NONE',  ( 37.25202387243752611, -23.21368208888610241, 70.00779233799262613 ) ) ;
#20758=CARTESIAN_POINT ( 'NONE',  ( 38.00113996487112189, -17.70384086642190979, 70.22690120949090442 ) ) ;
#20759=CARTESIAN_POINT ( 'NONE',  ( 37.25202387243752611, -5.213682088886100630, 70.00779233799264034 ) ) ;
#20764=CARTESIAN_POINT ( 'NONE',  ( 38.82593461698265003, -4.703840866421914235, 73.13360434286904876 ) ) ;
#20767=CARTESIAN_POINT ( 'NONE',  ( 38.26194895904383486, -7.013682088886100452, 69.64448340153879258 ) ) ;
#20769=CARTESIAN_POINT ( 'NONE',  ( 39.73277004305198545, -8.213682088886105959, 73.23812341099225875 ) ) ;
#20773=CARTESIAN_POINT ( 'NONE',  ( 39.37952058850012804, -15.00384086642191228, 71.78268878715390144 ) ) ;
#20779=CARTESIAN_POINT ( 'NONE',  ( 37.61123632939164452, -15.70384086642191157, 69.02690120949091579 ) ) ;
#20782=CARTESIAN_POINT ( 'NONE',  ( 36.87297107704152666, -21.71368208888610951, 72.49904802271740323 ) ) ;
#20788=CARTESIAN_POINT ( 'NONE',  ( 40.14115730948191185, -7.103840866421910150, 71.43714994484034264 ) ) ;
#20793=CARTESIAN_POINT ( 'NONE',  ( 37.80618814713140097, -23.91368208888610880, 73.13360434286902034 ) ) ;
#20795=CARTESIAN_POINT ( 'NONE',  ( 40.14115730948191185, -23.10384086642191193, 71.43714994484030001 ) ) ;
#20797=CARTESIAN_POINT ( 'NONE',  ( 39.29254315202756231, -26.81368208888610027, 69.94417936956671156 ) ) ;
#20802=CARTESIAN_POINT ( 'NONE',  ( 39.51027997493896748, 1.486317911113900658, 71.32335560751961623 ) ) ;
#20803=CARTESIAN_POINT ( 'NONE',  ( 38.37017380507020192, -0.01368208888610084051, 72.51602215082118619 ) ) ;
#20811=CARTESIAN_POINT ( 'NONE',  ( 37.80618814713138676, -3.703840866421904909, 69.62690120949091011 ) ) ;
#20817=CARTESIAN_POINT ( 'NONE',  ( 39.98359781491296161, -4.413682088886105248, 71.86517103874048473 ) ) ;
#20819=CARTESIAN_POINT ( 'NONE',  ( 36.64852494920107517, -26.20384086642191335, 71.86517103874047052 ) ) ;
#20833=CARTESIAN_POINT ( 'NONE',  ( 39.51027997493896748, -14.51368208888610134, 71.32335560751960202 ) ) ;
#20838=CARTESIAN_POINT ( 'NONE',  ( 37.25202387243752611, 0.7863179111138978161, 70.00779233799264034 ) ) ;
#20839=CARTESIAN_POINT ( 'NONE',  ( 39.82603832034400426, -23.30384086642190766, 70.35351908239857721 ) ) ;
#20841=CARTESIAN_POINT ( 'NONE',  ( 36.29569395875879678, -7.313682088886101162, 69.98269868914869107 ) ) ;
#20857=CARTESIAN_POINT ( 'NONE',  ( 40.77203464402485622, -15.10384086642191548, 71.43714994484032843 ) ) ;
#20858=CARTESIAN_POINT ( 'NONE',  ( 36.64852494920107517, -19.41368208888610525, 70.89533451361947414 ) ) ;
#20860=SURFACE_STYLE_FILL_AREA ( #16736 ) ;
#20864=CARTESIAN_POINT ( 'NONE',  ( 40.77203464402485622, -28.51368208888610667, 71.32335560751960202 ) ) ;
#20871=CARTESIAN_POINT ( 'NONE',  ( 36.80608444377001121, -1.313682088886099386, 70.35351908239860563 ) ) ;
#20874=CARTESIAN_POINT ( 'NONE',  ( 39.82603832034401847, -22.31368208888610738, 72.40698646996131060 ) ) ;
#20877=CARTESIAN_POINT ( 'NONE',  ( 39.02742774030101458, -19.40384086642191264, 70.49320253461759478 ) ) ;
#20878=CARTESIAN_POINT ( 'NONE',  ( 38.93415946300897446, -8.113682088886108090, 73.09843995877331224 ) ) ;
#20883=CARTESIAN_POINT ( 'NONE',  ( 39.95015449827720744, -5.003840866421912281, 71.96809898377888715 ) ) ;
#20888=CARTESIAN_POINT ( 'NONE',  ( 36.64852494920107517, -1.413682088886102806, 70.89533451361948835 ) ) ;
#20890=CARTESIAN_POINT ( 'NONE',  ( 40.55423172469004811, -12.41368208888610525, 72.05058123536544201 ) ) ;
#20894=CARTESIAN_POINT ( 'NONE',  ( 39.51027997493896748, -11.10384086642191015, 71.43714994484034264 ) ) ;
#20900=CARTESIAN_POINT ( 'NONE',  ( 40.52078840805429394, -17.00384086642191406, 72.15350918040381600 ) ) ;
#20903=CARTESIAN_POINT ( 'NONE',  ( 36.64852494920107517, -21.41368208888610525, 70.89533451361947414 ) ) ;
#20912=CARTESIAN_POINT ( 'NONE',  ( 36.49096545463212493, -8.103840866421908373, 71.32335560751963044 ) ) ;
#20915=CARTESIAN_POINT ( 'NONE',  ( 39.95015449827720744, -26.61368208888610809, 70.79240656858104330 ) ) ;
#20917=CARTESIAN_POINT ( 'NONE',  ( 37.33957961208645315, -21.80384086642190766, 69.94417936956672577 ) ) ;
#20919=CARTESIAN_POINT ( 'NONE',  ( 39.29254315202756231, -18.81368208888610027, 69.94417936956672577 ) ) ;
#20921=CARTESIAN_POINT ( 'NONE',  ( 39.64521430340304420, -26.81368208888610738, 69.45876917294174291 ) ) ;
#20925=CARTESIAN_POINT ( 'NONE',  ( 37.25260217561390874, 0.3863179111139002364, 71.78268878715394408 ) ) ;
#20934=CARTESIAN_POINT ( 'NONE',  ( 39.95015449827720744, -7.003840866421910505, 71.96809898377888715 ) ) ;
#20942=CARTESIAN_POINT ( 'NONE',  ( 36.68196826583682935, 0.3863179111138967392, 71.96809898377890136 ) ) ;
#20962=CARTESIAN_POINT ( 'NONE',  ( 37.60469502381300089, -17.21368208888610241, 70.49320253461759478 ) ) ;
#20967=CARTESIAN_POINT ( 'NONE',  ( 37.80618814713138676, -23.70384086642190979, 69.62690120949091011 ) ) ;
#20970=CARTESIAN_POINT ( 'NONE',  ( 40.26954217208371034, -4.713682088886099741, 69.89063713639259845 ) ) ;
#20988=CARTESIAN_POINT ( 'NONE',  ( 40.26954217208372455, -10.90384086642191974, 72.86986841596736042 ) ) ;
#20992=CARTESIAN_POINT ( 'NONE',  ( 36.87297107704152666, -23.71368208888610951, 72.49904802271738902 ) ) ;
#20998=CARTESIAN_POINT ( 'NONE',  ( 40.33642880535524000, -20.31368208888610738, 72.77780686321126780 ) ) ;
#21000=CARTESIAN_POINT ( 'NONE',  ( 38.82593461698262871, 1.086317911113899637, 69.62690120949091011 ) ) ;
#21002=CARTESIAN_POINT ( 'NONE',  ( 40.14115730948191185, -14.51368208888610489, 71.32335560751960202 ) ) ;
#21007=CARTESIAN_POINT ( 'NONE',  ( 37.89291511884479036, -16.50384086642191050, 72.49843995877330372 ) ) ;
#21008=CARTESIAN_POINT ( 'NONE',  ( 39.82603832034400426, -8.313682088886110932, 72.40698646996135324 ) ) ;
#21014=CARTESIAN_POINT ( 'NONE',  ( 38.82593461698265003, -6.703840866421914235, 73.13360434286904876 ) ) ;
#21017=CARTESIAN_POINT ( 'NONE',  ( 36.80608444377001121, 0.6863179111138983934, 70.35351908239860563 ) ) ;
#21020=CARTESIAN_POINT ( 'NONE',  ( 40.55423172469004811, -6.413682088886103472, 72.05058123536544201 ) ) ;
#21023=CARTESIAN_POINT ( 'NONE',  ( 38.26194895904384197, -2.603840866421912814, 72.51602215082118619 ) ) ;
#21029=CARTESIAN_POINT ( 'NONE',  ( 38.26194895904384197, -18.60384086642191548, 73.71602215082113219 ) ) ;
#21033=CARTESIAN_POINT ( 'NONE',  ( 39.75915168707250302, -20.71368208888610596, 70.26145752964251301 ) ) ;
#21039=CARTESIAN_POINT ( 'NONE',  ( 36.64852494920107517, -6.203840866421912459, 71.86517103874049894 ) ) ;
#21042=CARTESIAN_POINT ( 'NONE',  ( 37.33957961208646736, -23.81368208888611093, 72.81632618279320468 ) ) ;
#21045=CARTESIAN_POINT ( 'NONE',  ( 39.75915168707251723, -22.90384086642190908, 72.49904802271738902 ) ) ;
#21049=CARTESIAN_POINT ( 'NONE',  ( 39.98359781491296161, -16.41368208888610525, 71.86517103874047052 ) ) ;
#21051=CARTESIAN_POINT ( 'NONE',  ( 40.52078840805429394, 0.9961591335780859424, 72.15350918040385864 ) ) ;
#21055=CARTESIAN_POINT ( 'NONE',  ( 37.31647492878124694, -24.30384086642191122, 72.03616607671141026 ) ) ;
#21062=CARTESIAN_POINT ( 'NONE',  ( 36.49096545463212493, -2.103840866421912814, 71.32335560751963044 ) ) ;
#21071=CARTESIAN_POINT ( 'NONE',  ( 36.87297107704153376, -1.713682088886107957, 72.49904802271743165 ) ) ;
#21073=CARTESIAN_POINT ( 'NONE',  ( 37.33957961208645315, -25.80384086642190766, 69.94417936956671156 ) ) ;
#21089=CARTESIAN_POINT ( 'NONE',  ( 39.37952058850012804, -16.61368208888610098, 70.97781676520601479 ) ) ;
#21095=CARTESIAN_POINT ( 'NONE',  ( 37.69796330110505522, -26.50384086642190695, 73.09843995877328382 ) ) ;
#21116=CARTESIAN_POINT ( 'NONE',  ( 36.11133435605973574, -10.00384086642191761, 70.60699637195612866 ) ) ;
#21119=CARTESIAN_POINT ( 'NONE',  ( 38.37017380507020192, -18.01368208888611022, 73.11602215082116629 ) ) ;
#21125=CARTESIAN_POINT ( 'NONE',  ( 36.89935272106204422, -23.21368208888610241, 69.52238214136765748 ) ) ;
#21134=CARTESIAN_POINT ( 'NONE',  ( 39.37952058850012804, -15.00384086642191228, 71.78268878715390144 ) ) ;
#21135=CARTESIAN_POINT ( 'NONE',  ( 39.82603832034400426, -0.3136820888861094336, 72.40698646996135324 ) ) ;
#21142=CARTESIAN_POINT ( 'NONE',  ( 39.02088643472237806, -28.70384086642191690, 73.73360434286898624 ) ) ;
#21144=CARTESIAN_POINT ( 'NONE',  ( 36.49096545463212493, -1.513682088886105559, 71.43714994484035685 ) ) ;
#21145=CARTESIAN_POINT ( 'NONE',  ( 40.26954217208371034, -2.713682088886101962, 69.89063713639259845 ) ) ;
#21149=CARTESIAN_POINT ( 'NONE',  ( 38.00113996487112189, -5.703840866421911571, 70.22690120949091863 ) ) ;
#21155=CARTESIAN_POINT ( 'NONE',  ( 40.55423172469004101, -7.203840866421916900, 70.70992431699450265 ) ) ;
#21159=CARTESIAN_POINT ( 'NONE',  ( 36.49096545463212493, -11.51368208888609956, 71.43714994484034264 ) ) ;
#21166=CARTESIAN_POINT ( 'NONE',  ( 38.26194895904384907, -6.603840866421916367, 73.11602215082118050 ) ) ;
#21169=CARTESIAN_POINT ( 'NONE',  ( 39.98359781491296161, -16.41368208888610525, 71.86517103874047052 ) ) ;
#21173=CARTESIAN_POINT ( 'NONE',  ( 39.29254315202757653, -16.80384086642191477, 72.81632618279321889 ) ) ;
#21175=CARTESIAN_POINT ( 'NONE',  ( 38.93415946300897446, -20.11368208888610809, 73.09843995877329803 ) ) ;
#21177=CARTESIAN_POINT ( 'NONE',  ( 36.98690846071097837, -27.81368208888610738, 73.30173637941817333 ) ) ;
#21182=CARTESIAN_POINT ( 'NONE',  ( 38.93987200065210175, -22.80384086642191122, 72.33091598616826445 ) ) ;
#21189=CARTESIAN_POINT ( 'NONE',  ( 40.55423172469004101, -27.20384086642191690, 70.70992431699446001 ) ) ;
#21197=CARTESIAN_POINT ( 'NONE',  ( 38.93415946300897446, -25.50384086642190695, 69.66206559358661821 ) ) ;
#21209=CARTESIAN_POINT ( 'NONE',  ( 39.37952058850012804, -12.61368208888609921, 70.97781676520601479 ) ) ;
#21211=CARTESIAN_POINT ( 'NONE',  ( 37.89291511884476904, -9.113682088886102761, 70.26206559358664094 ) ) ;
#21213=ORIENTED_EDGE ( 'NONE', *, *, #5307, .T. ) ;
#21216=CARTESIAN_POINT ( 'NONE',  ( 39.95015449827720744, 1.386317911113894130, 70.79240656858108593 ) ) ;
#21217=CARTESIAN_POINT ( 'NONE',  ( 36.87297107704149823, -17.90384086642190908, 70.26145752964252722 ) ) ;
#21222=CARTESIAN_POINT ( 'NONE',  ( 39.02742774030102879, -18.21368208888610241, 72.26730301774234988 ) ) ;
#21237=CARTESIAN_POINT ( 'NONE',  ( 40.52078840805429394, -9.003840866421915834, 72.15350918040385864 ) ) ;
#21239=CARTESIAN_POINT ( 'NONE',  ( 37.33957961208646736, -15.81368208888610916, 72.81632618279321889 ) ) ;
#21246=CARTESIAN_POINT ( 'NONE',  ( 39.12911128074873801, -20.11368208888610809, 73.69843995877327814 ) ) ;
#21253=CARTESIAN_POINT ( 'NONE',  ( 37.12184278917507640, -14.10384086642191370, 71.32335560751961623 ) ) ;
#21254=CARTESIAN_POINT ( 'NONE',  ( 38.82593461698262871, -0.9136820888861022505, 69.62690120949091011 ) ) ;
#21261=CARTESIAN_POINT ( 'NONE',  ( 40.26954217208372455, -28.90384086642191619, 72.86986841596730358 ) ) ;
#21262=CARTESIAN_POINT ( 'NONE',  ( 39.75915168707250302, 1.286317911113898260, 70.26145752964255564 ) ) ;
#21263=CARTESIAN_POINT ( 'NONE',  ( 36.89935272106204422, -5.213682088886100630, 69.52238214136768590 ) ) ;
#21267=CARTESIAN_POINT ( 'NONE',  ( 39.31564783533279694, -7.303840866421912104, 70.72433947564853440 ) ) ;
#21274=CARTESIAN_POINT ( 'NONE',  ( 37.61123632939164452, -11.70384086642191335, 69.02690120949094421 ) ) ;
#21277=CARTESIAN_POINT ( 'NONE',  ( 39.98359781491296161, -12.41368208888610525, 71.86517103874047052 ) ) ;
#21282=CARTESIAN_POINT ( 'NONE',  ( 36.68196826583682935, -8.003840866421912281, 70.79240656858108593 ) ) ;
#21286=CARTESIAN_POINT ( 'NONE',  ( 39.95015449827720744, -20.61368208888610454, 70.79240656858105751 ) ) ;
#21290=CARTESIAN_POINT ( 'NONE',  ( 38.93415946300896024, -15.50384086642190873, 69.66206559358661821 ) ) ;
#21292=CARTESIAN_POINT ( 'NONE',  ( 36.80608444377001121, -15.31368208888610383, 70.35351908239857721 ) ) ;
#21294=CARTESIAN_POINT ( 'NONE',  ( 39.64521430340304420, -20.81368208888610027, 69.45876917294175712 ) ) ;
#21298=CARTESIAN_POINT ( 'NONE',  ( 37.89291511884479036, -22.50384086642191050, 72.49843995877330372 ) ) ;
#21306=CARTESIAN_POINT ( 'NONE',  ( 39.95015449827720744, -1.003840866421912281, 71.96809898377888715 ) ) ;
#21316=CARTESIAN_POINT ( 'NONE',  ( 38.82593461698264292, -28.70384086642190979, 73.13360434286902034 ) ) ;
#21322=CARTESIAN_POINT ( 'NONE',  ( 37.21915885897815457, -4.203840866421909794, 71.67976084211552745 ) ) ;
#21329=CARTESIAN_POINT ( 'NONE',  ( 38.37017380507020192, -12.01368208888610134, 72.51602215082118619 ) ) ;
#21330=CARTESIAN_POINT ( 'NONE',  ( 37.12184278917507640, -9.513682088886101340, 71.43714994484035685 ) ) ;
#21338=CARTESIAN_POINT ( 'NONE',  ( 36.64852494920107517, -14.20384086642191157, 71.86517103874048473 ) ) ;
#21341=CARTESIAN_POINT ( 'NONE',  ( 39.37952058850012804, -18.61368208888609743, 70.97781676520601479 ) ) ;
#21358=CARTESIAN_POINT ( 'NONE',  ( 36.29569395875881099, -8.303840866421920097, 72.77780686321129622 ) ) ;
#21362=CARTESIAN_POINT ( 'NONE',  ( 37.33957961208646736, -13.81368208888610916, 72.81632618279321889 ) ) ;
#21367=CARTESIAN_POINT ( 'NONE',  ( 40.55423172469004811, -24.41368208888610880, 72.05058123536539938 ) ) ;
#21382=CARTESIAN_POINT ( 'NONE',  ( 38.37017380507018771, -9.603840866421911926, 70.24448340153877268 ) ) ;
#21383=CARTESIAN_POINT ( 'NONE',  ( 38.37017380507020192, -28.01368208888610312, 72.51602215082114355 ) ) ;
#21392=CARTESIAN_POINT ( 'NONE',  ( 36.68196826583682935, -2.003840866421909617, 70.79240656858108593 ) ) ;
#21394=CARTESIAN_POINT ( 'NONE',  ( 40.14115730948191185, -0.5136820888861047818, 71.32335560751961623 ) ) ;
#21395=CARTESIAN_POINT ( 'NONE',  ( 40.77203464402485622, -0.5136820888861047818, 71.32335560751961623 ) ) ;
#21398=CARTESIAN_POINT ( 'NONE',  ( 37.60469502381300799, -6.403840866421910860, 72.26730301774236409 ) ) ;
#21403=CARTESIAN_POINT ( 'NONE',  ( 35.86008812008917346, -12.10384086642191548, 71.32335560751961623 ) ) ;
#21406=CARTESIAN_POINT ( 'NONE',  ( 36.49096545463212493, -13.51368208888610489, 71.43714994484034264 ) ) ;
#21413=CARTESIAN_POINT ( 'NONE',  ( 36.64852494920107517, -0.2038408664219101829, 71.86517103874049894 ) ) ;
#21416=CARTESIAN_POINT ( 'NONE',  ( 38.82593461698262871, -16.91368208888610170, 69.62690120949091011 ) ) ;
#21418=CARTESIAN_POINT ( 'NONE',  ( 38.37017380507018771, -19.60384086642191193, 69.64448340153877837 ) ) ;
#21421=CARTESIAN_POINT ( 'NONE',  ( 37.80618814713140097, -17.91368208888609814, 73.13360434286903455 ) ) ;
#21423=CARTESIAN_POINT ( 'NONE',  ( 40.26954217208371034, -22.71368208888610241, 69.89063713639258424 ) ) ;
#21428=CARTESIAN_POINT ( 'NONE',  ( 39.24876120206129571, -24.90384086642191264, 72.12822762946746025 ) ) ;
#21434=CARTESIAN_POINT ( 'NONE',  ( 39.02088643472237806, -28.70384086642191690, 73.73360434286898624 ) ) ;
#21438=CARTESIAN_POINT ( 'NONE',  ( 39.02088643472237095, -4.913682088886102584, 69.02690120949094421 ) ) ;
#21443=CARTESIAN_POINT ( 'NONE',  ( 38.31606138205702194, 1.691238522345987150, 73.11602215082119471 ) ) ;
#21445=CARTESIAN_POINT ( 'NONE',  ( 39.75915168707251723, -22.90384086642191264, 72.49904802271738902 ) ) ;
#21454=CARTESIAN_POINT ( 'NONE',  ( 37.38336156205273397, -3.903840866421911748, 70.63227792289248441 ) ) ;
#21460=CARTESIAN_POINT ( 'NONE',  ( 37.69225076346193504, -9.813682088886100274, 72.33091598616827866 ) ) ;
#21461=CARTESIAN_POINT ( 'NONE',  ( 37.60469502381300089, -13.21368208888610241, 70.49320253461759478 ) ) ;
#21468=CARTESIAN_POINT ( 'NONE',  ( 39.98359781491296161, -19.20384086642191335, 70.89533451361945993 ) ) ;
#21469=ADVANCED_FACE ( 'NONE', ( #4945 ), #7005, .T. ) ;
#21473=CARTESIAN_POINT ( 'NONE',  ( 37.21915885897815457, -17.41368208888610170, 71.08074471024443142 ) ) ;
#21477=CARTESIAN_POINT ( 'NONE',  ( 36.64852494920107517, -11.41368208888610525, 70.89533451361947414 ) ) ;
#21492=CARTESIAN_POINT ( 'NONE',  ( 35.86008812008917346, -10.10384086642191548, 71.32335560751961623 ) ) ;
#21495=CARTESIAN_POINT ( 'NONE',  ( 38.93415946300897446, -14.11368208888610631, 73.09843995877329803 ) ) ;
#21499=CARTESIAN_POINT ( 'NONE',  ( 40.26954217208371034, -18.71368208888610241, 69.89063713639258424 ) ) ;
#21511=CARTESIAN_POINT ( 'NONE',  ( 37.89291511884479036, -14.50384086642191228, 72.49843995877330372 ) ) ;
#21512=CARTESIAN_POINT ( 'NONE',  ( 36.80608444377001121, -1.313682088886099386, 70.35351908239860563 ) ) ;
#21520=CARTESIAN_POINT ( 'NONE',  ( 39.73277004305197124, -29.40384086642191264, 69.52238214136765748 ) ) ;
#21522=CARTESIAN_POINT ( 'NONE',  ( 37.21915885897815457, -23.41368208888610170, 71.08074471024441721 ) ) ;
#21523=CARTESIAN_POINT ( 'NONE',  ( 35.86008812008917346, -5.513682088886105781, 71.43714994484035685 ) ) ;
#21526=CARTESIAN_POINT ( 'NONE',  ( 39.51027997493896748, -5.103840866421911926, 71.43714994484034264 ) ) ;
#21534=CARTESIAN_POINT ( 'NONE',  ( 36.36258059203030513, -11.90384086642191441, 69.89063713639259845 ) ) ;
#21540=CARTESIAN_POINT ( 'NONE',  ( 39.29254315202756231, -16.81368208888610383, 69.94417936956672577 ) ) ;
#21546=CARTESIAN_POINT ( 'NONE',  ( 36.87297107704151244, 0.09615913357809147133, 70.26145752964255564 ) ) ;
#21549=CARTESIAN_POINT ( 'NONE',  ( 37.33957961208646736, -19.81368208888611093, 72.81632618279321889 ) ) ;
#21552=CARTESIAN_POINT ( 'NONE',  ( 37.33957961208645315, -19.80384086642191122, 69.94417936956672577 ) ) ;
#21554=CARTESIAN_POINT ( 'NONE',  ( 36.87297107704152666, -11.71368208888611129, 72.49904802271740323 ) ) ;
#21556=CARTESIAN_POINT ( 'NONE',  ( 38.26194895904383486, -23.01368208888610312, 69.04448340153878405 ) ) ;
#21561=CARTESIAN_POINT ( 'NONE',  ( 37.60469502381300799, -22.40384086642191264, 72.26730301774234988 ) ) ;
#21568=CARTESIAN_POINT ( 'NONE',  ( 39.29254315202757653, -0.8038408664219134359, 72.81632618279323310 ) ) ;
#21570=CARTESIAN_POINT ( 'NONE',  ( 36.89935272106204422, -1.213682088886100630, 69.52238214136768590 ) ) ;
#21577=CARTESIAN_POINT ( 'NONE',  ( 37.25202387243754032, -20.40384086642191619, 72.75271321436731853 ) ) ;
#21586=CARTESIAN_POINT ( 'NONE',  ( 38.73920764526923932, -7.503840866421911393, 70.26206559358664094 ) ) ;
#21594=CARTESIAN_POINT ( 'NONE',  ( 39.51027997493896748, -12.51368208888610134, 71.32335560751960202 ) ) ;
#21595=CARTESIAN_POINT ( 'NONE',  ( 38.00113996487114321, -9.913682088886099919, 72.53360434286905445 ) ) ;
#21602=CARTESIAN_POINT ( 'NONE',  ( 36.87297107704149823, -15.90384086642190908, 70.26145752964252722 ) ) ;
#21606=CARTESIAN_POINT ( 'NONE',  ( 38.26194895904383486, -19.01368208888609956, 70.24448340153875847 ) ) ;
#21610=CARTESIAN_POINT ( 'NONE',  ( 39.75915168707250302, -12.71368208888610063, 70.26145752964252722 ) ) ;
#21614=CARTESIAN_POINT ( 'NONE',  ( 40.15363366728724515, -29.10876147765395672, 71.30696959218165887 ) ) ;
#21622=CARTESIAN_POINT ( 'NONE',  ( 40.77203464402485622, -7.103840866421913702, 71.43714994484034264 ) ) ;
#21625=CARTESIAN_POINT ( 'NONE',  ( 36.68196826583682935, -17.61368208888610454, 71.96809898377888715 ) ) ;
#21630=CARTESIAN_POINT ( 'NONE',  ( 37.61123632939165873, -11.91368208888610880, 73.73360434286898624 ) ) ;
#21636=CARTESIAN_POINT ( 'NONE',  ( 38.00113996487112189, -15.70384086642191157, 70.22690120949090442 ) ) ;
#21637=CARTESIAN_POINT ( 'NONE',  ( 39.82603832034400426, -2.313682088886107380, 72.40698646996135324 ) ) ;
#21643=CARTESIAN_POINT ( 'NONE',  ( 38.37017380507018771, -27.60384086642191548, 69.04448340153878405 ) ) ;
#21645=CARTESIAN_POINT ( 'NONE',  ( 39.31564783533280405, -26.31368208888610027, 72.03616607671136762 ) ) ;
#21647=CARTESIAN_POINT ( 'NONE',  ( 39.02088643472237095, -0.9136820888861024725, 69.02690120949094421 ) ) ;
#21650=CARTESIAN_POINT ( 'NONE',  ( 38.73920764526923932, 0.4961591335780889955, 70.26206559358665515 ) ) ;
#21656=CARTESIAN_POINT ( 'NONE',  ( 36.98690846071097127, -3.803840866421912992, 69.45876917294177133 ) ) ;
#21659=CARTESIAN_POINT ( 'NONE',  ( 37.33957961208646736, -11.81368208888610916, 72.81632618279321889 ) ) ;
#21661=CARTESIAN_POINT ( 'NONE',  ( 38.93415946300898867, -24.11368208888610809, 73.09843995877328382 ) ) ;
#21663=CARTESIAN_POINT ( 'NONE',  ( 39.75915168707251723, 1.096159133578084921, 72.49904802271743165 ) ) ;
#21666=CARTESIAN_POINT ( 'NONE',  ( 36.49096545463212493, -21.51368208888609956, 71.43714994484034264 ) ) ;
#21671=CARTESIAN_POINT ( 'NONE',  ( 36.80608444377001831, -16.30384086642191477, 72.40698646996135324 ) ) ;
#21675=CARTESIAN_POINT ( 'NONE',  ( 38.37017380507020192, -14.01368208888610845, 73.11602215082116629 ) ) ;
#21677=CARTESIAN_POINT ( 'NONE',  ( 38.37017380507020192, -22.01368208888611022, 73.71602215082113219 ) ) ;
#21681=CARTESIAN_POINT ( 'NONE',  ( 37.12184278917507640, -20.10384086642191193, 71.32335560751961623 ) ) ;
#21687=CARTESIAN_POINT ( 'NONE',  ( 36.36258059203030513, -27.90384086642191264, 69.89063713639258424 ) ) ;
#21689=CARTESIAN_POINT ( 'NONE',  ( 37.50301148336529167, -1.113682088886101207, 69.06206559358666652 ) ) ;
#21698=CARTESIAN_POINT ( 'NONE',  ( 37.25202387243754032, -24.40384086642191619, 72.75271321436730432 ) ) ;
#21705=CARTESIAN_POINT ( 'NONE',  ( 39.31564783533279694, -9.303840866421909439, 70.72433947564853440 ) ) ;
#21714=CARTESIAN_POINT ( 'NONE',  ( 37.38336156205274818, -11.71368208888610241, 72.12822762946750288 ) ) ;
#21717=CARTESIAN_POINT ( 'NONE',  ( 37.69225076346193504, -5.813682088886100274, 72.33091598616827866 ) ) ;
#21725=CARTESIAN_POINT ( 'NONE',  ( 39.98359781491296161, -17.20384086642190979, 70.89533451361945993 ) ) ;
#21728=CARTESIAN_POINT ( 'NONE',  ( 38.93987200065208754, -20.81368208888610027, 70.42958956619168021 ) ) ;
#21732=CARTESIAN_POINT ( 'NONE',  ( 38.37017380507020192, -12.01368208888610845, 73.11602215082116629 ) ) ;
#21745=CARTESIAN_POINT ( 'NONE',  ( 39.12911128074872380, -1.503840866421912725, 69.06206559358666652 ) ) ;
#21749=CARTESIAN_POINT ( 'NONE',  ( 36.87297107704152666, -7.713682088886109511, 72.49904802271743165 ) ) ;
#21753=CARTESIAN_POINT ( 'NONE',  ( 36.36258059203031934, -17.71368208888610596, 72.86986841596736042 ) ) ;
#21765=CARTESIAN_POINT ( 'NONE',  ( 38.26194895904383486, -23.01368208888610312, 70.24448340153875847 ) ) ;
#21774=CARTESIAN_POINT ( 'NONE',  ( 36.36258059203030513, -21.90384086642191619, 69.89063713639259845 ) ) ;
#21776=CARTESIAN_POINT ( 'NONE',  ( 39.51027997493896748, -24.51368208888610312, 71.32335560751960202 ) ) ;
#21777=CARTESIAN_POINT ( 'NONE',  ( 36.36258059203031934, 0.2863179111138938193, 72.86986841596736042 ) ) ;
#21780=CARTESIAN_POINT ( 'NONE',  ( 37.12184278917507640, -0.1038408664219107880, 71.32335560751961623 ) ) ;
#21786=CARTESIAN_POINT ( 'NONE',  ( 36.07789103942399578, -2.203840866421915123, 72.05058123536544201 ) ) ;
#21790=CARTESIAN_POINT ( 'NONE',  ( 38.26194895904383486, -5.013682088886102228, 69.64448340153879258 ) ) ;
#21792=CARTESIAN_POINT ( 'NONE',  ( 36.87297107704153376, -27.71368208888610596, 72.49904802271738902 ) ) ;
#21795=CARTESIAN_POINT ( 'NONE',  ( 37.33957961208645315, -1.803840866421907441, 69.94417936956673998 ) ) ;
#21798=CARTESIAN_POINT ( 'NONE',  ( 37.33957961208646736, -9.813682088886107380, 72.81632618279323310 ) ) ;
#21801=CARTESIAN_POINT ( 'NONE',  ( 38.26194895904384907, -10.60384086642191726, 73.11602215082118050 ) ) ;
#21803=CARTESIAN_POINT ( 'NONE',  ( 39.38009889167650357, -12.21368208888610596, 72.75271321436731853 ) ) ;
#21805=CARTESIAN_POINT ( 'NONE',  ( 40.52078840805428683, -22.61368208888610454, 70.60699637195608602 ) ) ;
#21809=CARTESIAN_POINT ( 'NONE',  ( 37.38336156205273397, -19.90384086642191264, 70.63227792289247020 ) ) ;
#21814=CARTESIAN_POINT ( 'NONE',  ( 36.07789103942399578, -20.20384086642191335, 72.05058123536544201 ) ) ;
#21816=CARTESIAN_POINT ( 'NONE',  ( 39.12911128074873801, -0.1136820888861071882, 73.69843995877330656 ) ) ;
#21823=CARTESIAN_POINT ( 'NONE',  ( 38.93415946300897446, -21.50384086642190340, 69.66206559358663242 ) ) ;
#21833=CARTESIAN_POINT ( 'NONE',  ( 38.26194895904384197, -4.603840866421910150, 72.51602215082118619 ) ) ;
#21836=FACE_OUTER_BOUND ( 'NONE', #1863, .T. ) ;
#21840=CARTESIAN_POINT ( 'NONE',  ( 37.38336156205274818, -7.713682088886103294, 72.12822762946751709 ) ) ;
#21841=CARTESIAN_POINT ( 'NONE',  ( 39.31564783533280405, -6.313682088886101162, 72.03616607671141026 ) ) ;
#21847=CARTESIAN_POINT ( 'NONE',  ( 36.87297107704149823, -7.903840866421908196, 70.26145752964255564 ) ) ;
#21861=CARTESIAN_POINT ( 'NONE',  ( 38.26194895904383486, -13.01368208888610134, 69.64448340153877837 ) ) ;
#21876=CARTESIAN_POINT ( 'NONE',  ( 36.98690846071097127, -3.803840866421912992, 69.45876917294177133 ) ) ;
#21877=VERTEX_POINT ( 'NONE', #4781 ) ;
#21881=CARTESIAN_POINT ( 'NONE',  ( 40.14115730948191185, -6.513682088886103116, 71.32335560751961623 ) ) ;
#21884=CARTESIAN_POINT ( 'NONE',  ( 38.26194895904383486, -13.01368208888610312, 69.04448340153878405 ) ) ;
#21894=CARTESIAN_POINT ( 'NONE',  ( 38.73920764526925353, -24.11368208888610098, 72.49843995877328950 ) ) ;
#21900=CARTESIAN_POINT ( 'NONE',  ( 36.11133435605973574, -24.00384086642191761, 70.60699637195608602 ) ) ;
#21902=CARTESIAN_POINT ( 'NONE',  ( 36.89935272106204422, 0.7863179111138978161, 69.52238214136768590 ) ) ;
#21909=CARTESIAN_POINT ( 'NONE',  ( 39.02088643472237806, -2.703840866421919120, 73.73360434286902887 ) ) ;
#21912=CARTESIAN_POINT ( 'NONE',  ( 36.64852494920107517, -7.413682088886104360, 70.89533451361948835 ) ) ;
#21916=CARTESIAN_POINT ( 'NONE',  ( 37.33957961208646736, -25.81368208888610738, 72.81632618279320468 ) ) ;
#21919=CARTESIAN_POINT ( 'NONE',  ( 39.38009889167648936, 0.5961591335780919154, 70.00779233799265455 ) ) ;
#21922=CARTESIAN_POINT ( 'NONE',  ( 38.00113996487112189, -23.70384086642191335, 70.22690120949089021 ) ) ;
#21923=CARTESIAN_POINT ( 'NONE',  ( 37.25202387243752611, -15.21368208888610063, 70.00779233799262613 ) ) ;
#21927=CARTESIAN_POINT ( 'NONE',  ( 38.93415946300896024, -13.50384086642190518, 69.66206559358661821 ) ) ;
#21930=CARTESIAN_POINT ( 'NONE',  ( 36.68196826583682935, -11.61368208888610276, 71.96809898377888715 ) ) ;
#21932=CARTESIAN_POINT ( 'NONE',  ( 39.64521430340304420, -14.81368208888610205, 69.45876917294175712 ) ) ;
#21936=CARTESIAN_POINT ( 'NONE',  ( 39.02742774030101458, -17.40384086642191264, 70.49320253461759478 ) ) ;
#21941=CARTESIAN_POINT ( 'NONE',  ( 36.29569395875881099, -24.30384086642192187, 72.77780686321126780 ) ) ;
#21944=CARTESIAN_POINT ( 'NONE',  ( 36.87297107704152666, -23.71368208888610951, 72.49904802271738902 ) ) ;
#21952=CARTESIAN_POINT ( 'NONE',  ( 38.37017380507018771, -23.60384086642190837, 69.64448340153877837 ) ) ;
#21959=CARTESIAN_POINT ( 'NONE',  ( 39.51027997493896748, -1.103840866421911704, 71.43714994484034264 ) ) ;
#21963=CARTESIAN_POINT ( 'NONE',  ( 39.29254315202756231, -28.81368208888610383, 69.94417936956671156 ) ) ;
#21968=CARTESIAN_POINT ( 'NONE',  ( 39.31564783533280405, -8.313682088886102051, 72.03616607671141026 ) ) ;
#21969=CARTESIAN_POINT ( 'NONE',  ( 37.38336156205274818, -5.713682088886101518, 72.12822762946751709 ) ) ;
#21975=CARTESIAN_POINT ( 'NONE',  ( 38.93415946300896024, -13.50384086642190518, 69.66206559358661821 ) ) ;
#21987=CARTESIAN_POINT ( 'NONE',  ( 39.98359781491296161, -6.413682088886103472, 71.86517103874048473 ) ) ;
#21992=CARTESIAN_POINT ( 'NONE',  ( 40.05245289102396100, -29.10876147765230115, 71.40796565871902146 ) ) ;
#22003=CARTESIAN_POINT ( 'NONE',  ( 39.73277004305197124, -7.403840866421910860, 69.52238214136768590 ) ) ;
#22008=CARTESIAN_POINT ( 'NONE',  ( 37.33957961208646736, -5.813682088886107380, 72.81632618279323310 ) ) ;
#22011=CARTESIAN_POINT ( 'NONE',  ( 39.12911128074873801, -18.11368208888610454, 73.69843995877327814 ) ) ;
#22018=CARTESIAN_POINT ( 'NONE',  ( 38.63098279924288647, -24.91368208888610170, 70.22690120949089021 ) ) ;
#22024=CARTESIAN_POINT ( 'NONE',  ( 39.02088643472237806, -26.70384086642192401, 73.73360434286898624 ) ) ;
#22027=CARTESIAN_POINT ( 'NONE',  ( 39.29254315202756231, -24.81368208888610383, 69.94417936956671156 ) ) ;
#22028=DIRECTION ( 'NONE',  ( 0.9835979625596965592, -0.1803747433772641684, -2.086002012065537230E-15 ) ) ;
#22035=CARTESIAN_POINT ( 'NONE',  ( 36.07789103942399578, -6.203840866421916900, 72.05058123536544201 ) ) ;
#22038=CARTESIAN_POINT ( 'NONE',  ( 37.80618814713140097, -9.913682088886107024, 73.13360434286904876 ) ) ;
#22040=CARTESIAN_POINT ( 'NONE',  ( 39.59324923284151510, -28.74115096347518161, 70.20355626897213597 ) ) ;
#22045=CARTESIAN_POINT ( 'NONE',  ( 37.60469502381300799, -24.40384086642190908, 72.26730301774232146 ) ) ;
#22046=CARTESIAN_POINT ( 'NONE',  ( 37.80618814713140097, -13.91368208888610347, 73.13360434286903455 ) ) ;
#22048=CARTESIAN_POINT ( 'NONE',  ( 37.25202387243754032, -14.40384086642191619, 72.75271321436731853 ) ) ;
#22050=CARTESIAN_POINT ( 'NONE',  ( 39.29254315202756231, -12.81368208888610383, 69.94417936956672577 ) ) ;
#22052=CARTESIAN_POINT ( 'NONE',  ( 39.73277004305198545, -14.21368208888610951, 73.23812341099225875 ) ) ;
#22056=CARTESIAN_POINT ( 'NONE',  ( 39.02742774030101458, -19.40384086642191264, 70.49320253461759478 ) ) ;
#22061=CARTESIAN_POINT ( 'NONE',  ( 36.89935272106205133, -22.40384086642191974, 73.23812341099225875 ) ) ;
#22063=CARTESIAN_POINT ( 'NONE',  ( 36.68196826583682935, -25.61368208888610454, 71.96809898377887293 ) ) ;
#22072=CARTESIAN_POINT ( 'NONE',  ( 36.68196826583682935, -14.00384086642191228, 70.79240656858107172 ) ) ;
#22078=CARTESIAN_POINT ( 'NONE',  ( 38.73920764526923932, 0.4961591335780889955, 70.26206559358665515 ) ) ;
#22088=CARTESIAN_POINT ( 'NONE',  ( 37.31647492878122563, -3.313682088886101607, 70.72433947564853440 ) ) ;
#22089=CARTESIAN_POINT ( 'NONE',  ( 38.93987200065208754, -6.813682088886101162, 70.42958956619168021 ) ) ;
#22096=CARTESIAN_POINT ( 'NONE',  ( 39.95015449827720744, -11.00384086642191050, 71.96809898377888715 ) ) ;
#22107=CARTESIAN_POINT ( 'NONE',  ( 39.95015449827720744, -8.613682088886104538, 70.79240656858107172 ) ) ;
#22122=CARTESIAN_POINT ( 'NONE',  ( 38.37017380507018771, -7.603840866421910150, 69.04448340153881247 ) ) ;
#22125=CARTESIAN_POINT ( 'NONE',  ( 39.75915168707250302, -10.71368208888609885, 70.26145752964252722 ) ) ;
#22127=CARTESIAN_POINT ( 'NONE',  ( 36.36258059203031934, -13.71368208888610773, 72.86986841596736042 ) ) ;
#22139=CARTESIAN_POINT ( 'NONE',  ( 37.69225076346193504, -23.81368208888610027, 72.33091598616823603 ) ) ;
#22146=CARTESIAN_POINT ( 'NONE',  ( 40.33642880535521869, -25.30384086642191477, 69.98269868914864844 ) ) ;
#22148=CARTESIAN_POINT ( 'NONE',  ( 39.64521430340304420, 1.186317911113898838, 69.45876917294178554 ) ) ;
#22155=CARTESIAN_POINT ( 'NONE',  ( 38.37017380507018771, -3.603840866421911038, 69.04448340153881247 ) ) ;
#22160=CARTESIAN_POINT ( 'NONE',  ( 38.37017380507020192, -10.01368208888611022, 73.11602215082118050 ) ) ;
#22163=CARTESIAN_POINT ( 'NONE',  ( 36.68196826583682935, -25.61368208888610454, 71.96809898377887293 ) ) ;
#22172=CARTESIAN_POINT ( 'NONE',  ( 38.93987200065210175, -22.80384086642191122, 72.33091598616826445 ) ) ;
#22173=CARTESIAN_POINT ( 'NONE',  ( 38.93415946300897446, -14.11368208888610631, 73.09843995877329803 ) ) ;
#22177=CARTESIAN_POINT ( 'NONE',  ( 36.68196826583682935, -10.00384086642191406, 70.79240656858108593 ) ) ;
#22179=CARTESIAN_POINT ( 'NONE',  ( 39.29254315202756231, -4.813682088886099386, 69.94417936956673998 ) ) ;
#22181=CARTESIAN_POINT ( 'NONE',  ( 39.02088643472237095, -14.91368208888609992, 69.02690120949091579 ) ) ;
#22185=CARTESIAN_POINT ( 'NONE',  ( 37.60469502381300799, -16.40384086642191264, 72.26730301774234988 ) ) ;
#22192=CARTESIAN_POINT ( 'NONE',  ( 36.36258059203030513, -21.90384086642191619, 69.89063713639259845 ) ) ;
#22194=CARTESIAN_POINT ( 'NONE',  ( 39.82603832034400426, -24.31368208888611093, 72.40698646996131060 ) ) ;
#22201=CARTESIAN_POINT ( 'NONE',  ( 37.80618814713138676, -17.70384086642190979, 69.62690120949091011 ) ) ;
#22207=CARTESIAN_POINT ( 'NONE',  ( 37.38336156205273397, -1.903840866421910638, 70.63227792289248441 ) ) ;
#22218=CARTESIAN_POINT ( 'NONE',  ( 37.31647492878122563, -7.313682088886101162, 70.72433947564853440 ) ) ;
#22219=CARTESIAN_POINT ( 'NONE',  ( 38.63098279924288647, -4.913682088886102584, 70.22690120949091863 ) ) ;
#22228=CARTESIAN_POINT ( 'NONE',  ( 39.75915168707251723, -8.903840866421916189, 72.49904802271740323 ) ) ;
#22235=CARTESIAN_POINT ( 'NONE',  ( 38.26194895904383486, -9.013682088886101340, 69.64448340153879258 ) ) ;
#22248=CARTESIAN_POINT ( 'NONE',  ( 39.73277004305198545, -28.21368208888611306, 73.23812341099225875 ) ) ;
#22250=CARTESIAN_POINT ( 'NONE',  ( 38.93987200065208754, -20.81368208888610027, 70.42958956619168021 ) ) ;
#22255=CARTESIAN_POINT ( 'NONE',  ( 36.64852494920107517, -11.41368208888610525, 70.89533451361947414 ) ) ;
#22256=CARTESIAN_POINT ( 'NONE',  ( 37.25260217561390874, -2.003840866421909617, 70.97781676520604321 ) ) ;
#22259=CARTESIAN_POINT ( 'NONE',  ( 36.36258059203031934, -11.71368208888610951, 72.86986841596736042 ) ) ;
#22274=CARTESIAN_POINT ( 'NONE',  ( 38.37017380507018771, -23.60384086642191903, 69.04448340153878405 ) ) ;
#22275=CARTESIAN_POINT ( 'NONE',  ( 37.33957961208646736, -25.81368208888610738, 72.81632618279320468 ) ) ;
#22278=( LENGTH_UNIT ( ) NAMED_UNIT ( * ) SI_UNIT ( .MILLI., .METRE. ) );
#22282=CARTESIAN_POINT ( 'NONE',  ( 37.50301148336529167, -25.11368208888610454, 69.06206559358663810 ) ) ;
#22286=CARTESIAN_POINT ( 'NONE',  ( 40.14115730948191185, -6.513682088886103116, 71.32335560751961623 ) ) ;
#22290=CARTESIAN_POINT ( 'NONE',  ( 37.69796330110504101, -23.11368208888609743, 69.66206559358661821 ) ) ;
#22293=CARTESIAN_POINT ( 'NONE',  ( 38.63098279924290068, -22.70384086642191335, 72.53360434286904024 ) ) ;
#22294=CARTESIAN_POINT ( 'NONE',  ( 38.93415946300897446, -10.11368208888610987, 73.09843995877331224 ) ) ;
#22299=CARTESIAN_POINT ( 'NONE',  ( 38.82593461698265003, -8.703840866421909794, 73.13360434286904876 ) ) ;
#22305=CARTESIAN_POINT ( 'NONE',  ( 36.80608444377001121, -3.313682088886100718, 70.35351908239860563 ) ) ;
#22307=CARTESIAN_POINT ( 'NONE',  ( 38.26194895904383486, -13.01368208888610312, 69.04448340153878405 ) ) ;
#22312=CARTESIAN_POINT ( 'NONE',  ( 39.37952058850012804, -9.003840866421910505, 71.78268878715392987 ) ) ;
#22319=CARTESIAN_POINT ( 'NONE',  ( 39.12911128074872380, -23.50384086642191050, 69.06206559358665231 ) ) ;
#22321=CARTESIAN_POINT ( 'NONE',  ( 40.77203464402485622, 1.486317911113896661, 71.32335560751961623 ) ) ;
#22331=CARTESIAN_POINT ( 'NONE',  ( 39.98359781491296161, -15.20384086642191157, 70.89533451361945993 ) ) ;
#22337=CARTESIAN_POINT ( 'NONE',  ( 39.51027997493896748, 0.8961591335780900724, 71.43714994484035685 ) ) ;
#22341=CARTESIAN_POINT ( 'NONE',  ( 39.38009889167650357, -24.21368208888610596, 72.75271321436730432 ) ) ;
#22347=CARTESIAN_POINT ( 'NONE',  ( 39.37952058850012804, -2.613682088886102761, 70.97781676520601479 ) ) ;
#22348=CARTESIAN_POINT ( 'NONE',  ( 37.21915885897815457, -1.413682088886099253, 71.08074471024443142 ) ) ;
#22355=CARTESIAN_POINT ( 'NONE',  ( 39.95015449827720744, -13.00384086642191228, 71.96809898377887293 ) ) ;
#22364=CARTESIAN_POINT ( 'NONE',  ( 36.87297107704153376, -9.713682088886107735, 72.49904802271743165 ) ) ;
#22378=CARTESIAN_POINT ( 'NONE',  ( 40.55423172469004811, -26.41368208888610880, 72.05058123536539938 ) ) ;
#22380=CARTESIAN_POINT ( 'NONE',  ( 37.12184278917507640, -25.51368208888609956, 71.43714994484032843 ) ) ;
#22384=CARTESIAN_POINT ( 'NONE',  ( 37.25202387243752611, -5.213682088886100630, 70.00779233799264034 ) ) ;
#22385=CARTESIAN_POINT ( 'NONE',  ( 37.89291511884479036, -0.5038408664219118371, 72.49843995877331793 ) ) ;
#22389=CARTESIAN_POINT ( 'NONE',  ( 35.86008812008917346, -7.513682088886104893, 71.43714994484035685 ) ) ;
#22405=CARTESIAN_POINT ( 'NONE',  ( 39.02088643472237806, -16.70384086642191690, 73.73360434286898624 ) ) ;
#22407=CARTESIAN_POINT ( 'NONE',  ( 39.29254315202756231, -22.81368208888610027, 69.94417936956672577 ) ) ;
#22413=CARTESIAN_POINT ( 'NONE',  ( 39.73277004305197124, 0.5961591335780883627, 69.52238214136770011 ) ) ;
#22418=CARTESIAN_POINT ( 'NONE',  ( 39.38009889167650357, 1.786317911113891821, 72.75271321436734695 ) ) ;
#22420=CARTESIAN_POINT ( 'NONE',  ( 38.93415946300898867, -18.11368208888610809, 73.09843995877329803 ) ) ;
#22423=CARTESIAN_POINT ( 'NONE',  ( 37.21915885897815457, -24.20384086642190979, 71.67976084211551324 ) ) ;
#22424=CARTESIAN_POINT ( 'NONE',  ( 39.75915168707250302, -6.713682088886099741, 70.26145752964252722 ) ) ;
#22429=CARTESIAN_POINT ( 'NONE',  ( 36.49096545463212493, -4.103840866421911038, 71.32335560751963044 ) ) ;
#22432=CARTESIAN_POINT ( 'NONE',  ( 36.87297107704152666, -5.713682088886105959, 72.49904802271743165 ) ) ;
#22434=CARTESIAN_POINT ( 'NONE',  ( 38.37017380507020192, -14.01368208888610845, 73.71602215082113219 ) ) ;
#22438=CARTESIAN_POINT ( 'NONE',  ( 38.93987200065210175, -14.80384086642191122, 72.33091598616826445 ) ) ;
#22443=CARTESIAN_POINT ( 'NONE',  ( 40.52078840805429394, -15.00384086642191583, 72.15350918040381600 ) ) ;
#22446=CARTESIAN_POINT ( 'NONE',  ( 39.38009889167650357, -22.21368208888610951, 72.75271321436731853 ) ) ;
#22454=CARTESIAN_POINT ( 'NONE',  ( 39.75915168707251723, -12.90384086642191797, 72.49904802271738902 ) ) ;
#22460=CARTESIAN_POINT ( 'NONE',  ( 40.14115730948191185, -25.10384086642190482, 71.43714994484028580 ) ) ;
#22464=CARTESIAN_POINT ( 'NONE',  ( 38.26194895904383486, -23.01368208888609956, 69.64448340153877837 ) ) ;
#22470=CARTESIAN_POINT ( 'NONE',  ( 38.37017380507020192, -2.013682088886102228, 72.51602215082118619 ) ) ;
#22471=CARTESIAN_POINT ( 'NONE',  ( 38.26194895904383486, -1.013682088886101784, 70.24448340153877268 ) ) ;
#22478=CARTESIAN_POINT ( 'NONE',  ( 36.49096545463212493, -4.103840866421911038, 71.32335560751963044 ) ) ;
#22487=CARTESIAN_POINT ( 'NONE',  ( 36.87297107704153376, 0.2863179111138939303, 72.49904802271743165 ) ) ;
#22500=CARTESIAN_POINT ( 'NONE',  ( 39.73277004305197124, 0.5961591335780883627, 69.52238214136770011 ) ) ;
#22504=CARTESIAN_POINT ( 'NONE',  ( 39.51027997493896748, -20.51368208888610312, 71.32335560751960202 ) ) ;
#22508=CARTESIAN_POINT ( 'NONE',  ( 38.82593461698262871, -0.9136820888861022505, 69.62690120949091011 ) ) ;
#22509=CARTESIAN_POINT ( 'NONE',  ( 38.73920764526923932, -1.503840866421912725, 70.26206559358664094 ) ) ;
#22512=CARTESIAN_POINT ( 'NONE',  ( 36.07789103942398867, -5.413682088886107024, 70.70992431699450265 ) ) ;
#22528=CARTESIAN_POINT ( 'NONE',  ( 36.89935272106205133, -14.40384086642191974, 73.23812341099225875 ) ) ;
#22529=CARTESIAN_POINT ( 'NONE',  ( 38.26194895904383486, -19.01368208888610312, 69.64448340153877837 ) ) ;
#22537=DIRECTION ( 'NONE',  ( 1.000000000000000000, 0.000000000000000000, 0.000000000000000000 ) ) ;
#22541=DIRECTION ( 'NONE',  ( 0.9835979625596985576, -0.1803747433772529551, -2.086002012065456372E-15 ) ) ;
#22542=CARTESIAN_POINT ( 'NONE',  ( 38.26194895904383486, -29.01368208888610312, 69.04448340153878405 ) ) ;
#22546=CARTESIAN_POINT ( 'NONE',  ( 39.82603832034400426, -0.3136820888861094336, 72.40698646996135324 ) ) ;
#22548=CARTESIAN_POINT ( 'NONE',  ( 39.95015449827720744, -22.61368208888610809, 70.79240656858105751 ) ) ;
#22552=CARTESIAN_POINT ( 'NONE',  ( 37.89291511884479036, -20.50384086642191406, 72.49843995877330372 ) ) ;
#22553=CARTESIAN_POINT ( 'NONE',  ( 39.95015449827720744, -2.613682088886105870, 70.79240656858107172 ) ) ;
#22558=CARTESIAN_POINT ( 'NONE',  ( 39.75915168707251723, -2.903840866421913525, 72.49904802271740323 ) ) ;
#22560=CARTESIAN_POINT ( 'NONE',  ( 37.69796330110504101, -7.113682088886100985, 69.66206559358663242 ) ) ;
#22562=CARTESIAN_POINT ( 'NONE',  ( 35.86008812008917346, -7.513682088886104893, 71.43714994484035685 ) ) ;
#22565=CARTESIAN_POINT ( 'NONE',  ( 39.37952058850012804, -11.00384086642191050, 71.78268878715392987 ) ) ;
#22570=CARTESIAN_POINT ( 'NONE',  ( 39.64521430340305841, -14.80384086642191832, 73.30173637941818754 ) ) ;
#22573=CARTESIAN_POINT ( 'NONE',  ( 36.87297107704152666, -19.71368208888610951, 72.49904802271740323 ) ) ;
#22581=CARTESIAN_POINT ( 'NONE',  ( 36.68196826583682935, -12.00384086642191228, 70.79240656858107172 ) ) ;
#22585=CARTESIAN_POINT ( 'NONE',  ( 38.93415946300897446, -28.11368208888610098, 73.09843995877328382 ) ) ;
#22588=CARTESIAN_POINT ( 'NONE',  ( 38.93415946300896024, -27.50384086642189985, 69.66206559358660400 ) ) ;
#22591=( BOUNDED_CURVE ( )  B_SPLINE_CURVE ( 2, ( #22040, #18060, #20111, #8399, #2447, #17939, #23712, #16109, #6335, #6078, #16240, #21792, #12396, #10324, #8267, #8022, #2071, #4150, #6456, #4528, #14314, #15977, #23834, #6206, #14062, #12019, #5956, #13936, #23961, #20236, #21916, #142, #22163, #19859, #2200, #2574, #9, #7891, #15739, #23589, #256, #9951, #13807, #10081, #12148, #15860, #19987, #21661, #2319, #17811, #11889, #14195, #20367, #12900, #16747, #6703, #20750, #22290, #6963, #18686, #6577, #10834, #22548, #9038, #24460, #20874, #10958, #1023, #2697, #764, #20488, #18811, #10580, #3212, #8655, #18559, #14814, #6832, #14683, #22673, #4651, #4898, #8520, #24715, #8907, #16882, #22802, #14946, #5030, #5164, #18316, #3087, #24582, #13021, #1148, #7090, #637, #8781, #16356, #12649, #18434, #16485, #24204, #14562, #14440, #12529, #24332, #22420, #4771, #2822, #10713, #888, #16617, #12776, #20620, #2952, #13755, #17620, #23524, #7962, #9646, #15925, #19544, #11221, #8084, #15543, #13625, #14008, #10018, #18946, #4090, #1284, #11706, #1748, #11830, #25322, #23781, #5283, #2013, #24847, #9894, #13150, #22921, #21002, #3344, #6020, #17747, #7700, #13877, #15065, #79, #19669, #7222, #19071, #3956, #15677, #2137, #25451, #21861, #11963, #15807, #21610, #23664, #7829, #5762, #206, #1880, #6148, #21732, #19800, #11089, #9764, #23393, #17881, #21477, #9167, #17497, #17013, #5893, #3823, #4214, #10527, #24032, #14381, #4472, #12595, #2266, #8339, #12468, #12083, #10142, #22364, #18132, #8722, #12338, #16181, #18004, #2391, #22235, #16554, #20180, #19931, #22107, #18374, #20430, #6405, #14259, #10652, #14134, #2515, #16428, #6276, #832, #10394, #18256, #20053, #587, #327, #8464, #23905, #16054, #10268, #24404, #457, #21987, #14631, #20313, #8208, #16298, #4723, #24149, #6522, #2645, #2761, #4597, #6645, #705, #8590, #6780, #24279, #14506, #4347, #18501, #12209, #20817, #20688, #19138, #11157, #8851, #1220, #14876, #3283, #25029, #7417, #22737, #3024, #24523, #16690, #1475, #19011, #16818, #3151, #7028, #13089, #15013, #5106, #2890, #10902, #9359, #18754, #17205, #21071, #12713, #12968, #1087, #18622, #22867, #9109, #962, #3415, #11294, #1349, #6901, #9238, #11024, #13222, #7161, #18881, #8972, #17084, #24903, #22487, #20942, #24654, #12838, #7286, #5226, #15135, #22989, #5355, #16948, #24780, #14757, #4840, #10776, #20557, #22614, #4970, #44 ),
 .UNSPECIFIED., .F., .T. ) 
 B_SPLINE_CURVE_WITH_KNOTS ( ( 3, 2, 2, 2, 2, 2, 2, 2, 2, 2, 2, 2, 2, 2, 2, 2, 2, 2, 2, 2, 2, 2, 2, 2, 2, 2, 2, 2, 2, 2, 2, 2, 2, 2, 2, 2, 2, 2, 2, 2, 2, 2, 2, 2, 2, 2, 2, 2, 2, 2, 2, 2, 2, 2, 2, 2, 2, 2, 2, 2, 2, 2, 2, 2, 2, 2, 2, 2, 2, 2, 2, 2, 2, 2, 2, 2, 2, 2, 2, 2, 2, 2, 2, 2, 2, 2, 2, 2, 2, 2, 2, 2, 2, 2, 2, 2, 2, 2, 2, 2, 2, 2, 2, 2, 2, 2, 2, 2, 2, 2, 2, 2, 2, 2, 2, 2, 2, 2, 2, 2, 2, 2, 2, 2, 2, 2, 2, 2, 2, 2, 2, 2, 2, 2, 2, 2, 2, 2, 2, 2, 2, 2, 2, 2, 2, 2, 2, 2, 2, 2, 2, 2, 2, 2, 3 ),
 ( 0.008536090408176065514, 0.01250000000000000069, 0.01874999999999999931, 0.02500000000000000139, 0.03125000000000000000, 0.03749999999999999861, 0.04374999999999999722, 0.05000000000000000278, 0.05625000000000000139, 0.06250000000000000000, 0.06875000000000000555, 0.07500000000000001110, 0.08125000000000001665, 0.08749999999999999445, 0.09375000000000000000, 0.1000000000000000056, 0.1062500000000000111, 0.1125000000000000167, 0.1187499999999999944, 0.1250000000000000000, 0.1312500000000000056, 0.1375000000000000111, 0.1437499999999999889, 0.1499999999999999944, 0.1562500000000000000, 0.1625000000000000056, 0.1687500000000000111, 0.1749999999999999889, 0.1812499999999999944, 0.1875000000000000000, 0.1937500000000000056, 0.2000000000000000111, 0.2062499999999999889, 0.2124999999999999944, 0.2187500000000000000, 0.2250000000000000056, 0.2312500000000000111, 0.2374999999999999889, 0.2437499999999999944, 0.2500000000000000000, 0.2562499999999999778, 0.2625000000000000111, 0.2687499999999999889, 0.2750000000000000222, 0.2812500000000000000, 0.2874999999999999778, 0.2937500000000000111, 0.2999999999999999889, 0.3062500000000000222, 0.3124999999999999445, 0.3187499999999999778, 0.3250000000000000111, 0.3312499999999999889, 0.3375000000000000222, 0.3437500000000000000, 0.3499999999999999778, 0.3562500000000000111, 0.3624999999999999889, 0.3687500000000000222, 0.3750000000000000000, 0.3812499999999999778, 0.3875000000000000111, 0.3937499999999999889, 0.4000000000000000222, 0.4062500000000000000, 0.4124999999999999778, 0.4187500000000000111, 0.4249999999999999889, 0.4312500000000000222, 0.4375000000000000000, 0.4437500000000000333, 0.4500000000000000111, 0.4562499999999999889, 0.4625000000000000222, 0.4687500000000000000, 0.4749999999999999778, 0.4812500000000000111, 0.4874999999999999889, 0.4937500000000000222, 0.5000000000000000000, 0.5062499999999999778, 0.5124999999999999556, 0.5187500000000000444, 0.5250000000000000222, 0.5312500000000000000, 0.5374999999999999778, 0.5437499999999999556, 0.5500000000000000444, 0.5562500000000000222, 0.5625000000000000000, 0.5687499999999999778, 0.5749999999999999556, 0.5812500000000000444, 0.5875000000000000222, 0.5937500000000000000, 0.5999999999999999778, 0.6062499999999999556, 0.6125000000000000444, 0.6187500000000000222, 0.6250000000000000000, 0.6312499999999999778, 0.6374999999999999556, 0.6437500000000000444, 0.6500000000000000222, 0.6562500000000000000, 0.6624999999999999778, 0.6687499999999999556, 0.6750000000000000444, 0.6812500000000000222, 0.6875000000000000000, 0.6937500000000000888, 0.6999999999999999556, 0.7062500000000000444, 0.7125000000000000222, 0.7187500000000000000, 0.7249999999999999778, 0.7312499999999999556, 0.7375000000000000444, 0.7437500000000000222, 0.7500000000000000000, 0.7562499999999999778, 0.7624999999999999556, 0.7687500000000000444, 0.7750000000000000222, 0.7812500000000000000, 0.7874999999999999778, 0.7937499999999999556, 0.7999999999999999334, 0.8062500000000000222, 0.8125000000000000000, 0.8187499999999999778, 0.8249999999999999556, 0.8312500000000000444, 0.8375000000000000222, 0.8437500000000000000, 0.8499999999999999778, 0.8562499999999999556, 0.8625000000000000444, 0.8687500000000000222, 0.8750000000000000000, 0.8812499999999999778, 0.8874999999999999556, 0.8937500000000000444, 0.9000000000000000222, 0.9062500000000000000, 0.9124999999999999778, 0.9187499999999999556, 0.9250000000000000444, 0.9312500000000000222, 0.9375000000000000000, 0.9437499999999999778, 0.9499999999999999556, 0.9562500000000000444, 0.9625000000000000222, 0.9687500000000000000 ),
 .UNSPECIFIED. ) 
 CURVE ( )  GEOMETRIC_REPRESENTATION_ITEM ( )  RATIONAL_B_SPLINE_CURVE ( ( 0.9772918381245772057, 0.9689587928776128845, 1.000000000000000000, 0.9510565162951535312, 1.000000000000000000, 0.9510565162951535312, 1.000000000000000000, 0.9510565162951535312, 1.000000000000000000, 0.9510565162951535312, 1.000000000000000000, 0.9510565162951535312, 1.000000000000000000, 0.9510565162951535312, 1.000000000000000000, 0.9510565162951535312, 1.000000000000000000, 0.9510565162951535312, 1.000000000000000000, 0.9510565162951535312, 1.000000000000000000, 0.9510565162951535312, 1.000000000000000000, 0.9510565162951535312, 1.000000000000000000, 0.9510565162951535312, 1.000000000000000000, 0.9510565162951535312, 1.000000000000000000, 0.9510565162951535312, 1.000000000000000000, 0.9510565162951535312, 1.000000000000000000, 0.9510565162951535312, 1.000000000000000000, 0.9510565162951535312, 1.000000000000000000, 0.9510565162951535312, 1.000000000000000000, 0.9510565162951535312, 1.000000000000000000, 0.9510565162951535312, 1.000000000000000000, 0.9510565162951535312, 1.000000000000000000, 0.9510565162951535312, 1.000000000000000000, 0.9510565162951535312, 1.000000000000000000, 0.9510565162951535312, 1.000000000000000000, 0.9510565162951535312, 1.000000000000000000, 0.9510565162951535312, 1.000000000000000000, 0.9510565162951535312, 1.000000000000000000, 0.9510565162951535312, 1.000000000000000000, 0.9510565162951535312, 1.000000000000000000, 0.9510565162951535312, 1.000000000000000000, 0.9510565162951535312, 1.000000000000000000, 0.9510565162951535312, 1.000000000000000000, 0.9510565162951535312, 1.000000000000000000, 0.9510565162951535312, 1.000000000000000000, 0.9510565162951535312, 1.000000000000000000, 0.9510565162951535312, 1.000000000000000000, 0.9510565162951535312, 1.000000000000000000, 0.9510565162951535312, 1.000000000000000000, 0.9510565162951535312, 1.000000000000000000, 0.9510565162951535312, 1.000000000000000000, 0.9510565162951535312, 1.000000000000000000, 0.9510565162951535312, 1.000000000000000000, 0.9510565162951535312, 1.000000000000000000, 0.9510565162951535312, 1.000000000000000000, 0.9510565162951535312, 1.000000000000000000, 0.9510565162951535312, 1.000000000000000000, 0.9510565162951535312, 1.000000000000000000, 0.9510565162951535312, 1.000000000000000000, 0.9510565162951535312, 1.000000000000000000, 0.9510565162951535312, 1.000000000000000000, 0.9510565162951535312, 1.000000000000000000, 0.9510565162951535312, 1.000000000000000000, 0.9510565162951535312, 1.000000000000000000, 0.9510565162951535312, 1.000000000000000000, 0.9510565162951535312, 1.000000000000000000, 0.9510565162951535312, 1.000000000000000000, 0.9510565162951535312, 1.000000000000000000, 0.9510565162951535312, 1.000000000000000000, 0.9510565162951535312, 1.000000000000000000, 0.9510565162951535312, 1.000000000000000000, 0.9510565162951535312, 1.000000000000000000, 0.9510565162951535312, 1.000000000000000000, 0.9510565162951535312, 1.000000000000000000, 0.9510565162951535312, 1.000000000000000000, 0.9510565162951535312, 1.000000000000000000, 0.9510565162951535312, 1.000000000000000000, 0.9510565162951535312, 1.000000000000000000, 0.9510565162951535312, 1.000000000000000000, 0.9510565162951535312, 1.000000000000000000, 0.9510565162951535312, 1.000000000000000000, 0.9510565162951535312, 1.000000000000000000, 0.9510565162951535312, 1.000000000000000000, 0.9510565162951535312, 1.000000000000000000, 0.9510565162951535312, 1.000000000000000000, 0.9510565162951535312, 1.000000000000000000, 0.9510565162951535312, 1.000000000000000000, 0.9510565162951535312, 1.000000000000000000, 0.9510565162951535312, 1.000000000000000000, 0.9510565162951535312, 1.000000000000000000, 0.9510565162951535312, 1.000000000000000000, 0.9510565162951535312, 1.000000000000000000, 0.9510565162951535312, 1.000000000000000000, 0.9510565162951535312, 1.000000000000000000, 0.9510565162951535312, 1.000000000000000000, 0.9510565162951535312, 1.000000000000000000, 0.9510565162951535312, 1.000000000000000000, 0.9510565162951535312, 1.000000000000000000, 0.9510565162951535312, 1.000000000000000000, 0.9510565162951535312, 1.000000000000000000, 0.9510565162951535312, 1.000000000000000000, 0.9510565162951535312, 1.000000000000000000, 0.9510565162951535312, 1.000000000000000000, 0.9510565162951535312, 1.000000000000000000, 0.9510565162951535312, 1.000000000000000000, 0.9510565162951535312, 1.000000000000000000, 0.9510565162951535312, 1.000000000000000000, 0.9510565162951535312, 1.000000000000000000, 0.9510565162951535312, 1.000000000000000000, 0.9510565162951535312, 1.000000000000000000, 0.9510565162951535312, 1.000000000000000000, 0.9510565162951535312, 1.000000000000000000, 0.9510565162951535312, 1.000000000000000000, 0.9510565162951535312, 1.000000000000000000, 0.9510565162951535312, 1.000000000000000000, 0.9510565162951535312, 1.000000000000000000, 0.9510565162951535312, 1.000000000000000000, 0.9510565162951535312, 1.000000000000000000, 0.9510565162951535312, 1.000000000000000000, 0.9510565162951535312, 1.000000000000000000, 0.9510565162951535312, 1.000000000000000000, 0.9510565162951535312, 1.000000000000000000, 0.9510565162951535312, 1.000000000000000000, 0.9510565162951535312, 1.000000000000000000, 0.9510565162951535312, 1.000000000000000000, 0.9510565162951535312, 1.000000000000000000, 0.9510565162951535312, 1.000000000000000000, 0.9510565162951535312, 1.000000000000000000, 0.9510565162951535312, 1.000000000000000000, 0.9510565162951535312, 1.000000000000000000, 0.9510565162951535312, 1.000000000000000000, 0.9510565162951535312, 1.000000000000000000, 0.9510565162951535312, 1.000000000000000000, 0.9510565162951535312, 1.000000000000000000, 0.9510565162951535312, 1.000000000000000000, 0.9510565162951535312, 1.000000000000000000, 0.9510565162951535312, 1.000000000000000000, 0.9510565162951535312, 1.000000000000000000, 0.9510565162951535312, 1.000000000000000000, 0.9510565162951535312, 1.000000000000000000, 0.9510565162951535312, 1.000000000000000000, 0.9510565162951535312, 1.000000000000000000, 0.9510565162951535312, 1.000000000000000000, 0.9510565162951535312, 1.000000000000000000, 0.9510565162951535312, 1.000000000000000000, 0.9510565162951535312, 1.000000000000000000, 0.9510565162951535312, 1.000000000000000000, 0.9510565162951535312, 1.000000000000000000, 0.9510565162951535312, 1.000000000000000000, 0.9510565162951535312, 1.000000000000000000, 0.9510565162951535312, 1.000000000000000000, 0.9510565162951535312, 1.000000000000000000, 0.9510565162951535312, 1.000000000000000000, 0.9510565162951535312, 1.000000000000000000, 0.9510565162951535312, 1.000000000000000000, 0.9510565162951535312, 1.000000000000000000, 0.9510565162951535312, 1.000000000000000000, 0.9510565162951535312, 1.000000000000000000, 0.9510565162951535312, 1.000000000000000000, 0.9510565162951535312, 1.000000000000000000, 0.9510565162951535312, 1.000000000000000000, 0.9510565162951535312, 1.000000000000000000, 0.9510565162951535312, 1.000000000000000000, 0.9510565162951535312, 1.000000000000000000 ) ) 
 REPRESENTATION_ITEM ( '' )  );
#22592=CARTESIAN_POINT ( 'NONE',  ( 37.80618814713140097, -21.91368208888610880, 73.13360434286903455 ) ) ;
#22597=CARTESIAN_POINT ( 'NONE',  ( 39.02742774030102879, -2.213682088886101518, 72.26730301774236409 ) ) ;
#22599=CARTESIAN_POINT ( 'NONE',  ( 38.63098279924290068, -28.70384086642190979, 72.53360434286901182 ) ) ;
#22605=CARTESIAN_POINT ( 'NONE',  ( 36.68196826583682935, -4.003840866421911393, 70.79240656858108593 ) ) ;
#22614=CARTESIAN_POINT ( 'NONE',  ( 39.38009889167650357, 1.786317911113891821, 72.75271321436734695 ) ) ;
#22631=CARTESIAN_POINT ( 'NONE',  ( 38.73920764526925353, -16.11368208888610454, 72.49843995877330372 ) ) ;
#22635=CARTESIAN_POINT ( 'NONE',  ( 39.98359781491296161, -4.413682088886105248, 71.86517103874048473 ) ) ;
#22636=CARTESIAN_POINT ( 'NONE',  ( 39.29254315202757653, -22.80384086642191477, 72.81632618279321889 ) ) ;
#22641=CARTESIAN_POINT ( 'NONE',  ( 39.02088643472237095, -8.913682088886103472, 69.02690120949094421 ) ) ;
#22658=UNCERTAINTY_MEASURE_WITH_UNIT (LENGTH_MEASURE( 1.000000000000000082E-05 ), #18674, 'distance_accuracy_value', 'NONE');
#22660=CARTESIAN_POINT ( 'NONE',  ( 40.55423172469004101, -15.20384086642191512, 70.70992431699450265 ) ) ;
#22661=CARTESIAN_POINT ( 'NONE',  ( 39.29254315202756231, -18.81368208888610027, 69.94417936956672577 ) ) ;
#22667=CARTESIAN_POINT ( 'NONE',  ( 40.33642880535524000, -26.31368208888610383, 72.77780686321125359 ) ) ;
#22671=CARTESIAN_POINT ( 'NONE',  ( 36.68196826583682935, -1.613682088886104982, 71.96809898377890136 ) ) ;
#22673=CARTESIAN_POINT ( 'NONE',  ( 38.82593461698262871, -20.91368208888609814, 69.62690120949091011 ) ) ;
#22677=CARTESIAN_POINT ( 'NONE',  ( 37.12184278917507640, -18.10384086642191193, 71.32335560751961623 ) ) ;
#22678=CARTESIAN_POINT ( 'NONE',  ( 39.29254315202756231, -8.813682088886100274, 69.94417936956673998 ) ) ;
#22683=CARTESIAN_POINT ( 'NONE',  ( 39.82603832034400426, -7.303840866421906775, 70.35351908239857721 ) ) ;
#22685=CARTESIAN_POINT ( 'NONE',  ( 39.95015449827720744, -2.613682088886105870, 70.79240656858107172 ) ) ;
#22687=CARTESIAN_POINT ( 'NONE',  ( 40.26954217208371034, -8.713682088886100630, 69.89063713639259845 ) ) ;
#22690=CARTESIAN_POINT ( 'NONE',  ( 37.38336156205273397, -9.903840866421909084, 70.63227792289248441 ) ) ;
#22696=CARTESIAN_POINT ( 'NONE',  ( 39.12911128074872380, -13.50384086642191228, 69.06206559358665231 ) ) ;
#22699=CARTESIAN_POINT ( 'NONE',  ( 36.49096545463212493, -23.51368208888609601, 71.43714994484030001 ) ) ;
#22706=CARTESIAN_POINT ( 'NONE',  ( 39.95015449827720744, -7.003840866421910505, 71.96809898377888715 ) ) ;
#22710=CARTESIAN_POINT ( 'NONE',  ( 39.29254315202756231, -22.81368208888610027, 69.94417936956672577 ) ) ;
#22715=CARTESIAN_POINT ( 'NONE',  ( 39.75915168707251723, -26.90384086642191619, 72.49904802271737481 ) ) ;
#22717=CARTESIAN_POINT ( 'NONE',  ( 39.38009889167650357, -26.21368208888610951, 72.75271321436730432 ) ) ;
#22722=CARTESIAN_POINT ( 'NONE',  ( 37.89291511884479036, -28.50384086642191406, 72.49843995877328950 ) ) ;
#22723=CARTESIAN_POINT ( 'NONE',  ( 39.31564783533280405, 1.686317911113899282, 72.03616607671141026 ) ) ;
#22729=CARTESIAN_POINT ( 'NONE',  ( 36.87297107704149823, -3.903840866421907752, 70.26145752964255564 ) ) ;
#22737=CARTESIAN_POINT ( 'NONE',  ( 36.64852494920107517, -3.413682088886104360, 70.89533451361948835 ) ) ;
#22755=CARTESIAN_POINT ( 'NONE',  ( 39.24876120206128860, -14.71368208888610241, 70.63227792289245599 ) ) ;
#22761=CARTESIAN_POINT ( 'NONE',  ( 37.80618814713140097, -1.913682088886106136, 73.13360434286904876 ) ) ;
#22762=CARTESIAN_POINT ( 'NONE',  ( 36.64852494920107517, -22.20384086642191335, 71.86517103874048473 ) ) ;
#22764=CARTESIAN_POINT ( 'NONE',  ( 36.11133435605973574, -7.613682088886103649, 72.15350918040385864 ) ) ;
#22786=CARTESIAN_POINT ( 'NONE',  ( 36.98690846071097127, -19.80384086642191477, 69.45876917294175712 ) ) ;
#22790=CARTESIAN_POINT ( 'NONE',  ( 37.69796330110504101, -23.11368208888609743, 69.66206559358660400 ) ) ;
#22796=CARTESIAN_POINT ( 'NONE',  ( 40.26954217208372455, 1.096159133578081812, 72.86986841596736042 ) ) ;
#22800=CARTESIAN_POINT ( 'NONE',  ( 39.75915168707250302, -0.7136820888860997414, 70.26145752964252722 ) ) ;
#22802=CARTESIAN_POINT ( 'NONE',  ( 39.38009889167650357, -20.21368208888610951, 72.75271321436731853 ) ) ;
#22808=CARTESIAN_POINT ( 'NONE',  ( 38.93987200065210175, -18.80384086642191122, 72.33091598616826445 ) ) ;
#22809=CARTESIAN_POINT ( 'NONE',  ( 39.38009889167650357, -6.213682088886108623, 72.75271321436733274 ) ) ;
#22814=CARTESIAN_POINT ( 'NONE',  ( 39.95015449827720744, -7.003840866421910505, 71.96809898377888715 ) ) ;
#22817=CARTESIAN_POINT ( 'NONE',  ( 37.33957961208646736, 0.1863179111138910105, 72.81632618279323310 ) ) ;
#22819=CARTESIAN_POINT ( 'NONE',  ( 39.64521430340304420, -8.813682088886096722, 69.45876917294177133 ) ) ;
#22823=CARTESIAN_POINT ( 'NONE',  ( 37.60469502381300799, -12.40384086642191441, 72.26730301774234988 ) ) ;
#22828=CARTESIAN_POINT ( 'NONE',  ( 35.86008812008917346, -18.10384086642191548, 71.32335560751961623 ) ) ;
#22830=CARTESIAN_POINT ( 'NONE',  ( 39.29254315202756231, -22.81368208888610027, 69.94417936956672577 ) ) ;
#22837=CARTESIAN_POINT ( 'NONE',  ( 40.14115730948191185, -11.10384086642191015, 71.43714994484034264 ) ) ;
#22841=CARTESIAN_POINT ( 'NONE',  ( 37.80618814713140097, -25.91368208888610880, 73.13360434286902034 ) ) ;
#22843=CARTESIAN_POINT ( 'NONE',  ( 36.49096545463212493, -24.10384086642190482, 71.32335560751960202 ) ) ;
#22845=CARTESIAN_POINT ( 'NONE',  ( 38.82593461698262871, -26.91368208888610170, 69.62690120949091011 ) ) ;
#22850=CARTESIAN_POINT ( 'NONE',  ( 37.38336156205274818, 0.2863179111139008137, 72.12822762946751709 ) ) ;
#22857=CARTESIAN_POINT ( 'NONE',  ( 36.68196826583682935, -2.003840866421909617, 70.79240656858108593 ) ) ;
#22867=CARTESIAN_POINT ( 'NONE',  ( 37.25202387243752611, -1.213682088886100630, 70.00779233799264034 ) ) ;
#22868=CARTESIAN_POINT ( 'NONE',  ( 38.26194895904384907, -28.60384086642191548, 73.11602215082115208 ) ) ;
#22883=CARTESIAN_POINT ( 'NONE',  ( 37.25260217561390874, -17.61368208888609743, 71.78268878715392987 ) ) ;
#22887=CARTESIAN_POINT ( 'NONE',  ( 38.26194895904383486, 0.9863179111138999922, 69.64448340153880679 ) ) ;
#22888=CARTESIAN_POINT ( 'NONE',  ( 38.82593461698265003, -20.70384086642191335, 73.13360434286903455 ) ) ;
#22890=CARTESIAN_POINT ( 'NONE',  ( 35.86008812008917346, -3.513682088886104005, 71.43714994484035685 ) ) ;
#22907=CARTESIAN_POINT ( 'NONE',  ( 36.07789103942399578, -8.203840866421915123, 72.05058123536544201 ) ) ;
#22909=CARTESIAN_POINT ( 'NONE',  ( 36.80608444377001121, -23.31368208888610383, 70.35351908239857721 ) ) ;
#22910=( NAMED_UNIT ( * ) PLANE_ANGLE_UNIT ( ) SI_UNIT ( $, .RADIAN. ) );
#22914=CARTESIAN_POINT ( 'NONE',  ( 40.55423172469004811, -20.41368208888610880, 72.05058123536544201 ) ) ;
#22919=CARTESIAN_POINT ( 'NONE',  ( 38.37017380507020192, -4.013682088886107557, 73.11602215082118050 ) ) ;
#22921=CARTESIAN_POINT ( 'NONE',  ( 39.95015449827720744, -14.61368208888610454, 70.79240656858105751 ) ) ;
#22925=CARTESIAN_POINT ( 'NONE',  ( 39.31564783533279694, -21.30384086642190766, 70.72433947564853440 ) ) ;
#22926=CARTESIAN_POINT ( 'NONE',  ( 39.95015449827720744, -8.613682088886104538, 70.79240656858107172 ) ) ;
#22931=CARTESIAN_POINT ( 'NONE',  ( 39.98359781491296161, -5.203840866421911571, 70.89533451361947414 ) ) ;
#22935=CARTESIAN_POINT ( 'NONE',  ( 40.14115730948191185, 1.486317911113896884, 71.32335560751963044 ) ) ;
#22937=CARTESIAN_POINT ( 'NONE',  ( 40.77203464402485622, -6.513682088886103116, 71.32335560751961623 ) ) ;
#22940=CARTESIAN_POINT ( 'NONE',  ( 39.02742774030101458, -5.403840866421909972, 70.49320253461759478 ) ) ;
#22947=CARTESIAN_POINT ( 'NONE',  ( 39.02088643472237806, -18.70384086642192045, 73.73360434286898624 ) ) ;
#22952=SURFACE_SIDE_STYLE ('',( #3373 ) ) ;
#22953=CARTESIAN_POINT ( 'NONE',  ( 38.37017380507020192, -18.01368208888611022, 73.11602215082116629 ) ) ;
#22962=CARTESIAN_POINT ( 'NONE',  ( 36.64852494920107517, -8.203840866421909794, 71.86517103874049894 ) ) ;
#22965=CARTESIAN_POINT ( 'NONE',  ( 37.33957961208646736, -25.81368208888610738, 72.81632618279320468 ) ) ;
#22967=CARTESIAN_POINT ( 'NONE',  ( 36.49096545463212493, -26.10384086642190482, 71.32335560751960202 ) ) ;
#22969=CARTESIAN_POINT ( 'NONE',  ( 37.25202387243752611, -17.21368208888610241, 70.00779233799262613 ) ) ;
#22971=CARTESIAN_POINT ( 'NONE',  ( 36.98690846071097837, -25.81368208888611093, 73.30173637941817333 ) ) ;
#22975=CARTESIAN_POINT ( 'NONE',  ( 38.37017380507020192, 1.986317911113897550, 72.51602215082118619 ) ) ;
#22982=CARTESIAN_POINT ( 'NONE',  ( 40.14115730948191185, -3.103840866421910150, 71.43714994484034264 ) ) ;
#22989=CARTESIAN_POINT ( 'NONE',  ( 38.26194895904383486, 0.9863179111138999922, 69.64448340153880679 ) ) ;
#22991=CARTESIAN_POINT ( 'NONE',  ( 39.29254315202757653, -28.80384086642191832, 72.81632618279320468 ) ) ;
#23008=CARTESIAN_POINT ( 'NONE',  ( 37.21915885897815457, -19.41368208888609814, 71.08074471024443142 ) ) ;
#23013=CARTESIAN_POINT ( 'NONE',  ( 37.33957961208645315, -23.80384086642191122, 69.94417936956671156 ) ) ;
#23032=CARTESIAN_POINT ( 'NONE',  ( 36.36258059203030513, -13.90384086642191264, 69.89063713639259845 ) ) ;
#23036=CARTESIAN_POINT ( 'NONE',  ( 36.87297107704152666, -13.71368208888610773, 72.49904802271740323 ) ) ;
#23042=CARTESIAN_POINT ( 'NONE',  ( 36.07789103942398867, -19.41368208888610525, 70.70992431699450265 ) ) ;
#23051=CARTESIAN_POINT ( 'NONE',  ( 38.26194895904384197, -12.60384086642191015, 72.51602215082118619 ) ) ;
#23052=CARTESIAN_POINT ( 'NONE',  ( 36.80608444377001121, 0.6863179111138983934, 70.35351908239860563 ) ) ;
#23058=CARTESIAN_POINT ( 'NONE',  ( 37.80618814713138676, 0.2961591335780937584, 69.62690120949091011 ) ) ;
#23059=CARTESIAN_POINT ( 'NONE',  ( 38.26194895904383486, -29.01368208888610312, 70.24448340153875847 ) ) ;
#23061=CARTESIAN_POINT ( 'NONE',  ( 37.61123632939165873, -11.91368208888610880, 73.73360434286898624 ) ) ;
#23064=CARTESIAN_POINT ( 'NONE',  ( 38.63098279924290068, -6.703840866421912459, 72.53360434286905445 ) ) ;
#23070=CARTESIAN_POINT ( 'NONE',  ( 38.26194895904384197, -10.60384086642192081, 73.71602215082116061 ) ) ;
#23074=CARTESIAN_POINT ( 'NONE',  ( 37.80618814713140097, -13.91368208888610347, 73.13360434286903455 ) ) ;
#23079=CARTESIAN_POINT ( 'NONE',  ( 38.93415946300897446, -11.50384086642190518, 69.66206559358664663 ) ) ;
#23083=CARTESIAN_POINT ( 'NONE',  ( 39.29254315202756231, -24.81368208888610383, 69.94417936956671156 ) ) ;
#23089=CARTESIAN_POINT ( 'NONE',  ( 36.80608444377001831, -20.30384086642191477, 72.40698646996135324 ) ) ;
#23093=CARTESIAN_POINT ( 'NONE',  ( 36.68196826583682935, -17.61368208888610454, 71.96809898377888715 ) ) ;
#23095=CARTESIAN_POINT ( 'NONE',  ( 36.89935272106205133, -0.4038408664219194089, 73.23812341099225875 ) ) ;
#23099=CARTESIAN_POINT ( 'NONE',  ( 39.31564783533279694, -23.30384086642191477, 70.72433947564853440 ) ) ;
#23105=CARTESIAN_POINT ( 'NONE',  ( 39.12911128074872380, -27.50384086642191406, 69.06206559358663810 ) ) ;
#23114=CARTESIAN_POINT ( 'NONE',  ( 38.82593461698264292, -26.70384086642191335, 73.13360434286902034 ) ) ;
#23128=CARTESIAN_POINT ( 'NONE',  ( 37.25260217561390874, -9.613682088886102761, 71.78268878715394408 ) ) ;
#23129=CARTESIAN_POINT ( 'NONE',  ( 38.00113996487114321, -11.91368208888610170, 72.53360434286904024 ) ) ;
#23135=CARTESIAN_POINT ( 'NONE',  ( 38.93415946300896024, -21.50384086642190340, 69.66206559358661821 ) ) ;
#23139=CARTESIAN_POINT ( 'NONE',  ( 39.41296390513587511, -16.41368208888610525, 71.67976084211551324 ) ) ;
#23156=CARTESIAN_POINT ( 'NONE',  ( 40.33642880535521869, -13.30384086642190944, 69.98269868914866265 ) ) ;
#23158=CARTESIAN_POINT ( 'NONE',  ( 39.95015449827720744, -12.61368208888610454, 70.79240656858105751 ) ) ;
#23164=CARTESIAN_POINT ( 'NONE',  ( 39.12911128074873801, -22.11368208888610809, 73.69843995877327814 ) ) ;
#23173=MECHANICAL_DESIGN_GEOMETRIC_PRESENTATION_REPRESENTATION('',(#5508),#4671);
#23177=CARTESIAN_POINT ( 'NONE',  ( 37.38336156205273397, -11.90384086642191441, 70.63227792289247020 ) ) ;
#23178=CARTESIAN_POINT ( 'NONE',  ( 40.14115730948191185, -2.513682088886103116, 71.32335560751961623 ) ) ;
#23186=CARTESIAN_POINT ( 'NONE',  ( 39.38009889167648936, -1.403840866421906419, 70.00779233799264034 ) ) ;
#23187=CARTESIAN_POINT ( 'NONE',  ( 38.82593461698262871, 1.086317911113899637, 69.62690120949091011 ) ) ;
#23188=CARTESIAN_POINT ( 'NONE',  ( 39.64521430340304420, -2.813682088886101162, 69.45876917294177133 ) ) ;
#23191=CARTESIAN_POINT ( 'NONE',  ( 39.51027997493896748, -3.103840866421909706, 71.43714994484034264 ) ) ;
#23196=CARTESIAN_POINT ( 'NONE',  ( 37.50301148336529877, -10.50384086642191761, 73.69843995877330656 ) ) ;
#23200=CARTESIAN_POINT ( 'NONE',  ( 37.33957961208646736, -13.81368208888610916, 72.81632618279321889 ) ) ;
#23206=CARTESIAN_POINT ( 'NONE',  ( 38.37017380507018771, -7.603840866421906597, 69.64448340153879258 ) ) ;
#23209=CARTESIAN_POINT ( 'NONE',  ( 37.80618814713140097, -15.91368208888610880, 73.13360434286903455 ) ) ;
#23214=CARTESIAN_POINT ( 'NONE',  ( 36.49096545463212493, -20.10384086642191193, 71.32335560751961623 ) ) ;
#23216=CARTESIAN_POINT ( 'NONE',  ( 39.95015449827720744, -20.61368208888610454, 70.79240656858105751 ) ) ;
#23218=CARTESIAN_POINT ( 'NONE',  ( 38.26194895904383486, -25.01368208888610312, 69.04448340153878405 ) ) ;
#23223=CARTESIAN_POINT ( 'NONE',  ( 39.02742774030101458, -27.40384086642191619, 70.49320253461758057 ) ) ;
#23230=CARTESIAN_POINT ( 'NONE',  ( 39.98359781491296161, -1.203840866421911127, 70.89533451361947414 ) ) ;
#23241=CARTESIAN_POINT ( 'NONE',  ( 39.98359781491296161, -27.20384086642191335, 70.89533451361944572 ) ) ;
#23249=CARTESIAN_POINT ( 'NONE',  ( 37.38336156205273397, -7.903840866421910860, 70.63227792289248441 ) ) ;
#23256=CARTESIAN_POINT ( 'NONE',  ( 38.26194895904383486, -15.01368208888610134, 70.24448340153875847 ) ) ;
#23257=CARTESIAN_POINT ( 'NONE',  ( 37.38336156205274818, -9.713682088886098853, 72.12822762946751709 ) ) ;
#23263=CARTESIAN_POINT ( 'NONE',  ( 39.29254315202756231, 1.186317911113898838, 69.94417936956675419 ) ) ;
#23264=CARTESIAN_POINT ( 'NONE',  ( 40.14115730948191185, -17.10384086642191193, 71.43714994484030001 ) ) ;
#23268=CARTESIAN_POINT ( 'NONE',  ( 37.31647492878122563, -21.31368208888610027, 70.72433947564853440 ) ) ;
#23285=CARTESIAN_POINT ( 'NONE',  ( 39.73277004305197124, -9.403840866421907307, 69.52238214136768590 ) ) ;
#23287=CARTESIAN_POINT ( 'NONE',  ( 39.82603832034400426, -14.31368208888610916, 72.40698646996133903 ) ) ;
#23291=CARTESIAN_POINT ( 'NONE',  ( 40.77203464402485622, -20.51368208888610667, 71.32335560751960202 ) ) ;
#23297=CARTESIAN_POINT ( 'NONE',  ( 39.31564783533279694, -11.30384086642191299, 70.72433947564853440 ) ) ;
#23298=CARTESIAN_POINT ( 'NONE',  ( 39.37952058850012804, -28.61368208888610454, 70.97781676520600058 ) ) ;
#23305=CARTESIAN_POINT ( 'NONE',  ( 40.33642880535521869, -27.30384086642191477, 69.98269868914864844 ) ) ;
#23308=CARTESIAN_POINT ( 'NONE',  ( 38.93415946300897446, -0.1136820888861071466, 73.09843995877331224 ) ) ;
#23309=CARTESIAN_POINT ( 'NONE',  ( 35.86008812008917346, -1.513682088886105781, 71.43714994484035685 ) ) ;
#23313=CARTESIAN_POINT ( 'NONE',  ( 39.51027997493896748, -7.103840866421911038, 71.43714994484034264 ) ) ;
#23320=CARTESIAN_POINT ( 'NONE',  ( 35.86008812008917346, -10.10384086642191548, 71.32335560751961623 ) ) ;
#23322=CARTESIAN_POINT ( 'NONE',  ( 37.80618814713140097, -11.91368208888611058, 73.13360434286903455 ) ) ;
#23328=CARTESIAN_POINT ( 'NONE',  ( 39.82603832034401137, -1.303840866421906775, 70.35351908239860563 ) ) ;
#23332=CARTESIAN_POINT ( 'NONE',  ( 38.37017380507020192, -20.01368208888610667, 73.11602215082116629 ) ) ;
#23337=CARTESIAN_POINT ( 'NONE',  ( 36.80608444377001831, -18.30384086642190766, 72.40698646996135324 ) ) ;
#23340=CARTESIAN_POINT ( 'NONE',  ( 38.26194895904383486, -19.01368208888610312, 69.64448340153877837 ) ) ;
#23342=CARTESIAN_POINT ( 'NONE',  ( 39.73277004305198545, -20.21368208888611306, 73.23812341099225875 ) ) ;
#23346=CARTESIAN_POINT ( 'NONE',  ( 38.37017380507018771, -21.60384086642191548, 70.24448340153875847 ) ) ;
#23352=CARTESIAN_POINT ( 'NONE',  ( 40.52078840805429394, -29.00384086642191406, 72.15350918040381600 ) ) ;
#23356=CARTESIAN_POINT ( 'NONE',  ( 39.12911128074873801, -4.113682088886107202, 73.69843995877330656 ) ) ;
#23364=CARTESIAN_POINT ( 'NONE',  ( 38.37017380507018771, -25.60384086642190837, 69.64448340153876416 ) ) ;
#23371=CARTESIAN_POINT ( 'NONE',  ( 39.51027997493896748, -5.103840866421911926, 71.43714994484034264 ) ) ;
#23378=CARTESIAN_POINT ( 'NONE',  ( 38.63098279924288647, -12.91368208888610525, 70.22690120949090442 ) ) ;
#23379=CARTESIAN_POINT ( 'NONE',  ( 38.26194895904383486, -9.013682088886101340, 70.24448340153877268 ) ) ;
#23385=CARTESIAN_POINT ( 'NONE',  ( 39.82603832034400426, -17.30384086642190056, 70.35351908239857721 ) ) ;
#23389=CARTESIAN_POINT ( 'NONE',  ( 38.26194895904383486, -21.01368208888610312, 70.24448340153875847 ) ) ;
#23393=CARTESIAN_POINT ( 'NONE',  ( 36.68196826583682935, -11.61368208888610276, 71.96809898377888715 ) ) ;
#23408=CARTESIAN_POINT ( 'NONE',  ( 37.50301148336529877, -12.50384086642191939, 73.69843995877327814 ) ) ;
#23414=CARTESIAN_POINT ( 'NONE',  ( 36.87297107704152666, -11.71368208888611129, 72.49904802271740323 ) ) ;
#23421=CARTESIAN_POINT ( 'NONE',  ( 39.64521430340304420, -20.81368208888610027, 69.45876917294175712 ) ) ;
#23435=CARTESIAN_POINT ( 'NONE',  ( 37.60469502381300799, -12.40384086642191441, 72.26730301774234988 ) ) ;
#23436=CARTESIAN_POINT ( 'NONE',  ( 38.37017380507020192, -2.013682088886109334, 73.11602215082118050 ) ) ;
#23443=CARTESIAN_POINT ( 'NONE',  ( 38.26194895904384907, 1.396159133578083633, 73.11602215082119471 ) ) ;
#23444=CARTESIAN_POINT ( 'NONE',  ( 37.69225076346193504, -25.81368208888610027, 72.33091598616823603 ) ) ;
#23445=CARTESIAN_POINT ( 'NONE',  ( 39.02088643472237095, -4.913682088886102584, 69.02690120949094421 ) ) ;
#23449=CARTESIAN_POINT ( 'NONE',  ( 38.37017380507018771, -3.603840866421911038, 70.24448340153877268 ) ) ;
#23453=CARTESIAN_POINT ( 'NONE',  ( 36.98690846071097127, -11.80384086642191477, 69.45876917294175712 ) ) ;
#23456=CARTESIAN_POINT ( 'NONE',  ( 39.98359781491296161, -14.41368208888610525, 71.86517103874047052 ) ) ;
#23463=CARTESIAN_POINT ( 'NONE',  ( 37.80618814713138676, -1.703840866421908018, 69.62690120949091011 ) ) ;
#23465=CARTESIAN_POINT ( 'NONE',  ( 39.98359781491296161, -20.41368208888610525, 71.86517103874047052 ) ) ;
#23467=CARTESIAN_POINT ( 'NONE',  ( 38.26194895904384907, -16.60384086642191548, 73.11602215082116629 ) ) ;
#23470=CARTESIAN_POINT ( 'NONE',  ( 38.93415946300897446, -16.11368208888611164, 73.09843995877329803 ) ) ;
#23472=CARTESIAN_POINT ( 'NONE',  ( 36.89935272106204422, -23.21368208888610241, 69.52238214136765748 ) ) ;
#23477=CARTESIAN_POINT ( 'NONE',  ( 37.69225076346193504, -23.80384086642191477, 70.42958956619166599 ) ) ;
#23483=CARTESIAN_POINT ( 'NONE',  ( 40.52078840805429394, -27.00384086642191761, 72.15350918040381600 ) ) ;
#23484=CARTESIAN_POINT ( 'NONE',  ( 37.61123632939165873, 0.08631791111389161553, 73.73360434286902887 ) ) ;
#23493=CARTESIAN_POINT ( 'NONE',  ( 37.80618814713138676, -19.70384086642190624, 69.62690120949091011 ) ) ;
#23500=CARTESIAN_POINT ( 'NONE',  ( 39.41296390513587511, -7.203840866421913347, 71.08074471024443142 ) ) ;
#23507=CARTESIAN_POINT ( 'NONE',  ( 37.89291511884476904, -15.11368208888610098, 70.26206559358661252 ) ) ;
#23508=CARTESIAN_POINT ( 'NONE',  ( 39.24876120206128860, -8.713682088886100630, 70.63227792289247020 ) ) ;
#23515=CARTESIAN_POINT ( 'NONE',  ( 37.69796330110505522, -14.50384086642191583, 73.09843995877329803 ) ) ;
#23518=( GEOMETRIC_REPRESENTATION_CONTEXT ( 3 ) GLOBAL_UNCERTAINTY_ASSIGNED_CONTEXT ( ( #438 ) ) GLOBAL_UNIT_ASSIGNED_CONTEXT ( ( #6854, #13049, #20643 ) ) REPRESENTATION_CONTEXT ( 'NONE', 'WORKASPACE' ) );
#23520=CARTESIAN_POINT ( 'NONE',  ( 37.60469502381300089, -19.21368208888609885, 70.49320253461759478 ) ) ;
#23524=CARTESIAN_POINT ( 'NONE',  ( 38.26194895904383486, -17.01368208888610312, 69.64448340153877837 ) ) ;
#23527=CARTESIAN_POINT ( 'NONE',  ( 38.82593461698262871, -28.91368208888610525, 69.62690120949091011 ) ) ;
#23538=CARTESIAN_POINT ( 'NONE',  ( 37.50301148336529877, -4.503840866421918498, 73.69843995877330656 ) ) ;
#23542=CARTESIAN_POINT ( 'NONE',  ( 36.80608444377001121, -17.31368208888609672, 70.35351908239857721 ) ) ;
#23543=ORIENTED_EDGE ( 'NONE', *, *, #19047, .T. ) ;
#23546=CARTESIAN_POINT ( 'NONE',  ( 39.73277004305198545, -12.21368208888610951, 73.23812341099225875 ) ) ;
#23561=CARTESIAN_POINT ( 'NONE',  ( 39.41296390513587511, -15.20384086642191157, 71.08074471024441721 ) ) ;
#23562=CARTESIAN_POINT ( 'NONE',  ( 38.00113996487114321, -27.91368208888610170, 72.53360434286901182 ) ) ;
#23571=CARTESIAN_POINT ( 'NONE',  ( 39.82603832034400426, 0.6961591335780910050, 70.35351908239860563 ) ) ;
#23573=CARTESIAN_POINT ( 'NONE',  ( 37.38336156205274818, -21.71368208888610241, 72.12822762946750288 ) ) ;
#23574=CARTESIAN_POINT ( 'NONE',  ( 40.55423172469004811, -0.4136820888861054146, 72.05058123536544201 ) ) ;
#23577=CARTESIAN_POINT ( 'NONE',  ( 39.95015449827720744, -27.00384086642191050, 71.96809898377885872 ) ) ;
#23583=CARTESIAN_POINT ( 'NONE',  ( 40.52078840805429394, -11.00384086642191406, 72.15350918040385864 ) ) ;
#23587=CARTESIAN_POINT ( 'NONE',  ( 36.68196826583682935, -13.61368208888610454, 71.96809898377888715 ) ) ;
#23589=CARTESIAN_POINT ( 'NONE',  ( 38.82593461698262871, -24.91368208888610170, 69.62690120949091011 ) ) ;
#23595=CARTESIAN_POINT ( 'NONE',  ( 36.68196826583682935, -2.003840866421909617, 70.79240656858108593 ) ) ;
#23598=CARTESIAN_POINT ( 'NONE',  ( 39.38009889167650357, -20.21368208888610951, 72.75271321436731853 ) ) ;
#23602=CARTESIAN_POINT ( 'NONE',  ( 39.98359781491296161, -17.20384086642190979, 70.89533451361945993 ) ) ;
#23605=CARTESIAN_POINT ( 'NONE',  ( 39.98359781491296161, -10.41368208888610347, 71.86517103874048473 ) ) ;
#23607=CARTESIAN_POINT ( 'NONE',  ( 36.36258059203031934, -23.71368208888610951, 72.86986841596734621 ) ) ;
#23612=CARTESIAN_POINT ( 'NONE',  ( 38.26194895904384197, -24.60384086642190837, 72.51602215082114355 ) ) ;
#23622=CARTESIAN_POINT ( 'NONE',  ( 40.14115730948191185, 0.8961591335780898504, 71.43714994484035685 ) ) ;
#23625=CARTESIAN_POINT ( 'NONE',  ( 40.77203464402485622, -4.513682088886104893, 71.32335560751961623 ) ) ;
#23632=CARTESIAN_POINT ( 'NONE',  ( 40.14115730948191185, -21.10384086642191193, 71.43714994484031422 ) ) ;
#23638=CARTESIAN_POINT ( 'NONE',  ( 37.69225076346193504, -7.803840866421912104, 70.42958956619168021 ) ) ;
#23646=CARTESIAN_POINT ( 'NONE',  ( 38.63098279924288647, -10.91368208888610170, 70.22690120949091863 ) ) ;
#23648=CARTESIAN_POINT ( 'NONE',  ( 38.63098279924288647, -12.91368208888610525, 70.22690120949090442 ) ) ;
#23656=CARTESIAN_POINT ( 'NONE',  ( 37.25202387243754032, -16.40384086642191619, 72.75271321436731853 ) ) ;
#23660=CARTESIAN_POINT ( 'NONE',  ( 39.41296390513587511, -20.41368208888610170, 71.67976084211551324 ) ) ;
#23664=CARTESIAN_POINT ( 'NONE',  ( 39.95015449827720744, -12.61368208888610454, 70.79240656858105751 ) ) ;
#23675=CARTESIAN_POINT ( 'NONE',  ( 36.29569395875881099, -4.303840866421919209, 72.77780686321129622 ) ) ;
#23678=CARTESIAN_POINT ( 'NONE',  ( 40.14115730948191185, -8.513682088886104893, 71.32335560751961623 ) ) ;
#23681=CARTESIAN_POINT ( 'NONE',  ( 39.02088643472237095, -16.91368208888609814, 69.02690120949091579 ) ) ;
#23689=CARTESIAN_POINT ( 'NONE',  ( 38.73920764526925353, -22.11368208888610098, 72.49843995877330372 ) ) ;
#23695=CARTESIAN_POINT ( 'NONE',  ( 40.26954217208372455, -24.90384086642191619, 72.86986841596730358 ) ) ;
#23696=CARTESIAN_POINT ( 'NONE',  ( 37.25260217561390874, -21.61368208888610098, 71.78268878715392987 ) ) ;
#23698=CARTESIAN_POINT ( 'NONE',  ( 38.82593461698262871, -24.91368208888610170, 69.62690120949091011 ) ) ;
#23701=CARTESIAN_POINT ( 'NONE',  ( 38.00113996487112189, -1.703840866421911571, 70.22690120949091863 ) ) ;
#23706=CARTESIAN_POINT ( 'NONE',  ( 38.37017380507018771, -5.603840866421911926, 69.04448340153881247 ) ) ;
#23709=CARTESIAN_POINT ( 'NONE',  ( 36.80608444377001121, -5.313682088886100274, 70.35351908239860563 ) ) ;
#23712=CARTESIAN_POINT ( 'NONE',  ( 39.38009889167650357, -28.21368208888610951, 72.75271321436730432 ) ) ;
#23714=CARTESIAN_POINT ( 'NONE',  ( 36.68196826583682935, -4.003840866421911393, 70.79240656858108593 ) ) ;
#23716=CARTESIAN_POINT ( 'NONE',  ( 36.49096545463212493, -11.51368208888609956, 71.43714994484034264 ) ) ;
#23719=CARTESIAN_POINT ( 'NONE',  ( 36.80608444377001831, -14.30384086642191122, 72.40698646996135324 ) ) ;
#23725=CARTESIAN_POINT ( 'NONE',  ( 40.14115730948191185, -12.51368208888610489, 71.32335560751960202 ) ) ;
#23727=CARTESIAN_POINT ( 'NONE',  ( 35.86008812008917346, -23.51368208888609956, 71.43714994484032843 ) ) ;
#23731=CARTESIAN_POINT ( 'NONE',  ( 39.41296390513587511, -15.20384086642191157, 71.08074471024441721 ) ) ;
#23736=CARTESIAN_POINT ( 'NONE',  ( 39.65578219934079840, -29.08214825217539712, 70.78045470424321195 ) ) ;
#23738=CARTESIAN_POINT ( 'NONE',  ( 40.33642880535521869, -25.30384086642191477, 69.98269868914864844 ) ) ;
#23740=CARTESIAN_POINT ( 'NONE',  ( 36.29569395875879678, 0.6863179111138985045, 69.98269868914869107 ) ) ;
#23750=CARTESIAN_POINT ( 'NONE',  ( 39.38009889167648936, -19.40384086642190908, 70.00779233799262613 ) ) ;
#23756=CARTESIAN_POINT ( 'NONE',  ( 38.73920764526923932, -5.503840866421911393, 70.26206559358664094 ) ) ;
#23764=CARTESIAN_POINT ( 'NONE',  ( 39.51027997493896748, -6.513682088886100452, 71.32335560751961623 ) ) ;
#23767=CARTESIAN_POINT ( 'NONE',  ( 39.51027997493896748, -4.513682088886101340, 71.32335560751961623 ) ) ;
#23774=CARTESIAN_POINT ( 'NONE',  ( 39.38009889167648936, -19.40384086642190908, 70.00779233799262613 ) ) ;
#23781=CARTESIAN_POINT ( 'NONE',  ( 37.25202387243752611, -15.21368208888610063, 70.00779233799262613 ) ) ;
#23793=CARTESIAN_POINT ( 'NONE',  ( 39.12911128074872380, -3.503840866421911393, 69.06206559358666652 ) ) ;
#23797=CARTESIAN_POINT ( 'NONE',  ( 37.69796330110504101, -7.113682088886100985, 69.66206559358663242 ) ) ;
#23801=CARTESIAN_POINT ( 'NONE',  ( 35.86008812008917346, -13.51368208888610667, 71.43714994484034264 ) ) ;
#23811=CARTESIAN_POINT ( 'NONE',  ( 38.63098279924288647, -26.91368208888610170, 70.22690120949089021 ) ) ;
#23818=CARTESIAN_POINT ( 'NONE',  ( 40.26954217208372455, -22.90384086642191974, 72.86986841596734621 ) ) ;
#23821=CARTESIAN_POINT ( 'NONE',  ( 37.80618814713140097, -27.91368208888610880, 73.13360434286902034 ) ) ;
#23828=CARTESIAN_POINT ( 'NONE',  ( 40.55423172469004101, -3.203840866421916456, 70.70992431699450265 ) ) ;
#23832=CARTESIAN_POINT ( 'NONE',  ( 39.38009889167650357, -10.21368208888610773, 72.75271321436733274 ) ) ;
#23834=CARTESIAN_POINT ( 'NONE',  ( 39.95015449827720744, -26.61368208888610809, 70.79240656858104330 ) ) ;
#23837=CARTESIAN_POINT ( 'NONE',  ( 36.87297107704151244, -3.903840866421908196, 70.26145752964255564 ) ) ;
#23840=CARTESIAN_POINT ( 'NONE',  ( 38.37017380507018771, -25.60384086642191548, 70.24448340153875847 ) ) ;
#23841=CARTESIAN_POINT ( 'NONE',  ( 37.69796330110504101, -9.113682088886100985, 69.66206559358663242 ) ) ;
#23843=CARTESIAN_POINT ( 'NONE',  ( 39.29254315202757653, -12.80384086642191299, 72.81632618279321889 ) ) ;
#23845=CARTESIAN_POINT ( 'NONE',  ( 37.25202387243752611, -9.213682088886100630, 70.00779233799264034 ) ) ;
#23847=CARTESIAN_POINT ( 'NONE',  ( 36.07789103942398867, -15.41368208888610347, 70.70992431699450265 ) ) ;
#23851=CARTESIAN_POINT ( 'NONE',  ( 37.69225076346193504, -17.80384086642191122, 70.42958956619168021 ) ) ;
#23857=CARTESIAN_POINT ( 'NONE',  ( 37.61123632939164452, -25.70384086642191690, 69.02690120949091579 ) ) ;
#23860=CARTESIAN_POINT ( 'NONE',  ( 40.14115730948191185, -26.51368208888610667, 71.32335560751958781 ) ) ;
#23867=CARTESIAN_POINT ( 'NONE',  ( 36.49096545463212493, -20.10384086642191193, 71.32335560751961623 ) ) ;
#23878=CARTESIAN_POINT ( 'NONE',  ( 37.21915885897815457, -0.2038408664219102107, 71.67976084211552745 ) ) ;
#23882=CARTESIAN_POINT ( 'NONE',  ( 39.98359781491296161, -28.41368208888610525, 71.86517103874045631 ) ) ;
#23889=CARTESIAN_POINT ( 'NONE',  ( 38.26194895904383486, -5.013682088886101340, 70.24448340153877268 ) ) ;
#23890=CARTESIAN_POINT ( 'NONE',  ( 37.12184278917507640, -5.513682088886102228, 71.43714994484035685 ) ) ;
#23897=CARTESIAN_POINT ( 'NONE',  ( 40.14115730948191185, -11.10384086642191015, 71.43714994484034264 ) ) ;
#23905=CARTESIAN_POINT ( 'NONE',  ( 38.82593461698262871, -6.913682088886100807, 69.62690120949091011 ) ) ;
#23911=CARTESIAN_POINT ( 'NONE',  ( 40.19479760108050215, -29.10876147765365829, 71.16487613871139217 ) ) ;
#23919=CARTESIAN_POINT ( 'NONE',  ( 40.33642880535521869, -1.303840866421910105, 69.98269868914867686 ) ) ;
#23923=CARTESIAN_POINT ( 'NONE',  ( 39.82603832034400426, -10.31368208888610383, 72.40698646996135324 ) ) ;
#23927=CARTESIAN_POINT ( 'NONE',  ( 36.98690846071097837, -17.81368208888610738, 73.30173637941818754 ) ) ;
#23937=CARTESIAN_POINT ( 'NONE',  ( 39.51027997493896748, -24.51368208888610312, 71.32335560751960202 ) ) ;
#23944=CARTESIAN_POINT ( 'NONE',  ( 40.26954217208372455, -20.90384086642191974, 72.86986841596734621 ) ) ;
#23945=CARTESIAN_POINT ( 'NONE',  ( 38.26194895904383486, -29.01368208888610312, 69.64448340153876416 ) ) ;
#23955=CARTESIAN_POINT ( 'NONE',  ( 37.50301148336529877, -0.5038408664219187205, 73.69843995877330656 ) ) ;
#23958=CARTESIAN_POINT ( 'NONE',  ( 38.37017380507020192, -6.013682088886109334, 73.11602215082118050 ) ) ;
#23961=CARTESIAN_POINT ( 'NONE',  ( 38.37017380507020192, -26.01368208888611022, 73.11602215082115208 ) ) ;
#23964=LINE ( 'NONE', #16721, #24978 ) ;
#23967=CARTESIAN_POINT ( 'NONE',  ( 38.00113996487112189, -25.70384086642191690, 70.22690120949089021 ) ) ;
#23968=CARTESIAN_POINT ( 'NONE',  ( 37.33957961208646736, -13.81368208888610916, 72.81632618279321889 ) ) ;
#23971=CARTESIAN_POINT ( 'NONE',  ( 37.25202387243754032, -10.40384086642191441, 72.75271321436733274 ) ) ;
#23974=CARTESIAN_POINT ( 'NONE',  ( 37.33957961208646736, -13.81368208888610916, 72.81632618279321889 ) ) ;
#23975=ORIENTED_EDGE ( 'NONE', *, *, #19356, .T. ) ;
#23976=CARTESIAN_POINT ( 'NONE',  ( 36.11133435605973574, -17.61368208888610454, 72.15350918040385864 ) ) ;
#23980=CARTESIAN_POINT ( 'NONE',  ( 37.31647492878124694, -16.30384086642191122, 72.03616607671141026 ) ) ;
#23985=CARTESIAN_POINT ( 'NONE',  ( 40.77203464402485622, -23.10384086642191548, 71.43714994484032843 ) ) ;
#23988=CARTESIAN_POINT ( 'NONE',  ( 36.87297107704152666, -27.71368208888610241, 72.49904802271738902 ) ) ;
#23996=CARTESIAN_POINT ( 'NONE',  ( 37.69796330110505522, -20.50384086642191050, 73.09843995877329803 ) ) ;
#24001=CARTESIAN_POINT ( 'NONE',  ( 38.00113996487112189, -1.703840866421911571, 70.22690120949091863 ) ) ;
#24010=CARTESIAN_POINT ( 'NONE',  ( 37.25260217561390874, -3.613682088886100097, 71.78268878715394408 ) ) ;
#24013=CARTESIAN_POINT ( 'NONE',  ( 39.31564783533280405, -4.313682088886102051, 72.03616607671141026 ) ) ;
#24020=CARTESIAN_POINT ( 'NONE',  ( 39.82603832034400426, -11.30384086642190944, 70.35351908239857721 ) ) ;
#24032=CARTESIAN_POINT ( 'NONE',  ( 39.95015449827720744, -10.61368208888610631, 70.79240656858107172 ) ) ;
#24038=CARTESIAN_POINT ( 'NONE',  ( 39.66066260159681889, -29.10876147764981781, 69.85357445396793707 ) ) ;
#24046=CARTESIAN_POINT ( 'NONE',  ( 40.26954217208372455, -2.903840866421918410, 72.86986841596736042 ) ) ;
#24051=CARTESIAN_POINT ( 'NONE',  ( 38.37017380507020192, -8.013682088886108446, 73.11602215082118050 ) ) ;
#24056=CARTESIAN_POINT ( 'NONE',  ( 40.77203464402485622, -14.51368208888610312, 71.32335560751960202 ) ) ;
#24066=CARTESIAN_POINT ( 'NONE',  ( 37.25260217561390874, -25.61368208888610098, 71.78268878715390144 ) ) ;
#24073=CARTESIAN_POINT ( 'NONE',  ( 38.26194895904384197, -20.60384086642191903, 73.71602215082113219 ) ) ;
#24074=CARTESIAN_POINT ( 'NONE',  ( 36.29569395875879678, 0.6863179111138985045, 69.98269868914869107 ) ) ;
#24080=CARTESIAN_POINT ( 'NONE',  ( 37.50301148336529877, -6.503840866421916722, 73.69843995877330656 ) ) ;
#24083=CARTESIAN_POINT ( 'NONE',  ( 36.68196826583682935, -7.613682088886103649, 71.96809898377890136 ) ) ;
#24089=CARTESIAN_POINT ( 'NONE',  ( 39.24876120206129571, -24.90384086642191264, 72.12822762946746025 ) ) ;
#24090=CARTESIAN_POINT ( 'NONE',  ( 39.38009889167650357, -12.21368208888610596, 72.75271321436731853 ) ) ;
#24093=CARTESIAN_POINT ( 'NONE',  ( 38.82593461698265003, -10.70384086642191690, 73.13360434286904876 ) ) ;
#24096=CARTESIAN_POINT ( 'NONE',  ( 38.93415946300897446, -12.11368208888610276, 73.09843995877329803 ) ) ;
#24098=CARTESIAN_POINT ( 'NONE',  ( 36.89935272106204422, -13.21368208888610241, 69.52238214136768590 ) ) ;
#24102=CARTESIAN_POINT ( 'NONE',  ( 37.21915885897815457, -20.20384086642191335, 71.67976084211552745 ) ) ;
#24107=CARTESIAN_POINT ( 'NONE',  ( 36.07789103942399578, -22.20384086642191690, 72.05058123536544201 ) ) ;
#24109=CARTESIAN_POINT ( 'NONE',  ( 40.14115730948191185, -24.51368208888609601, 71.32335560751958781 ) ) ;
#24114=CARTESIAN_POINT ( 'NONE',  ( 39.95015449827720744, -13.00384086642191228, 71.96809898377887293 ) ) ;
#24121=CARTESIAN_POINT ( 'NONE',  ( 39.02742774030101458, -1.403840866421909972, 70.49320253461759478 ) ) ;
#24130=CARTESIAN_POINT ( 'NONE',  ( 38.93987200065208754, -4.813682088886099386, 70.42958956619168021 ) ) ;
#24131=CARTESIAN_POINT ( 'NONE',  ( 37.25260217561390874, -5.613682088886101873, 71.78268878715394408 ) ) ;
#24139=CARTESIAN_POINT ( 'NONE',  ( 39.82603832034400426, -9.303840866421907663, 70.35351908239857721 ) ) ;
#24149=CARTESIAN_POINT ( 'NONE',  ( 37.33957961208646736, -5.813682088886107380, 72.81632618279323310 ) ) ;
#24161=CARTESIAN_POINT ( 'NONE',  ( 36.11133435605973574, -27.61368208888610809, 72.15350918040381600 ) ) ;
#24162=CARTESIAN_POINT ( 'NONE',  ( 37.60469502381300089, -21.21368208888610241, 70.49320253461759478 ) ) ;
#24166=CARTESIAN_POINT ( 'NONE',  ( 36.64852494920107517, -5.413682088886106136, 70.89533451361948835 ) ) ;
#24167=CARTESIAN_POINT ( 'NONE',  ( 37.25202387243754032, -28.40384086642191619, 72.75271321436730432 ) ) ;
#24169=CARTESIAN_POINT ( 'NONE',  ( 40.52078840805428683, -6.613682088886105426, 70.60699637195608602 ) ) ;
#24189=CARTESIAN_POINT ( 'NONE',  ( 39.02088643472237806, -22.70384086642191690, 73.73360434286898624 ) ) ;
#24191=CARTESIAN_POINT ( 'NONE',  ( 39.38009889167650357, -28.21368208888610951, 72.75271321436730432 ) ) ;
#24195=CARTESIAN_POINT ( 'NONE',  ( 39.59324923284151510, -28.74115096347518161, 70.20355626897213597 ) ) ;
#24199=CARTESIAN_POINT ( 'NONE',  ( 40.33642880535521869, -1.303840866421910105, 69.98269868914867686 ) ) ;
#24201=CARTESIAN_POINT ( 'NONE',  ( 36.80608444377001121, -9.313682088886100274, 70.35351908239860563 ) ) ;
#24204=CARTESIAN_POINT ( 'NONE',  ( 39.95015449827720744, -18.61368208888610454, 70.79240656858105751 ) ) ;
#24209=CARTESIAN_POINT ( 'NONE',  ( 37.89291511884479036, -26.50384086642191406, 72.49843995877328950 ) ) ;
#24210=CARTESIAN_POINT ( 'NONE',  ( 39.98359781491296161, -14.41368208888610525, 71.86517103874047052 ) ) ;
#24215=CARTESIAN_POINT ( 'NONE',  ( 38.26194895904384907, -14.60384086642191548, 73.11602215082116629 ) ) ;
#24217=CARTESIAN_POINT ( 'NONE',  ( 37.69796330110504101, -3.113682088886098764, 69.66206559358663242 ) ) ;
#24219=CARTESIAN_POINT ( 'NONE',  ( 37.50301148336529167, -13.11368208888610454, 69.06206559358665231 ) ) ;
#24223=CARTESIAN_POINT ( 'NONE',  ( 37.21915885897815457, -12.20384086642191157, 71.67976084211552745 ) ) ;
#24229=CARTESIAN_POINT ( 'NONE',  ( 38.26194895904384197, -20.60384086642191903, 73.71602215082113219 ) ) ;
#24231=CARTESIAN_POINT ( 'NONE',  ( 39.95015449827720744, -24.61368208888610454, 70.79240656858104330 ) ) ;
#24241=CARTESIAN_POINT ( 'NONE',  ( 38.82593461698264292, -16.70384086642191690, 73.13360434286903455 ) ) ;
#24248=CARTESIAN_POINT ( 'NONE',  ( 38.26194895904384907, -28.60384086642191548, 73.11602215082115208 ) ) ;
#24253=CARTESIAN_POINT ( 'NONE',  ( 38.37017380507020192, -24.01368208888610667, 73.11602215082115208 ) ) ;
#24259=CARTESIAN_POINT ( 'NONE',  ( 39.41296390513587511, -8.413682088886101695, 71.67976084211552745 ) ) ;
#24260=CARTESIAN_POINT ( 'NONE',  ( 38.26194895904383486, -5.013682088886101340, 70.24448340153877268 ) ) ;
#24267=CARTESIAN_POINT ( 'NONE',  ( 39.98359781491296161, -9.203840866421911571, 70.89533451361947414 ) ) ;
#24279=CARTESIAN_POINT ( 'NONE',  ( 38.82593461698262871, -4.913682088886101695, 69.62690120949091011 ) ) ;
#24291=CARTESIAN_POINT ( 'NONE',  ( 39.02088643472237095, -28.91368208888610170, 69.02690120949091579 ) ) ;
#24292=CARTESIAN_POINT ( 'NONE',  ( 38.93987200065208754, -24.81368208888610738, 70.42958956619166599 ) ) ;
#24297=CARTESIAN_POINT ( 'NONE',  ( 36.87297107704152666, -3.713682088886109511, 72.49904802271743165 ) ) ;
#24298=CARTESIAN_POINT ( 'NONE',  ( 39.41296390513587511, -1.203840866421910905, 71.08074471024443142 ) ) ;
#24300=CARTESIAN_POINT ( 'NONE',  ( 38.37017380507020192, -8.013682088886108446, 73.71602215082116061 ) ) ;
#24314=CARTESIAN_POINT ( 'NONE',  ( 36.98690846071097127, -15.80384086642191299, 69.45876917294175712 ) ) ;
#24315=CARTESIAN_POINT ( 'NONE',  ( 36.68196826583682935, -23.61368208888610454, 71.96809898377887293 ) ) ;
#24322=FACE_OUTER_BOUND ( 'NONE', #3738, .T. ) ;
#24323=CARTESIAN_POINT ( 'NONE',  ( 40.55423172469004811, -28.41368208888610525, 72.05058123536539938 ) ) ;
#24329=CARTESIAN_POINT ( 'NONE',  ( 39.98359781491296161, 1.586317911113896528, 71.86517103874049894 ) ) ;
#24332=CARTESIAN_POINT ( 'NONE',  ( 39.38009889167650357, -18.21368208888610951, 72.75271321436731853 ) ) ;
#24336=CARTESIAN_POINT ( 'NONE',  ( 38.00113996487112189, -27.70384086642191690, 70.22690120949089021 ) ) ;
#24337=CARTESIAN_POINT ( 'NONE',  ( 39.75915168707250302, -4.713682088886100630, 70.26145752964252722 ) ) ;
#24341=CARTESIAN_POINT ( 'NONE',  ( 37.80618814713138676, -7.703840866421907130, 69.62690120949091011 ) ) ;
#24344=CARTESIAN_POINT ( 'NONE',  ( 37.25202387243752611, -7.213682088886102406, 70.00779233799264034 ) ) ;
#24346=CARTESIAN_POINT ( 'NONE',  ( 38.26194895904383486, -17.01368208888610312, 69.04448340153878405 ) ) ;
#24350=CARTESIAN_POINT ( 'NONE',  ( 37.21915885897815457, -10.20384086642191335, 71.67976084211552745 ) ) ;
#24357=CARTESIAN_POINT ( 'NONE',  ( 39.73277004305197124, -15.40384086642191441, 69.52238214136768590 ) ) ;
#24362=CARTESIAN_POINT ( 'NONE',  ( 39.95015449827720744, -26.61368208888610809, 70.79240656858104330 ) ) ;
#24370=CARTESIAN_POINT ( 'NONE',  ( 39.38009889167648936, -17.40384086642190908, 70.00779233799262613 ) ) ;
#24376=CARTESIAN_POINT ( 'NONE',  ( 38.37017380507018771, -29.60384086642190837, 69.64448340153876416 ) ) ;
#24379=SHAPE_REPRESENTATION ( 'Pusher Pull Spring', ( #2000 ), #13127 ) ;
#24382=CARTESIAN_POINT ( 'NONE',  ( 37.25202387243752611, -23.21368208888610241, 70.00779233799262613 ) ) ;
#24388=CARTESIAN_POINT ( 'NONE',  ( 37.21915885897815457, -28.20384086642191335, 71.67976084211551324 ) ) ;
#24389=CARTESIAN_POINT ( 'NONE',  ( 37.89291511884476904, 0.8863179111139005695, 70.26206559358665515 ) ) ;
#24396=CARTESIAN_POINT ( 'NONE',  ( 36.68196826583682935, -8.003840866421912281, 70.79240656858108593 ) ) ;
#24404=CARTESIAN_POINT ( 'NONE',  ( 39.95015449827720744, -6.613682088886106314, 70.79240656858107172 ) ) ;
#24420=CARTESIAN_POINT ( 'NONE',  ( 39.12911128074873801, -26.11368208888610809, 73.69843995877326392 ) ) ;
#24422=CARTESIAN_POINT ( 'NONE',  ( 37.38336156205274818, -15.71368208888609885, 72.12822762946750288 ) ) ;
#24426=CARTESIAN_POINT ( 'NONE',  ( 37.33957961208646736, -3.813682088886109156, 72.81632618279323310 ) ) ;
#24427=CARTESIAN_POINT ( 'NONE',  ( 38.37017380507018771, -27.60384086642191193, 69.64448340153876416 ) ) ;
#24431=CARTESIAN_POINT ( 'NONE',  ( 39.12911128074873801, -6.113682088886108978, 73.69843995877330656 ) ) ;
#24446=CARTESIAN_POINT ( 'NONE',  ( 40.33642880535521869, -17.30384086642191477, 69.98269868914866265 ) ) ;
#24447=CARTESIAN_POINT ( 'NONE',  ( 37.33957961208646736, -23.81368208888611093, 72.81632618279320468 ) ) ;
#24454=CARTESIAN_POINT ( 'NONE',  ( 40.52078840805428683, -28.61368208888610454, 70.60699637195608602 ) ) ;
#24458=CARTESIAN_POINT ( 'NONE',  ( 38.37017380507020192, -2.013682088886109334, 73.11602215082118050 ) ) ;
#24460=CARTESIAN_POINT ( 'NONE',  ( 39.98359781491296161, -22.41368208888610525, 71.86517103874047052 ) ) ;
#24463=CARTESIAN_POINT ( 'NONE',  ( 38.26194895904384197, -16.60384086642191193, 72.51602215082118619 ) ) ;
#24464=CARTESIAN_POINT ( 'NONE',  ( 36.87297107704152666, -3.713682088886109511, 72.49904802271743165 ) ) ;
#24467=CARTESIAN_POINT ( 'NONE',  ( 39.29254315202757653, -6.803840866421915656, 72.81632618279323310 ) ) ;
#24469=CARTESIAN_POINT ( 'NONE',  ( 39.98359781491296161, -4.413682088886105248, 71.86517103874048473 ) ) ;
#24471=CARTESIAN_POINT ( 'NONE',  ( 38.37017380507020192, -12.01368208888611022, 73.71602215082113219 ) ) ;
#24474=CARTESIAN_POINT ( 'NONE',  ( 39.41296390513587511, -13.20384086642191157, 71.08074471024441721 ) ) ;
#24480=CARTESIAN_POINT ( 'NONE',  ( 36.36258059203030513, -15.90384086642191264, 69.89063713639259845 ) ) ;
#24482=CARTESIAN_POINT ( 'NONE',  ( 39.29254315202756231, -18.81368208888610027, 69.94417936956672577 ) ) ;
#24488=CARTESIAN_POINT ( 'NONE',  ( 37.33957961208645315, -13.80384086642190766, 69.94417936956672577 ) ) ;
#24492=CARTESIAN_POINT ( 'NONE',  ( 38.37017380507020192, -26.01368208888611022, 73.11602215082115208 ) ) ;
#24498=CARTESIAN_POINT ( 'NONE',  ( 37.80618814713138676, -25.70384086642190979, 69.62690120949091011 ) ) ;
#24502=CARTESIAN_POINT ( 'NONE',  ( 37.33957961208646736, -25.81368208888610738, 72.81632618279320468 ) ) ;
#24507=CARTESIAN_POINT ( 'NONE',  ( 38.26194895904383486, 0.9863179111139001032, 70.24448340153880110 ) ) ;
#24508=CARTESIAN_POINT ( 'NONE',  ( 39.51027997493896748, -29.10384086642191193, 71.43714994484031422 ) ) ;
#24516=CARTESIAN_POINT ( 'NONE',  ( 36.68196826583682935, -6.003840866421913169, 70.79240656858108593 ) ) ;
#24523=CARTESIAN_POINT ( 'NONE',  ( 37.25202387243752611, -3.213682088886102406, 70.00779233799264034 ) ) ;
#24525=CARTESIAN_POINT ( 'NONE',  ( 39.66066260159757917, -29.10876147765399580, 70.75778293607493197 ) ) ;
#24539=CARTESIAN_POINT ( 'NONE',  ( 38.37017380507020192, -20.01368208888610312, 72.51602215082118619 ) ) ;
#24543=CARTESIAN_POINT ( 'NONE',  ( 36.49096545463212493, 0.4863179111138959954, 71.43714994484035685 ) ) ;
#24544=CARTESIAN_POINT ( 'NONE',  ( 38.37017380507018771, -21.60384086642190837, 69.64448340153877837 ) ) ;
#24546=CARTESIAN_POINT ( 'NONE',  ( 37.50301148336529167, -9.113682088886102761, 69.06206559358666652 ) ) ;
#24562=CARTESIAN_POINT ( 'NONE',  ( 39.73277004305197124, -15.40384086642191441, 69.52238214136768590 ) ) ;
#24563=CARTESIAN_POINT ( 'NONE',  ( 37.25202387243752611, -21.21368208888610241, 70.00779233799262613 ) ) ;
#24573=CARTESIAN_POINT ( 'NONE',  ( 38.26194895904383486, -25.01368208888610312, 69.04448340153878405 ) ) ;
#24580=CARTESIAN_POINT ( 'NONE',  ( 36.68196826583682935, 0.3863179111138967392, 71.96809898377890136 ) ) ;
#24582=CARTESIAN_POINT ( 'NONE',  ( 36.68196826583682935, -19.61368208888610809, 71.96809898377888715 ) ) ;
#24585=CARTESIAN_POINT ( 'NONE',  ( 39.51027997493896748, -21.10384086642191193, 71.43714994484032843 ) ) ;
#24586=CARTESIAN_POINT ( 'NONE',  ( 36.64852494920107517, -5.413682088886106136, 70.89533451361948835 ) ) ;
#24592=CARTESIAN_POINT ( 'NONE',  ( 36.80608444377001831, -2.303840866421914768, 72.40698646996136745 ) ) ;
#24594=CARTESIAN_POINT ( 'NONE',  ( 39.82603832034400426, -8.313682088886110932, 72.40698646996135324 ) ) ;
#24596=CARTESIAN_POINT ( 'NONE',  ( 40.77203464402485622, -10.51368208888610312, 71.32335560751961623 ) ) ;
#24599=CARTESIAN_POINT ( 'NONE',  ( 37.25260217561390874, -14.00384086642191050, 70.97781676520601479 ) ) ;
#24605=CARTESIAN_POINT ( 'NONE',  ( 36.11133435605973574, -14.00384086642191583, 70.60699637195608602 ) ) ;
#24609=CARTESIAN_POINT ( 'NONE',  ( 36.64852494920107517, -17.41368208888610525, 70.89533451361947414 ) ) ;
#24615=CARTESIAN_POINT ( 'NONE',  ( 37.80618814713138676, -9.703840866421906242, 69.62690120949091011 ) ) ;
#24619=CARTESIAN_POINT ( 'NONE',  ( 38.82593461698262871, -22.91368208888609459, 69.62690120949091011 ) ) ;
#24623=CARTESIAN_POINT ( 'NONE',  ( 38.82593461698265003, -26.70384086642190624, 73.13360434286902034 ) ) ;
#24626=CARTESIAN_POINT ( 'NONE',  ( 36.49096545463212493, -23.51368208888609601, 71.43714994484030001 ) ) ;
#24631=CARTESIAN_POINT ( 'NONE',  ( 39.24876120206128860, -0.7136820888861000745, 70.63227792289247020 ) ) ;
#24633=CARTESIAN_POINT ( 'NONE',  ( 38.93987200065208754, 1.186317911113898838, 70.42958956619170863 ) ) ;
#24640=CARTESIAN_POINT ( 'NONE',  ( 38.82593461698265003, -6.703840866421914235, 73.13360434286904876 ) ) ;
#24654=CARTESIAN_POINT ( 'NONE',  ( 36.49096545463212493, 0.4863179111138961064, 71.43714994484035685 ) ) ;
#24673=CARTESIAN_POINT ( 'NONE',  ( 37.31647492878122563, -17.31368208888610383, 70.72433947564853440 ) ) ;
#24677=CARTESIAN_POINT ( 'NONE',  ( 36.68196826583682935, 0.3863179111138967392, 71.96809898377890136 ) ) ;
#24678=CARTESIAN_POINT ( 'NONE',  ( 36.68196826583682935, -24.00384086642191050, 70.79240656858105751 ) ) ;
#24681=CARTESIAN_POINT ( 'NONE',  ( 37.61123632939165873, -7.913682088886107913, 73.73360434286902887 ) ) ;
#24690=CARTESIAN_POINT ( 'NONE',  ( 38.82593461698264292, 1.296159133578084210, 73.13360434286906298 ) ) ;
#24701=CARTESIAN_POINT ( 'NONE',  ( 36.89935272106205133, -20.40384086642192329, 73.23812341099225875 ) ) ;
#24703=CARTESIAN_POINT ( 'NONE',  ( 37.69796330110504101, -19.11368208888610098, 69.66206559358661821 ) ) ;
#24708=CARTESIAN_POINT ( 'NONE',  ( 40.55423172469004811, -26.41368208888610880, 72.05058123536539938 ) ) ;
#24712=CARTESIAN_POINT ( 'NONE',  ( 39.98359781491296161, -0.4136820888861053591, 71.86517103874048473 ) ) ;
#24715=CARTESIAN_POINT ( 'NONE',  ( 40.14115730948191185, -20.51368208888610312, 71.32335560751960202 ) ) ;
#24719=CARTESIAN_POINT ( 'NONE',  ( 37.69225076346193504, -17.80384086642191122, 70.42958956619168021 ) ) ;
#24720=CARTESIAN_POINT ( 'NONE',  ( 36.87297107704152666, -7.713682088886109511, 72.49904802271743165 ) ) ;
#24725=CARTESIAN_POINT ( 'NONE',  ( 39.98359781491296161, -7.203840866421913347, 70.89533451361947414 ) ) ;
#24728=CARTESIAN_POINT ( 'NONE',  ( 37.25260217561390874, -27.61368208888610454, 71.78268878715390144 ) ) ;
#24730=CARTESIAN_POINT ( 'NONE',  ( 38.26194895904383486, -11.01368208888609956, 69.04448340153881247 ) ) ;
#24733=CARTESIAN_POINT ( 'NONE',  ( 38.73920764526923932, -9.503840866421912281, 70.26206559358664094 ) ) ;
#24739=CARTESIAN_POINT ( 'NONE',  ( 36.07789103942399578, -16.20384086642191690, 72.05058123536544201 ) ) ;
#24742=CARTESIAN_POINT ( 'NONE',  ( 36.80608444377001121, -17.31368208888609672, 70.35351908239857721 ) ) ;
#24750=CARTESIAN_POINT ( 'NONE',  ( 39.38009889167648936, -9.403840866421907307, 70.00779233799264034 ) ) ;
#24754=CARTESIAN_POINT ( 'NONE',  ( 38.93415946300897446, -22.11368208888610454, 73.09843995877329803 ) ) ;
#24757=CARTESIAN_POINT ( 'NONE',  ( 38.93415946300896024, -25.50384086642190340, 69.66206559358660400 ) ) ;
#24759=CARTESIAN_POINT ( 'NONE',  ( 40.14115730948191185, -22.51368208888609956, 71.32335560751960202 ) ) ;
#24764=CARTESIAN_POINT ( 'NONE',  ( 37.31647492878122563, -1.313682088886099830, 70.72433947564853440 ) ) ;
#24771=CARTESIAN_POINT ( 'NONE',  ( 38.37017380507018771, -5.603840866421908373, 69.64448340153879258 ) ) ;
#24780=CARTESIAN_POINT ( 'NONE',  ( 39.75915168707250302, 1.286317911113898482, 70.26145752964255564 ) ) ;
#24799=CARTESIAN_POINT ( 'NONE',  ( 37.38336156205274818, -19.71368208888610596, 72.12822762946750288 ) ) ;
#24805=CARTESIAN_POINT ( 'NONE',  ( 37.69796330110504101, -1.113682088886101207, 69.66206559358663242 ) ) ;
#24806=CARTESIAN_POINT ( 'NONE',  ( 39.82603832034400426, -25.30384086642190766, 70.35351908239857721 ) ) ;
#24810=CARTESIAN_POINT ( 'NONE',  ( 40.77203464402485622, -2.513682088886103116, 71.32335560751961623 ) ) ;
#24819=CIRCLE ( 'NONE', #4269, 0.2999999999999938827 ) ;
#24829=CARTESIAN_POINT ( 'NONE',  ( 36.11133435605973574, -16.00384086642191406, 70.60699637195608602 ) ) ;
#24833=CARTESIAN_POINT ( 'NONE',  ( 39.82603832034400426, -18.31368208888610738, 72.40698646996133903 ) ) ;
#24834=SURFACE_SIDE_STYLE ('',( #20860 ) ) ;
#24839=CARTESIAN_POINT ( 'NONE',  ( 39.64521430340304420, -24.81368208888610738, 69.45876917294174291 ) ) ;
#24845=CARTESIAN_POINT ( 'NONE',  ( 36.87297107704152666, 0.2863179111138939303, 72.49904802271743165 ) ) ;
#24847=CARTESIAN_POINT ( 'NONE',  ( 38.82593461698262871, -14.91368208888609992, 69.62690120949091011 ) ) ;
#24851=CARTESIAN_POINT ( 'NONE',  ( 37.25260217561390874, -18.00384086642191050, 70.97781676520601479 ) ) ;
#24852=CARTESIAN_POINT ( 'NONE',  ( 39.29254315202756231, -2.813682088886101162, 69.94417936956673998 ) ) ;
#24856=CARTESIAN_POINT ( 'NONE',  ( 37.25202387243754032, -8.403840866421916189, 72.75271321436733274 ) ) ;
#24858=CARTESIAN_POINT ( 'NONE',  ( 37.33957961208646736, -1.813682088886107380, 72.81632618279323310 ) ) ;
#24860=CARTESIAN_POINT ( 'NONE',  ( 40.26954217208371034, -6.713682088886101518, 69.89063713639259845 ) ) ;
#24863=CARTESIAN_POINT ( 'NONE',  ( 37.21915885897815457, -8.203840866421909794, 71.67976084211552745 ) ) ;
#24868=CARTESIAN_POINT ( 'NONE',  ( 36.36258059203030513, -13.90384086642191264, 69.89063713639259845 ) ) ;
#24870=CARTESIAN_POINT ( 'NONE',  ( 39.98359781491296161, -18.41368208888610880, 71.86517103874047052 ) ) ;
#24873=ADVANCED_FACE ( 'NONE', ( #21836 ), #19141, .T. ) ;
#24876=CARTESIAN_POINT ( 'NONE',  ( 39.95015449827720744, -11.00384086642191050, 71.96809898377888715 ) ) ;
#24878=CARTESIAN_POINT ( 'NONE',  ( 38.37017380507020192, -24.01368208888610667, 73.11602215082115208 ) ) ;
#24880=CARTESIAN_POINT ( 'NONE',  ( 39.29254315202757653, -26.80384086642191477, 72.81632618279320468 ) ) ;
#24882=CARTESIAN_POINT ( 'NONE',  ( 36.87297107704152666, -17.71368208888610951, 72.49904802271740323 ) ) ;
#24884=CARTESIAN_POINT ( 'NONE',  ( 36.36258059203031934, -25.71368208888611306, 72.86986841596734621 ) ) ;
#24888=CARTESIAN_POINT ( 'NONE',  ( 39.41296390513587511, -2.413682088886099919, 71.67976084211552745 ) ) ;
#24895=CARTESIAN_POINT ( 'NONE',  ( 39.29254315202757653, -4.803840866421913880, 72.81632618279323310 ) ) ;
#24903=CARTESIAN_POINT ( 'NONE',  ( 37.33957961208646736, 0.1863179111138910105, 72.81632618279323310 ) ) ;
#24919=CARTESIAN_POINT ( 'NONE',  ( 39.31564783533280405, -18.31368208888610027, 72.03616607671141026 ) ) ;
#24924=CARTESIAN_POINT ( 'NONE',  ( 37.25202387243754032, -24.40384086642191619, 72.75271321436730432 ) ) ;
#24926=CARTESIAN_POINT ( 'NONE',  ( 38.26194895904383486, -3.013682088886100008, 69.04448340153881247 ) ) ;
#24945=CARTESIAN_POINT ( 'NONE',  ( 35.86008812008917346, -12.10384086642191548, 71.32335560751961623 ) ) ;
#24947=CARTESIAN_POINT ( 'NONE',  ( 36.68196826583682935, -15.61368208888610454, 71.96809898377888715 ) ) ;
#24952=CARTESIAN_POINT ( 'NONE',  ( 36.07789103942398867, -23.41368208888610525, 70.70992431699450265 ) ) ;
#24967=CARTESIAN_POINT ( 'NONE',  ( 37.69225076346193504, -19.80384086642191477, 70.42958956619168021 ) ) ;
#24968=CARTESIAN_POINT ( 'NONE',  ( 39.95015449827720744, -0.6136820888861040935, 70.79240656858107172 ) ) ;
#24977=CARTESIAN_POINT ( 'NONE',  ( 36.80608444377001831, -0.3038408664219130473, 72.40698646996136745 ) ) ;
#24978=VECTOR ( 'NONE', #14913, 1000.000000000000000 ) ;
#24979=CARTESIAN_POINT ( 'NONE',  ( 39.24876120206128860, -28.71368208888610241, 70.63227792289242757 ) ) ;
#24980=CARTESIAN_POINT ( 'NONE',  ( 36.07789103942398867, -11.41368208888610525, 70.70992431699450265 ) ) ;
#24983=CARTESIAN_POINT ( 'NONE',  ( 39.37952058850012804, -5.003840866421912281, 71.78268878715392987 ) ) ;
#24989=CARTESIAN_POINT ( 'NONE',  ( 40.33642880535521869, -7.303840866421912104, 69.98269868914867686 ) ) ;
#24991=CARTESIAN_POINT ( 'NONE',  ( 37.33957961208646736, -19.81368208888611093, 72.81632618279321889 ) ) ;
#24998=CARTESIAN_POINT ( 'NONE',  ( 39.29254315202757653, -6.803840866421915656, 72.81632618279323310 ) ) ;
#25001=CARTESIAN_POINT ( 'NONE',  ( 38.26194895904383486, -23.01368208888609956, 69.64448340153877837 ) ) ;
#25004=CARTESIAN_POINT ( 'NONE',  ( 36.64852494920107517, -26.20384086642191335, 71.86517103874047052 ) ) ;
#25006=CARTESIAN_POINT ( 'NONE',  ( 39.98359781491296161, -20.41368208888610525, 71.86517103874047052 ) ) ;
#25008=CARTESIAN_POINT ( 'NONE',  ( 39.12911128074872380, 0.4961591335780889955, 69.06206559358666652 ) ) ;
#25012=CARTESIAN_POINT ( 'NONE',  ( 38.00113996487112189, -27.70384086642191690, 70.22690120949089021 ) ) ;
#25021=CARTESIAN_POINT ( 'NONE',  ( 39.75915168707251723, 1.096159133578084699, 72.49904802271743165 ) ) ;
#25029=CARTESIAN_POINT ( 'NONE',  ( 36.68196826583682935, -3.613682088886103205, 71.96809898377890136 ) ) ;
#25030=CARTESIAN_POINT ( 'NONE',  ( 36.68196826583682935, -28.00384086642191050, 70.79240656858105751 ) ) ;
#25044=CARTESIAN_POINT ( 'NONE',  ( 38.00113996487114321, -9.913682088886099919, 72.53360434286905445 ) ) ;
#25046=CARTESIAN_POINT ( 'NONE',  ( 37.21915885897815457, -11.41368208888610170, 71.08074471024443142 ) ) ;
#25052=CARTESIAN_POINT ( 'NONE',  ( 36.87297107704149823, -21.90384086642189843, 70.26145752964252722 ) ) ;
#25054=CARTESIAN_POINT ( 'NONE',  ( 37.89291511884476904, -17.11368208888609743, 70.26206559358661252 ) ) ;
#25071=CARTESIAN_POINT ( 'NONE',  ( 40.77203464402485622, -13.10384086642191548, 71.43714994484032843 ) ) ;
#25074=CARTESIAN_POINT ( 'NONE',  ( 39.98359781491296161, -12.41368208888610525, 71.86517103874047052 ) ) ;
#25080=CARTESIAN_POINT ( 'NONE',  ( 39.12911128074873801, -24.11368208888611164, 73.69843995877326392 ) ) ;
#25091=CARTESIAN_POINT ( 'NONE',  ( 38.26194895904384197, -10.60384086642191370, 72.51602215082118619 ) ) ;
#25092=CARTESIAN_POINT ( 'NONE',  ( 39.29254315202756231, -0.8136820888860994971, 69.94417936956673998 ) ) ;
#25098=CARTESIAN_POINT ( 'NONE',  ( 36.49096545463212493, -2.103840866421912814, 71.32335560751963044 ) ) ;
#25101=CARTESIAN_POINT ( 'NONE',  ( 37.12184278917507640, -27.51368208888609956, 71.43714994484032843 ) ) ;
#25102=CARTESIAN_POINT ( 'NONE',  ( 36.07789103942398867, -1.413682088886102584, 70.70992431699450265 ) ) ;
#25105=CARTESIAN_POINT ( 'NONE',  ( 37.25260217561390874, -6.003840866421913169, 70.97781676520604321 ) ) ;
#25112=CARTESIAN_POINT ( 'NONE',  ( 36.89935272106205133, -12.40384086642192152, 73.23812341099225875 ) ) ;
#25116=CARTESIAN_POINT ( 'NONE',  ( 37.80618814713140097, -15.91368208888610880, 73.13360434286903455 ) ) ;
#25122=CARTESIAN_POINT ( 'NONE',  ( 38.93415946300897446, -5.503840866421908729, 69.66206559358664663 ) ) ;
#25125=CARTESIAN_POINT ( 'NONE',  ( 38.82593461698262871, -18.91368208888609459, 69.62690120949091011 ) ) ;
#25127=CARTESIAN_POINT ( 'NONE',  ( 39.98359781491296161, -21.20384086642190979, 70.89533451361945993 ) ) ;
#25131=COLOUR_RGB ( '', 0.09019608, 0.27058824, 0.51372549) ;
#25132=CARTESIAN_POINT ( 'NONE',  ( 37.33957961208646736, -17.81368208888611093, 72.81632618279321889 ) ) ;
#25134=CARTESIAN_POINT ( 'NONE',  ( 36.98690846071097837, -21.81368208888610738, 73.30173637941818754 ) ) ;
#25138=CARTESIAN_POINT ( 'NONE',  ( 39.24876120206129571, -22.90384086642191264, 72.12822762946747446 ) ) ;
#25147=CARTESIAN_POINT ( 'NONE',  ( 36.11133435605973574, -28.00384086642191761, 70.60699637195608602 ) ) ;
#25156=CARTESIAN_POINT ( 'NONE',  ( 36.87297107704151244, -27.90384086642190908, 70.26145752964252722 ) ) ;
#25163=CARTESIAN_POINT ( 'NONE',  ( 37.38336156205273397, -5.903840866421909972, 70.63227792289248441 ) ) ;
#25170=CARTESIAN_POINT ( 'NONE',  ( 37.60469502381300089, -13.21368208888610241, 70.49320253461759478 ) ) ;
#25172=CARTESIAN_POINT ( 'NONE',  ( 37.31647492878122563, -9.313682088886098498, 70.72433947564853440 ) ) ;
#25178=CARTESIAN_POINT ( 'NONE',  ( 37.25202387243754032, -14.40384086642191619, 72.75271321436731853 ) ) ;
#25182=CARTESIAN_POINT ( 'NONE',  ( 38.63098279924288647, -20.91368208888609814, 70.22690120949090442 ) ) ;
#25203=CARTESIAN_POINT ( 'NONE',  ( 36.36258059203030513, -11.90384086642191441, 69.89063713639259845 ) ) ;
#25207=CARTESIAN_POINT ( 'NONE',  ( 38.82593461698262871, -16.91368208888610170, 69.62690120949091011 ) ) ;
#25214=CARTESIAN_POINT ( 'NONE',  ( 38.26194895904383486, -21.01368208888610312, 69.04448340153878405 ) ) ;
#25227=CARTESIAN_POINT ( 'NONE',  ( 39.51027997493896748, -15.10384086642191370, 71.43714994484032843 ) ) ;
#25228=CARTESIAN_POINT ( 'NONE',  ( 38.82593461698262871, 1.086317911113899637, 69.62690120949091011 ) ) ;
#25235=CARTESIAN_POINT ( 'NONE',  ( 37.25202387243754032, -0.4038408664219159117, 72.75271321436733274 ) ) ;
#25237=CARTESIAN_POINT ( 'NONE',  ( 36.68196826583682935, 0.3863179111138967392, 71.96809898377890136 ) ) ;
#25238=CARTESIAN_POINT ( 'NONE',  ( 36.11133435605973574, -3.613682088886103205, 72.15350918040385864 ) ) ;
#25241=CARTESIAN_POINT ( 'NONE',  ( 37.89291511884479036, -8.503840866421912281, 72.49843995877331793 ) ) ;
#25247=CARTESIAN_POINT ( 'NONE',  ( 36.07789103942399578, -8.203840866421915123, 72.05058123536544201 ) ) ;
#25250=CARTESIAN_POINT ( 'NONE',  ( 39.95015449827720744, -14.61368208888610454, 70.79240656858105751 ) ) ;
#25256=CARTESIAN_POINT ( 'NONE',  ( 39.95015449827720744, -3.003840866421910505, 71.96809898377888715 ) ) ;
#25259=CARTESIAN_POINT ( 'NONE',  ( 39.29254315202756231, -18.81368208888610027, 69.94417936956672577 ) ) ;
#25263=CARTESIAN_POINT ( 'NONE',  ( 36.87297107704149823, -15.90384086642190908, 70.26145752964252722 ) ) ;
#25266=CARTESIAN_POINT ( 'NONE',  ( 39.38009889167650357, -20.21368208888610951, 72.75271321436731853 ) ) ;
#25268=CARTESIAN_POINT ( 'NONE',  ( 37.50301148336529167, -21.11368208888610098, 69.06206559358665231 ) ) ;
#25273=CARTESIAN_POINT ( 'NONE',  ( 37.69225076346193504, -27.80384086642191477, 70.42958956619166599 ) ) ;
#25280=CARTESIAN_POINT ( 'NONE',  ( 39.29254315202757653, 1.196159133578084788, 72.81632618279324731 ) ) ;
#25290=CARTESIAN_POINT ( 'NONE',  ( 39.95015449827720744, -29.00384086642191406, 71.96809898377885872 ) ) ;
#25299=CARTESIAN_POINT ( 'NONE',  ( 37.89291511884479036, -6.503840866421909617, 72.49843995877331793 ) ) ;
#25308=CARTESIAN_POINT ( 'NONE',  ( 39.41296390513587511, -10.41368208888610170, 71.67976084211552745 ) ) ;
#25309=CARTESIAN_POINT ( 'NONE',  ( 37.12184278917507640, -11.51368208888610134, 71.43714994484034264 ) ) ;
#25316=CARTESIAN_POINT ( 'NONE',  ( 36.49096545463212493, -18.10384086642191193, 71.32335560751961623 ) ) ;
#25319=CARTESIAN_POINT ( 'NONE',  ( 38.37017380507020192, -20.01368208888610312, 72.51602215082118619 ) ) ;
#25322=CARTESIAN_POINT ( 'NONE',  ( 36.80608444377001121, -15.31368208888610027, 70.35351908239860563 ) ) ;
#25333=CARTESIAN_POINT ( 'NONE',  ( 40.55423172469004101, -13.20384086642191690, 70.70992431699450265 ) ) ;
#25336=CARTESIAN_POINT ( 'NONE',  ( 38.37017380507020192, -12.01368208888610845, 73.11602215082116629 ) ) ;
#25342=CARTESIAN_POINT ( 'NONE',  ( 39.73277004305198545, -20.21368208888611306, 73.23812341099225875 ) ) ;
#25352=CARTESIAN_POINT ( 'NONE',  ( 37.38336156205273397, -9.903840866421909084, 70.63227792289248441 ) ) ;
#25353=CARTESIAN_POINT ( 'NONE',  ( 40.14115730948191185, 1.486317911113896884, 71.32335560751963044 ) ) ;
#25359=CARTESIAN_POINT ( 'NONE',  ( 39.75915168707251723, 1.096159133578084699, 72.49904802271743165 ) ) ;
#25360=CARTESIAN_POINT ( 'NONE',  ( 39.24876120206128860, -26.71368208888610596, 70.63227792289242757 ) ) ;
#25361=CARTESIAN_POINT ( 'NONE',  ( 37.61123632939165873, -3.913682088886108357, 73.73360434286902887 ) ) ;
#25365=CARTESIAN_POINT ( 'NONE',  ( 37.38336156205273397, -5.903840866421909972, 70.63227792289248441 ) ) ;
#25374=CARTESIAN_POINT ( 'NONE',  ( 39.64521430340305841, -12.80384086642191832, 73.30173637941818754 ) ) ;
#25376=CARTESIAN_POINT ( 'NONE',  ( 36.87297107704152666, -13.71368208888610773, 72.49904802271740323 ) ) ;
#25380=CARTESIAN_POINT ( 'NONE',  ( 40.14115730948191185, -3.103840866421910150, 71.43714994484034264 ) ) ;
#25384=CARTESIAN_POINT ( 'NONE',  ( 39.98359781491296161, -18.41368208888610880, 71.86517103874047052 ) ) ;
#25388=CARTESIAN_POINT ( 'NONE',  ( 39.98359781491296161, -15.20384086642191157, 70.89533451361945993 ) ) ;
#25390=CARTESIAN_POINT ( 'NONE',  ( 39.29254315202756231, -16.81368208888610383, 69.94417936956672577 ) ) ;
#25392=CARTESIAN_POINT ( 'NONE',  ( 36.11133435605973574, -19.61368208888610454, 72.15350918040385864 ) ) ;
#25396=CARTESIAN_POINT ( 'NONE',  ( 39.02742774030101458, -25.40384086642191264, 70.49320253461758057 ) ) ;
#25402=CARTESIAN_POINT ( 'NONE',  ( 38.82593461698265003, -0.7038408664219141242, 73.13360434286904876 ) ) ;
#25407=CARTESIAN_POINT ( 'NONE',  ( 40.55423172469004811, -0.4136820888861054146, 72.05058123536544201 ) ) ;
#25414=CARTESIAN_POINT ( 'NONE',  ( 39.29254315202757653, -18.80384086642191477, 72.81632618279321889 ) ) ;
#25416=VERTEX_POINT ( 'NONE', #24195 ) ;
#25420=CARTESIAN_POINT ( 'NONE',  ( 37.21915885897815457, -8.203840866421909794, 71.67976084211552745 ) ) ;
#25428=CARTESIAN_POINT ( 'NONE',  ( 39.37952058850012804, -10.61368208888610276, 70.97781676520601479 ) ) ;
#25432=CARTESIAN_POINT ( 'NONE',  ( 37.89291511884476904, -13.11368208888610454, 70.26206559358661252 ) ) ;
#25439=CARTESIAN_POINT ( 'NONE',  ( 37.80618814713138676, -19.70384086642190624, 69.62690120949091011 ) ) ;
#25446=CARTESIAN_POINT ( 'NONE',  ( 37.69225076346193504, -19.81368208888610383, 72.33091598616826445 ) ) ;
#25451=CARTESIAN_POINT ( 'NONE',  ( 37.69796330110504101, -13.11368208888609921, 69.66206559358663242 ) ) ;
#25464=CARTESIAN_POINT ( 'NONE',  ( 38.26194895904384197, -12.60384086642191903, 73.71602215082113219 ) ) ;
#25468=CARTESIAN_POINT ( 'NONE',  ( 39.75915168707250302, -14.71368208888610063, 70.26145752964251301 ) ) ;
#25475=CARTESIAN_POINT ( 'NONE',  ( 40.33642880535524000, -14.31368208888610738, 72.77780686321126780 ) ) ;
#25487=CARTESIAN_POINT ( 'NONE',  ( 37.60469502381300799, -14.40384086642191441, 72.26730301774234988 ) ) ;
#25488=CARTESIAN_POINT ( 'NONE',  ( 37.69225076346193504, 0.1961591335780874246, 70.42958956619168021 ) ) ;
ENDSEC;
END-ISO-10303-21;
